ISO-10303-21;
HEADER;
/* Generated by software containing ST-Developer
 * from STEP Tools, Inc. (www.steptools.com) 
 */

FILE_DESCRIPTION(
/* description */ (''),
/* implementation_level */ '2;1');

FILE_NAME(
/* name */ 'Socket head cap screw M3x16.step',
/* time_stamp */ '2026-11-12T00:53:40-08:00',
/* author */ (''),
/* organization */ (''),
/* preprocessor_version */ 'ST-DEVELOPER v20.2',
/* originating_system */ 'Autodesk Translation Framework v15.17.0.0',
/* authorisation */ '');

FILE_SCHEMA (('AUTOMOTIVE_DESIGN { 1 0 10303 214 3 1 1 }'));
ENDSEC;

DATA;
#10=MECHANICAL_DESIGN_GEOMETRIC_PRESENTATION_REPRESENTATION('',(#577),#22129);
#75=CONICAL_SURFACE('',#9377,0.1,0.785398163397448);
#156=B_SPLINE_SURFACE_WITH_KNOTS('',3,3,((#18792,#18793,#18794,#18795,#18796,
#18797,#18798,#18799,#18800,#18801,#18802,#18803,#18804,#18805,#18806,#18807,
#18808,#18809,#18810,#18811,#18812,#18813,#18814,#18815,#18816,#18817,#18818,
#18819,#18820,#18821,#18822,#18823,#18824,#18825,#18826,#18827,#18828,#18829,
#18830,#18831,#18832,#18833,#18834,#18835,#18836,#18837,#18838,#18839,#18840,
#18841,#18842,#18843,#18844,#18845,#18846,#18847,#18848,#18849,#18850,#18851,
#18852,#18853,#18854,#18855,#18856,#18857,#18858,#18859,#18860,#18861,#18862,
#18863,#18864,#18865,#18866,#18867,#18868,#18869,#18870,#18871,#18872,#18873,
#18874,#18875,#18876,#18877,#18878,#18879,#18880,#18881,#18882,#18883,#18884,
#18885,#18886,#18887,#18888,#18889,#18890,#18891,#18892,#18893,#18894,#18895,
#18896,#18897,#18898,#18899,#18900,#18901,#18902,#18903,#18904,#18905,#18906,
#18907,#18908,#18909,#18910,#18911,#18912,#18913,#18914,#18915,#18916,#18917,
#18918,#18919,#18920,#18921,#18922,#18923,#18924,#18925,#18926,#18927,#18928,
#18929,#18930,#18931,#18932,#18933,#18934,#18935,#18936,#18937,#18938,#18939,
#18940,#18941,#18942,#18943,#18944,#18945,#18946,#18947,#18948,#18949,#18950,
#18951,#18952,#18953,#18954,#18955,#18956,#18957,#18958,#18959,#18960,#18961,
#18962,#18963,#18964,#18965,#18966,#18967,#18968,#18969,#18970,#18971,#18972,
#18973,#18974,#18975,#18976,#18977,#18978,#18979,#18980,#18981,#18982,#18983,
#18984,#18985,#18986,#18987),(#18988,#18989,#18990,#18991,#18992,#18993,
#18994,#18995,#18996,#18997,#18998,#18999,#19000,#19001,#19002,#19003,#19004,
#19005,#19006,#19007,#19008,#19009,#19010,#19011,#19012,#19013,#19014,#19015,
#19016,#19017,#19018,#19019,#19020,#19021,#19022,#19023,#19024,#19025,#19026,
#19027,#19028,#19029,#19030,#19031,#19032,#19033,#19034,#19035,#19036,#19037,
#19038,#19039,#19040,#19041,#19042,#19043,#19044,#19045,#19046,#19047,#19048,
#19049,#19050,#19051,#19052,#19053,#19054,#19055,#19056,#19057,#19058,#19059,
#19060,#19061,#19062,#19063,#19064,#19065,#19066,#19067,#19068,#19069,#19070,
#19071,#19072,#19073,#19074,#19075,#19076,#19077,#19078,#19079,#19080,#19081,
#19082,#19083,#19084,#19085,#19086,#19087,#19088,#19089,#19090,#19091,#19092,
#19093,#19094,#19095,#19096,#19097,#19098,#19099,#19100,#19101,#19102,#19103,
#19104,#19105,#19106,#19107,#19108,#19109,#19110,#19111,#19112,#19113,#19114,
#19115,#19116,#19117,#19118,#19119,#19120,#19121,#19122,#19123,#19124,#19125,
#19126,#19127,#19128,#19129,#19130,#19131,#19132,#19133,#19134,#19135,#19136,
#19137,#19138,#19139,#19140,#19141,#19142,#19143,#19144,#19145,#19146,#19147,
#19148,#19149,#19150,#19151,#19152,#19153,#19154,#19155,#19156,#19157,#19158,
#19159,#19160,#19161,#19162,#19163,#19164,#19165,#19166,#19167,#19168,#19169,
#19170,#19171,#19172,#19173,#19174,#19175,#19176,#19177,#19178,#19179,#19180,
#19181,#19182,#19183),(#19184,#19185,#19186,#19187,#19188,#19189,#19190,
#19191,#19192,#19193,#19194,#19195,#19196,#19197,#19198,#19199,#19200,#19201,
#19202,#19203,#19204,#19205,#19206,#19207,#19208,#19209,#19210,#19211,#19212,
#19213,#19214,#19215,#19216,#19217,#19218,#19219,#19220,#19221,#19222,#19223,
#19224,#19225,#19226,#19227,#19228,#19229,#19230,#19231,#19232,#19233,#19234,
#19235,#19236,#19237,#19238,#19239,#19240,#19241,#19242,#19243,#19244,#19245,
#19246,#19247,#19248,#19249,#19250,#19251,#19252,#19253,#19254,#19255,#19256,
#19257,#19258,#19259,#19260,#19261,#19262,#19263,#19264,#19265,#19266,#19267,
#19268,#19269,#19270,#19271,#19272,#19273,#19274,#19275,#19276,#19277,#19278,
#19279,#19280,#19281,#19282,#19283,#19284,#19285,#19286,#19287,#19288,#19289,
#19290,#19291,#19292,#19293,#19294,#19295,#19296,#19297,#19298,#19299,#19300,
#19301,#19302,#19303,#19304,#19305,#19306,#19307,#19308,#19309,#19310,#19311,
#19312,#19313,#19314,#19315,#19316,#19317,#19318,#19319,#19320,#19321,#19322,
#19323,#19324,#19325,#19326,#19327,#19328,#19329,#19330,#19331,#19332,#19333,
#19334,#19335,#19336,#19337,#19338,#19339,#19340,#19341,#19342,#19343,#19344,
#19345,#19346,#19347,#19348,#19349,#19350,#19351,#19352,#19353,#19354,#19355,
#19356,#19357,#19358,#19359,#19360,#19361,#19362,#19363,#19364,#19365,#19366,
#19367,#19368,#19369,#19370,#19371,#19372,#19373,#19374,#19375,#19376,#19377,
#19378,#19379),(#19380,#19381,#19382,#19383,#19384,#19385,#19386,#19387,
#19388,#19389,#19390,#19391,#19392,#19393,#19394,#19395,#19396,#19397,#19398,
#19399,#19400,#19401,#19402,#19403,#19404,#19405,#19406,#19407,#19408,#19409,
#19410,#19411,#19412,#19413,#19414,#19415,#19416,#19417,#19418,#19419,#19420,
#19421,#19422,#19423,#19424,#19425,#19426,#19427,#19428,#19429,#19430,#19431,
#19432,#19433,#19434,#19435,#19436,#19437,#19438,#19439,#19440,#19441,#19442,
#19443,#19444,#19445,#19446,#19447,#19448,#19449,#19450,#19451,#19452,#19453,
#19454,#19455,#19456,#19457,#19458,#19459,#19460,#19461,#19462,#19463,#19464,
#19465,#19466,#19467,#19468,#19469,#19470,#19471,#19472,#19473,#19474,#19475,
#19476,#19477,#19478,#19479,#19480,#19481,#19482,#19483,#19484,#19485,#19486,
#19487,#19488,#19489,#19490,#19491,#19492,#19493,#19494,#19495,#19496,#19497,
#19498,#19499,#19500,#19501,#19502,#19503,#19504,#19505,#19506,#19507,#19508,
#19509,#19510,#19511,#19512,#19513,#19514,#19515,#19516,#19517,#19518,#19519,
#19520,#19521,#19522,#19523,#19524,#19525,#19526,#19527,#19528,#19529,#19530,
#19531,#19532,#19533,#19534,#19535,#19536,#19537,#19538,#19539,#19540,#19541,
#19542,#19543,#19544,#19545,#19546,#19547,#19548,#19549,#19550,#19551,#19552,
#19553,#19554,#19555,#19556,#19557,#19558,#19559,#19560,#19561,#19562,#19563,
#19564,#19565,#19566,#19567,#19568,#19569,#19570,#19571,#19572,#19573,#19574,
#19575)),.UNSPECIFIED.,.F.,.F.,.F.,(4,4),(4,1,1,1,1,1,1,1,1,1,1,1,1,1,1,
1,1,1,1,1,1,1,1,1,1,1,1,1,1,1,1,1,1,1,1,1,1,1,1,1,1,1,1,1,1,1,1,1,1,1,1,
1,1,1,1,1,1,1,1,1,1,1,1,1,1,1,1,1,1,1,1,1,1,1,1,1,1,1,1,1,1,1,1,1,1,1,1,
1,1,1,1,1,1,1,1,1,1,1,1,1,1,1,1,1,1,1,1,1,1,1,1,1,1,1,1,1,1,1,1,1,1,1,1,
1,1,1,1,1,1,1,1,1,1,1,1,1,1,1,1,1,1,1,1,1,1,1,1,1,1,1,1,1,1,1,1,1,1,1,1,
1,1,1,1,1,1,1,1,1,1,1,1,1,1,1,1,1,1,1,1,1,1,1,1,1,1,1,1,1,1,1,1,1,1,4),
(0.,0.0329955678841871),(11.6159397475006,12.61358260836,13.6112254692194,
14.6088683300789,15.6065111909383,16.6041540517977,17.6017969126571,18.5994397735165,
19.5970826343759,20.5947254952353,21.5923683560947,22.5900112169541,23.5876540778135,
24.5852969386729,25.5829397995323,26.5805826603917,27.5782255212511,28.5758683821105,
29.5735112429699,30.5711541038294,31.5687969646888,32.5664398255482,33.5640826864076,
34.561725547267,35.5593684081264,36.5570112689858,37.5546541298452,38.5522969907046,
39.549939851564,40.5475827124234,41.5452255732828,42.5428684341422,43.5405112950016,
44.538154155861,45.5357970167204,46.5334398775799,47.5310827384393,48.5287255992987,
49.5263684601581,50.5240113210175,51.5216541818769,52.5192970427363,53.5169399035957,
54.5145827644551,55.5122256253145,56.5098684861739,57.5075113470333,58.5051542078927,
59.5027970687521,60.5004399296115,61.4980827904709,62.4957256513303,63.4933685121897,
64.4910113730492,65.4886542339086,66.486297094768,67.4839399556274,68.4815828164868,
69.4792256773462,70.4768685382056,71.474511399065,72.4721542599244,73.4697971207838,
74.4674399816432,75.4650828425026,76.462725703362,77.4603685642214,78.4580114250808,
79.4556542859402,80.4532971467996,81.4509400076591,82.4485828685185,83.4462257293779,
84.4438685902373,85.4415114510967,86.4391543119561,87.4367971728155,88.4344400336749,
89.4320828945343,90.4297257553937,91.4273686162531,92.4250114771125,93.4226543379719,
94.4202971988313,95.4179400596907,96.4155829205502,97.4132257814096,98.410868642269,
99.4085115031284,100.406154363988,101.403797224847,102.401440085707,103.399082946566,
104.396725807425,105.394368668285,106.392011529144,107.389654390004,108.387297250863,
109.384940111722,110.382582972582,111.380225833441,112.377868694301,113.37551155516,
114.373154416019,115.370797276879,116.368440137738,117.366082998598,118.363725859457,
119.361368720316,120.359011581176,121.356654442035,122.354297302895,123.351940163754,
124.349583024614,125.347225885473,126.344868746332,127.342511607192,128.340154468051,
129.337797328911,130.33544018977,131.333083050629,132.330725911489,133.328368772348,
134.326011633208,135.323654494067,136.321297354926,137.318940215786,138.316583076645,
139.314225937505,140.311868798364,141.309511659223,142.307154520083,143.304797380942,
144.302440241802,145.300083102661,146.29772596352,147.29536882438,148.293011685239,
149.290654546099,150.288297406958,151.285940267817,152.283583128677,153.281225989536,
154.278868850396,155.276511711255,156.274154572115,157.271797432974,158.269440293833,
159.267083154693,160.264726015552,161.262368876412,162.260011737271,163.25765459813,
164.25529745899,165.252940319849,166.250583180709,167.248226041568,168.245868902427,
169.243511763287,170.241154624146,171.238797485006,172.236440345865,173.234083206724,
174.231726067584,175.229368928443,176.227011789303,177.224654650162,178.222297511021,
179.219940371881,180.21758323274,181.2152260936,182.212868954459,183.210511815318,
184.208154676178,185.205797537037,186.203440397897,187.201083258756,188.198726119616,
189.196368980475,190.194011841334,191.191654702194,192.189297563053,193.186940423913,
194.184583284772,195.182226145631,196.179869006491,197.17751186735,198.17515472821,
199.172797589069,200.170440449928,201.168083310788,202.165726171647,203.163369032507,
204.161011893366),.UNSPECIFIED.);
#157=B_SPLINE_SURFACE_WITH_KNOTS('',3,3,((#19665,#19666,#19667,#19668,#19669,
#19670,#19671,#19672,#19673,#19674,#19675,#19676,#19677,#19678,#19679,#19680,
#19681,#19682,#19683,#19684,#19685,#19686,#19687,#19688,#19689,#19690,#19691,
#19692,#19693,#19694,#19695,#19696,#19697,#19698,#19699,#19700,#19701,#19702,
#19703,#19704,#19705,#19706,#19707,#19708,#19709,#19710,#19711,#19712,#19713,
#19714,#19715,#19716,#19717,#19718,#19719,#19720,#19721,#19722,#19723,#19724,
#19725,#19726,#19727,#19728,#19729,#19730,#19731,#19732,#19733,#19734,#19735,
#19736,#19737,#19738,#19739,#19740,#19741,#19742,#19743,#19744,#19745,#19746,
#19747,#19748,#19749,#19750,#19751,#19752,#19753,#19754,#19755,#19756,#19757,
#19758,#19759,#19760,#19761,#19762,#19763,#19764,#19765,#19766,#19767,#19768,
#19769,#19770,#19771,#19772,#19773,#19774,#19775,#19776,#19777,#19778,#19779,
#19780,#19781,#19782,#19783,#19784,#19785,#19786,#19787,#19788,#19789,#19790,
#19791,#19792,#19793,#19794,#19795,#19796,#19797,#19798,#19799,#19800,#19801,
#19802,#19803,#19804,#19805,#19806,#19807,#19808,#19809,#19810,#19811,#19812,
#19813,#19814,#19815,#19816,#19817,#19818,#19819,#19820,#19821,#19822,#19823,
#19824,#19825,#19826,#19827,#19828,#19829,#19830,#19831,#19832,#19833,#19834,
#19835,#19836,#19837,#19838,#19839,#19840,#19841,#19842,#19843,#19844,#19845,
#19846,#19847,#19848,#19849,#19850,#19851,#19852,#19853,#19854,#19855,#19856,
#19857,#19858,#19859,#19860,#19861,#19862),(#19863,#19864,#19865,#19866,
#19867,#19868,#19869,#19870,#19871,#19872,#19873,#19874,#19875,#19876,#19877,
#19878,#19879,#19880,#19881,#19882,#19883,#19884,#19885,#19886,#19887,#19888,
#19889,#19890,#19891,#19892,#19893,#19894,#19895,#19896,#19897,#19898,#19899,
#19900,#19901,#19902,#19903,#19904,#19905,#19906,#19907,#19908,#19909,#19910,
#19911,#19912,#19913,#19914,#19915,#19916,#19917,#19918,#19919,#19920,#19921,
#19922,#19923,#19924,#19925,#19926,#19927,#19928,#19929,#19930,#19931,#19932,
#19933,#19934,#19935,#19936,#19937,#19938,#19939,#19940,#19941,#19942,#19943,
#19944,#19945,#19946,#19947,#19948,#19949,#19950,#19951,#19952,#19953,#19954,
#19955,#19956,#19957,#19958,#19959,#19960,#19961,#19962,#19963,#19964,#19965,
#19966,#19967,#19968,#19969,#19970,#19971,#19972,#19973,#19974,#19975,#19976,
#19977,#19978,#19979,#19980,#19981,#19982,#19983,#19984,#19985,#19986,#19987,
#19988,#19989,#19990,#19991,#19992,#19993,#19994,#19995,#19996,#19997,#19998,
#19999,#20000,#20001,#20002,#20003,#20004,#20005,#20006,#20007,#20008,#20009,
#20010,#20011,#20012,#20013,#20014,#20015,#20016,#20017,#20018,#20019,#20020,
#20021,#20022,#20023,#20024,#20025,#20026,#20027,#20028,#20029,#20030,#20031,
#20032,#20033,#20034,#20035,#20036,#20037,#20038,#20039,#20040,#20041,#20042,
#20043,#20044,#20045,#20046,#20047,#20048,#20049,#20050,#20051,#20052,#20053,
#20054,#20055,#20056,#20057,#20058,#20059,#20060),(#20061,#20062,#20063,
#20064,#20065,#20066,#20067,#20068,#20069,#20070,#20071,#20072,#20073,#20074,
#20075,#20076,#20077,#20078,#20079,#20080,#20081,#20082,#20083,#20084,#20085,
#20086,#20087,#20088,#20089,#20090,#20091,#20092,#20093,#20094,#20095,#20096,
#20097,#20098,#20099,#20100,#20101,#20102,#20103,#20104,#20105,#20106,#20107,
#20108,#20109,#20110,#20111,#20112,#20113,#20114,#20115,#20116,#20117,#20118,
#20119,#20120,#20121,#20122,#20123,#20124,#20125,#20126,#20127,#20128,#20129,
#20130,#20131,#20132,#20133,#20134,#20135,#20136,#20137,#20138,#20139,#20140,
#20141,#20142,#20143,#20144,#20145,#20146,#20147,#20148,#20149,#20150,#20151,
#20152,#20153,#20154,#20155,#20156,#20157,#20158,#20159,#20160,#20161,#20162,
#20163,#20164,#20165,#20166,#20167,#20168,#20169,#20170,#20171,#20172,#20173,
#20174,#20175,#20176,#20177,#20178,#20179,#20180,#20181,#20182,#20183,#20184,
#20185,#20186,#20187,#20188,#20189,#20190,#20191,#20192,#20193,#20194,#20195,
#20196,#20197,#20198,#20199,#20200,#20201,#20202,#20203,#20204,#20205,#20206,
#20207,#20208,#20209,#20210,#20211,#20212,#20213,#20214,#20215,#20216,#20217,
#20218,#20219,#20220,#20221,#20222,#20223,#20224,#20225,#20226,#20227,#20228,
#20229,#20230,#20231,#20232,#20233,#20234,#20235,#20236,#20237,#20238,#20239,
#20240,#20241,#20242,#20243,#20244,#20245,#20246,#20247,#20248,#20249,#20250,
#20251,#20252,#20253,#20254,#20255,#20256,#20257,#20258),(#20259,#20260,
#20261,#20262,#20263,#20264,#20265,#20266,#20267,#20268,#20269,#20270,#20271,
#20272,#20273,#20274,#20275,#20276,#20277,#20278,#20279,#20280,#20281,#20282,
#20283,#20284,#20285,#20286,#20287,#20288,#20289,#20290,#20291,#20292,#20293,
#20294,#20295,#20296,#20297,#20298,#20299,#20300,#20301,#20302,#20303,#20304,
#20305,#20306,#20307,#20308,#20309,#20310,#20311,#20312,#20313,#20314,#20315,
#20316,#20317,#20318,#20319,#20320,#20321,#20322,#20323,#20324,#20325,#20326,
#20327,#20328,#20329,#20330,#20331,#20332,#20333,#20334,#20335,#20336,#20337,
#20338,#20339,#20340,#20341,#20342,#20343,#20344,#20345,#20346,#20347,#20348,
#20349,#20350,#20351,#20352,#20353,#20354,#20355,#20356,#20357,#20358,#20359,
#20360,#20361,#20362,#20363,#20364,#20365,#20366,#20367,#20368,#20369,#20370,
#20371,#20372,#20373,#20374,#20375,#20376,#20377,#20378,#20379,#20380,#20381,
#20382,#20383,#20384,#20385,#20386,#20387,#20388,#20389,#20390,#20391,#20392,
#20393,#20394,#20395,#20396,#20397,#20398,#20399,#20400,#20401,#20402,#20403,
#20404,#20405,#20406,#20407,#20408,#20409,#20410,#20411,#20412,#20413,#20414,
#20415,#20416,#20417,#20418,#20419,#20420,#20421,#20422,#20423,#20424,#20425,
#20426,#20427,#20428,#20429,#20430,#20431,#20432,#20433,#20434,#20435,#20436,
#20437,#20438,#20439,#20440,#20441,#20442,#20443,#20444,#20445,#20446,#20447,
#20448,#20449,#20450,#20451,#20452,#20453,#20454,#20455,#20456)),
 .UNSPECIFIED.,.F.,.F.,.F.,(4,4),(4,1,1,1,1,1,1,1,1,1,1,1,1,1,1,1,1,1,1,
1,1,1,1,1,1,1,1,1,1,1,1,1,1,1,1,1,1,1,1,1,1,1,1,1,1,1,1,1,1,1,1,1,1,1,1,
1,1,1,1,1,1,1,1,1,1,1,1,1,1,1,1,1,1,1,1,1,1,1,1,1,1,1,1,1,1,1,1,1,1,1,1,
1,1,1,1,1,1,1,1,1,1,1,1,1,1,1,1,1,1,1,1,1,1,1,1,1,1,1,1,1,1,1,1,1,1,1,1,
1,1,1,1,1,1,1,1,1,1,1,1,1,1,1,1,1,1,1,1,1,1,1,1,1,1,1,1,1,1,1,1,1,1,1,1,
1,1,1,1,1,1,1,1,1,1,1,1,1,1,1,1,1,1,1,1,1,1,1,1,1,1,1,1,1,1,1,1,4),(0.,
0.0329955678841871),(8.30203615430855,9.30007843543257,10.2981207165566,
11.2961629976806,12.2942052788047,13.2922475599287,14.2902898410527,15.2883321221767,
16.2863744033008,17.2844166844248,18.2824589655488,19.2805012466728,20.2785435277969,
21.2765858089209,22.2746280900449,23.272670371169,24.270712652293,25.268754933417,
26.266797214541,27.2648394956651,28.2628817767891,29.2609240579131,30.2589663390371,
31.2570086201612,32.2550509012852,33.2530931824092,34.2511354635333,35.2491777446573,
36.2472200257813,37.2452623069053,38.2433045880294,39.2413468691534,40.2393891502774,
41.2374314314014,42.2354737125255,43.2335159936495,44.2315582747735,45.2296005558975,
46.2276428370216,47.2256851181456,48.2237273992696,49.2217696803937,50.2198119615177,
51.2178542426417,52.2158965237657,53.2139388048898,54.2119810860138,55.2100233671378,
56.2080656482619,57.2061079293859,58.2041502105099,59.2021924916339,60.200234772758,
61.198277053882,62.196319335006,63.19436161613,64.1924038972541,65.1904461783781,
66.1884884595021,67.1865307406262,68.1845730217502,69.1826153028742,70.1806575839982,
71.1786998651223,72.1767421462463,73.1747844273703,74.1728267084943,75.1708689896184,
76.1689112707424,77.1669535518664,78.1649958329905,79.1630381141145,80.1610803952385,
81.1591226763625,82.1571649574865,83.1552072386106,84.1532495197346,85.1512918008586,
86.1493340819827,87.1473763631067,88.1454186442307,89.1434609253548,90.1415032064788,
91.1395454876028,92.1375877687268,93.1356300498508,94.1336723309749,95.1317146120989,
96.1297568932229,97.127799174347,98.125841455471,99.123883736595,100.121926017719,
101.119968298843,102.118010579967,103.116052861091,104.114095142215,105.112137423339,
106.110179704463,107.108221985587,108.106264266711,109.104306547835,110.102348828959,
111.100391110083,112.098433391207,113.096475672331,114.094517953455,115.092560234579,
116.090602515703,117.088644796828,118.086687077952,119.084729359076,120.0827716402,
121.080813921324,122.078856202448,123.076898483572,124.074940764696,125.07298304582,
126.071025326944,127.069067608068,128.067109889192,129.065152170316,130.06319445144,
131.061236732564,132.059279013688,133.057321294812,134.055363575936,135.05340585706,
136.051448138184,137.049490419308,138.047532700432,139.045574981556,140.04361726268,
141.041659543804,142.039701824928,143.037744106052,144.035786387176,145.0338286683,
146.031870949424,147.029913230548,148.027955511672,149.025997792796,150.02404007392,
151.022082355044,152.020124636168,153.018166917292,154.016209198417,155.014251479541,
156.012293760665,157.010336041789,158.008378322913,159.006420604037,160.004462885161,
161.002505166285,162.000547447409,162.998589728533,163.996632009657,164.994674290781,
165.992716571905,166.990758853029,167.988801134153,168.986843415277,169.984885696401,
170.982927977525,171.980970258649,172.979012539773,173.977054820897,174.975097102021,
175.973139383145,176.971181664269,177.969223945393,178.967266226517,179.965308507641,
180.963350788765,181.961393069889,182.959435351013,183.957477632137,184.955519913261,
185.953562194385,186.951604475509,187.949646756633,188.947689037757,189.945731318881,
190.943773600006,191.94181588113,192.939858162254,193.937900443378,194.935942724502,
195.933985005626,196.93202728675,197.930069567874,198.928111848998,199.926154130122,
200.924196411246,201.92223869237,202.920280973494),.UNSPECIFIED.);
#372=B_SPLINE_CURVE_WITH_KNOTS('',3,(#16416,#16417,#16418,#16419,#16420,
#16421,#16422,#16423,#16424,#16425),.UNSPECIFIED.,.F.,.F.,(4,3,3,4),(-4.09202352044852,
-3.99057144343763,-2.99292858257822,-2.07317267331971),.UNSPECIFIED.);
#373=B_SPLINE_CURVE_WITH_KNOTS('',3,(#16428,#16429,#16430,#16431,#16432,
#16433,#16434),.UNSPECIFIED.,.F.,.F.,(4,3,4),(0.,0.998042281124014,1.12274180646116),
 .UNSPECIFIED.);
#374=B_SPLINE_CURVE_WITH_KNOTS('',3,(#16439,#16440,#16441,#16442,#16443,
#16444,#16445,#16446,#16447,#16448,#16449,#16450,#16451,#16452,#16453,#16454,
#16455,#16456,#16457,#16458,#16459,#16460),.UNSPECIFIED.,.F.,.F.,(4,3,3,
3,3,3,3,4),(-10.3752088276281,-9.97642860859406,-8.97878574773466,-7.98114288687525,
-6.98350002601584,-5.98585716515644,-4.98821430429703,-4.09202352044852),
 .UNSPECIFIED.);
#375=B_SPLINE_CURVE_WITH_KNOTS('',3,(#16461,#16462,#16463,#16464,#16465,
#16466,#16467,#16468,#16469,#16470,#16471,#16472,#16473,#16474,#16475,#16476,
#16477,#16478,#16479,#16480,#16481,#16482),.UNSPECIFIED.,.F.,.F.,(4,3,3,
3,3,3,3,4),(1.12274180646116,1.99608456224804,2.99412684337208,3.99216912449611,
4.99021140562014,5.98825368674417,6.98629596786821,7.40592711364074),
 .UNSPECIFIED.);
#376=B_SPLINE_CURVE_WITH_KNOTS('',3,(#16487,#16488,#16489,#16490,#16491,
#16492,#16493,#16494,#16495,#16496,#16497,#16498,#16499,#16500,#16501,#16502,
#16503,#16504,#16505,#16506,#16507,#16508),.UNSPECIFIED.,.F.,.F.,(4,3,3,
3,3,3,3,4),(-16.6583941348077,-15.9622857737505,-14.9646429128911,-13.9670000520317,
-12.9693571911723,-11.9717143303129,-10.9740714694535,-10.3752088276281),
 .UNSPECIFIED.);
#377=B_SPLINE_CURVE_WITH_KNOTS('',3,(#16509,#16510,#16511,#16512,#16513,
#16514,#16515,#16516,#16517,#16518,#16519,#16520,#16521,#16522,#16523,#16524,
#16525,#16526,#16527,#16528,#16529,#16530),.UNSPECIFIED.,.F.,.F.,(4,3,3,
3,3,3,3,4),(7.40592711364074,7.98433824899223,8.98238053011626,9.98042281124028,
10.9784650923643,11.9765073734883,12.9745496546124,13.6891124208203),
 .UNSPECIFIED.);
#378=B_SPLINE_CURVE_WITH_KNOTS('',3,(#16535,#16536,#16537,#16538,#16539,
#16540,#16541,#16542,#16543,#16544,#16545,#16546,#16547,#16548,#16549,#16550,
#16551,#16552,#16553,#16554,#16555,#16556),.UNSPECIFIED.,.F.,.F.,(4,3,3,
3,3,3,3,4),(-22.9415794419873,-21.9481429389069,-20.9505000780475,-19.9528572171881,
-18.9552143563287,-17.9575714954693,-16.9599286346099,-16.6583941348077),
 .UNSPECIFIED.);
#379=B_SPLINE_CURVE_WITH_KNOTS('',3,(#16557,#16558,#16559,#16560,#16561,
#16562,#16563,#16564,#16565,#16566,#16567,#16568,#16569,#16570,#16571,#16572,
#16573,#16574,#16575,#16576,#16577,#16578,#16579,#16580,#16581),
 .UNSPECIFIED.,.F.,.F.,(4,3,3,3,3,3,3,3,4),(13.6891124208203,13.9725919357364,
14.9706342168604,15.9686764979844,16.9667187791085,17.9647610602325,18.9628033413565,
19.9608456224805,19.9722977279999),.UNSPECIFIED.);
#380=B_SPLINE_CURVE_WITH_KNOTS('',3,(#16586,#16587,#16588,#16589,#16590,
#16591,#16592,#16593,#16594,#16595,#16596,#16597,#16598,#16599,#16600,#16601,
#16602,#16603,#16604,#16605,#16606,#16607),.UNSPECIFIED.,.F.,.F.,(4,3,3,
3,3,3,3,4),(-29.2247647491669,-28.9316429649228,-27.9340001040634,-26.936357243204,
-25.9387143823446,-24.9410715214852,-23.9434286606257,-22.9415794419873),
 .UNSPECIFIED.);
#381=B_SPLINE_CURVE_WITH_KNOTS('',3,(#16608,#16609,#16610,#16611,#16612,
#16613,#16614,#16615,#16616,#16617,#16618,#16619,#16620,#16621,#16622,#16623,
#16624,#16625,#16626,#16627,#16628,#16629),.UNSPECIFIED.,.F.,.F.,(4,3,3,
3,3,3,3,4),(19.9722977279999,20.9588879036046,21.9569301847286,22.9549724658526,
23.9530147469767,24.9510570281007,25.9490993092247,26.2554830351795),
 .UNSPECIFIED.);
#382=B_SPLINE_CURVE_WITH_KNOTS('',3,(#16634,#16635,#16636,#16637,#16638,
#16639,#16640,#16641,#16642,#16643,#16644,#16645,#16646,#16647,#16648,#16649,
#16650,#16651,#16652,#16653,#16654,#16655),.UNSPECIFIED.,.F.,.F.,(4,3,3,
3,3,3,3,4),(-35.5079500563465,-34.9175001300792,-33.9198572692198,-32.9222144083604,
-31.924571547501,-30.9269286866416,-29.9292858257822,-29.2247647491669),
 .UNSPECIFIED.);
#383=B_SPLINE_CURVE_WITH_KNOTS('',3,(#16656,#16657,#16658,#16659,#16660,
#16661,#16662,#16663,#16664,#16665,#16666,#16667,#16668,#16669,#16670,#16671,
#16672,#16673,#16674,#16675,#16676,#16677),.UNSPECIFIED.,.F.,.F.,(4,3,3,
3,3,3,3,4),(26.2554830351795,26.9471415903487,27.9451838714728,28.9432261525968,
29.9412684337208,30.9393107148448,31.9373529959689,32.5386683423591),
 .UNSPECIFIED.);
#384=B_SPLINE_CURVE_WITH_KNOTS('',3,(#16682,#16683,#16684,#16685,#16686,
#16687,#16688,#16689,#16690,#16691,#16692,#16693,#16694,#16695,#16696,#16697,
#16698,#16699,#16700,#16701,#16702,#16703),.UNSPECIFIED.,.F.,.F.,(4,3,3,
3,3,3,3,4),(-41.791135363526,-40.9033572952357,-39.9057144343762,-38.9080715735168,
-37.9104287126574,-36.912785851798,-35.9151429909386,-35.5079500563465),
 .UNSPECIFIED.);
#385=B_SPLINE_CURVE_WITH_KNOTS('',3,(#16704,#16705,#16706,#16707,#16708,
#16709,#16710,#16711,#16712,#16713,#16714,#16715,#16716,#16717,#16718,#16719,
#16720,#16721,#16722,#16723,#16724,#16725),.UNSPECIFIED.,.F.,.F.,(4,3,3,
3,3,3,3,4),(32.5386683423591,32.9353952770929,33.9334375582169,34.931479839341,
35.929522120465,36.927564401589,37.9256066827131,38.8218536495387),
 .UNSPECIFIED.);
#386=B_SPLINE_CURVE_WITH_KNOTS('',3,(#16730,#16731,#16732,#16733,#16734,
#16735,#16736,#16737,#16738,#16739,#16740,#16741,#16742,#16743,#16744,#16745,
#16746,#16747,#16748,#16749,#16750,#16751,#16752,#16753,#16754),
 .UNSPECIFIED.,.F.,.F.,(4,3,3,3,3,3,3,3,4),(-48.0743206707056,-47.8868573212515,
-46.8892144603921,-45.8915715995327,-44.8939287386733,-43.8962858778139,
-42.8986430169545,-41.9010001560951,-41.791135363526),.UNSPECIFIED.);
#387=B_SPLINE_CURVE_WITH_KNOTS('',3,(#16755,#16756,#16757,#16758,#16759,
#16760,#16761,#16762,#16763,#16764,#16765,#16766,#16767,#16768,#16769,#16770,
#16771,#16772,#16773,#16774,#16775,#16776,#16777,#16778,#16779),
 .UNSPECIFIED.,.F.,.F.,(4,3,3,3,3,3,3,3,4),(38.8218536495387,38.9236489638371,
39.9216912449611,40.9197335260851,41.9177758072091,42.9158180883332,43.9138603694572,
44.9119026505812,45.1050389567183),.UNSPECIFIED.);
#388=B_SPLINE_CURVE_WITH_KNOTS('',3,(#16784,#16785,#16786,#16787,#16788,
#16789,#16790,#16791,#16792,#16793,#16794,#16795,#16796,#16797,#16798,#16799,
#16800,#16801,#16802,#16803,#16804,#16805),.UNSPECIFIED.,.F.,.F.,(4,3,3,
3,3,3,3,4),(-54.3575059778852,-53.8727144864079,-52.8750716255485,-51.8774287646891,
-50.8797859038297,-49.8821430429703,-48.8845001821109,-48.0743206707056),
 .UNSPECIFIED.);
#389=B_SPLINE_CURVE_WITH_KNOTS('',3,(#16806,#16807,#16808,#16809,#16810,
#16811,#16812,#16813,#16814,#16815,#16816,#16817,#16818,#16819,#16820,#16821,
#16822,#16823,#16824,#16825,#16826,#16827),.UNSPECIFIED.,.F.,.F.,(4,3,3,
3,3,3,3,4),(45.1050389567183,45.9099449317052,46.9079872128293,47.9060294939533,
48.9040717750773,49.9021140562014,50.9001563373254,51.3882242638979),
 .UNSPECIFIED.);
#390=B_SPLINE_CURVE_WITH_KNOTS('',3,(#16832,#16833,#16834,#16835,#16836,
#16837,#16838,#16839,#16840,#16841,#16842,#16843,#16844,#16845,#16846,#16847,
#16848,#16849,#16850,#16851,#16852,#16853),.UNSPECIFIED.,.F.,.F.,(4,3,3,
3,3,3,3,4),(-60.6406912850648,-59.8585716515644,-58.860928790705,-57.8632859298455,
-56.8656430689861,-55.8680002081267,-54.8703573472673,-54.3575059778852),
 .UNSPECIFIED.);
#391=B_SPLINE_CURVE_WITH_KNOTS('',3,(#16854,#16855,#16856,#16857,#16858,
#16859,#16860,#16861,#16862,#16863,#16864,#16865,#16866,#16867,#16868,#16869,
#16870,#16871,#16872,#16873,#16874,#16875),.UNSPECIFIED.,.F.,.F.,(4,3,3,
3,3,3,3,4),(51.3882242638979,51.8981986184494,52.8962408995734,53.8942831806975,
54.8923254618215,55.8903677429455,56.8884100240695,57.6714095710775),
 .UNSPECIFIED.);
#392=B_SPLINE_CURVE_WITH_KNOTS('',3,(#16880,#16881,#16882,#16883,#16884,
#16885,#16886,#16887,#16888,#16889,#16890,#16891,#16892,#16893,#16894,#16895,
#16896,#16897,#16898,#16899,#16900,#16901,#16902,#16903,#16904),
 .UNSPECIFIED.,.F.,.F.,(4,3,3,3,3,3,3,3,4),(-66.9238765922444,-66.8420716775802,
-65.8444288167208,-64.8467859558614,-63.849143095002,-62.8515002341426,
-61.8538573732832,-60.8562145124238,-60.6406912850648),.UNSPECIFIED.);
#393=B_SPLINE_CURVE_WITH_KNOTS('',3,(#16905,#16906,#16907,#16908,#16909,
#16910,#16911,#16912,#16913,#16914,#16915,#16916,#16917,#16918,#16919,#16920,
#16921,#16922,#16923,#16924,#16925,#16926,#16927,#16928,#16929),
 .UNSPECIFIED.,.F.,.F.,(4,3,3,3,3,3,3,3,4),(57.6714095710775,57.8864523051936,
58.8844945863176,59.8825368674416,60.8805791485657,61.8786214296897,62.8766637108137,
63.8747059919378,63.9545948782571),.UNSPECIFIED.);
#394=B_SPLINE_CURVE_WITH_KNOTS('',3,(#16934,#16935,#16936,#16937,#16938,
#16939,#16940,#16941,#16942,#16943,#16944,#16945,#16946,#16947,#16948,#16949,
#16950,#16951,#16952,#16953,#16954,#16955),.UNSPECIFIED.,.F.,.F.,(4,3,3,
3,3,3,3,4),(-73.207061899424,-72.8279288427366,-71.8302859818773,-70.8326431210178,
-69.8350002601584,-68.837357399299,-67.8397145384396,-66.9238765922444),
 .UNSPECIFIED.);
#395=B_SPLINE_CURVE_WITH_KNOTS('',3,(#16956,#16957,#16958,#16959,#16960,
#16961,#16962,#16963,#16964,#16965,#16966,#16967,#16968,#16969,#16970,#16971,
#16972,#16973,#16974,#16975,#16976,#16977),.UNSPECIFIED.,.F.,.F.,(4,3,3,
3,3,3,3,4),(63.9545948782571,64.8727482730618,65.8707905541858,66.8688328353098,
67.8668751164338,68.8649173975579,69.8629596786819,70.2377801854366),
 .UNSPECIFIED.);
#396=B_SPLINE_CURVE_WITH_KNOTS('',3,(#16982,#16983,#16984,#16985,#16986,
#16987,#16988,#16989,#16990,#16991,#16992,#16993,#16994,#16995,#16996,#16997,
#16998,#16999,#17000,#17001,#17002,#17003),.UNSPECIFIED.,.F.,.F.,(4,3,3,
3,3,3,3,4),(-79.4902472066036,-78.8137860078931,-77.8161431470337,-76.8185002861743,
-75.8208574253149,-74.8232145644555,-73.825571703596,-73.207061899424),
 .UNSPECIFIED.);
#397=B_SPLINE_CURVE_WITH_KNOTS('',3,(#17004,#17005,#17006,#17007,#17008,
#17009,#17010,#17011,#17012,#17013,#17014,#17015,#17016,#17017,#17018,#17019,
#17020,#17021,#17022,#17023,#17024,#17025),.UNSPECIFIED.,.F.,.F.,(4,3,3,
3,3,3,3,4),(70.2377801854366,70.8610019598059,71.85904424093,72.857086522054,
73.855128803178,74.853171084302,75.8512133654261,76.5209654926162),
 .UNSPECIFIED.);
#398=B_SPLINE_CURVE_WITH_KNOTS('',3,(#17030,#17031,#17032,#17033,#17034,
#17035,#17036,#17037,#17038,#17039,#17040,#17041,#17042,#17043,#17044,#17045,
#17046,#17047,#17048,#17049,#17050,#17051),.UNSPECIFIED.,.F.,.F.,(4,3,3,
3,3,3,3,4),(-85.7734325137832,-84.7996431730495,-83.8020003121901,-82.8043574513307,
-81.8067145904713,-80.8090717296119,-79.8114288687525,-79.4902472066036),
 .UNSPECIFIED.);
#399=B_SPLINE_CURVE_WITH_KNOTS('',3,(#17052,#17053,#17054,#17055,#17056,
#17057,#17058,#17059,#17060,#17061,#17062,#17063,#17064,#17065,#17066,#17067,
#17068,#17069,#17070,#17071,#17072,#17073),.UNSPECIFIED.,.F.,.F.,(4,3,3,
3,3,3,3,4),(76.5209654926162,76.8492556465501,77.8472979276741,78.8453402087982,
79.8433824899222,80.8414247710462,81.8394670521702,82.8041507997958),
 .UNSPECIFIED.);
#400=B_SPLINE_CURVE_WITH_KNOTS('',3,(#17078,#17079,#17080,#17081,#17082,
#17083,#17084,#17085,#17086,#17087,#17088,#17089,#17090,#17091,#17092,#17093,
#17094,#17095,#17096,#17097,#17098,#17099,#17100,#17101,#17102),
 .UNSPECIFIED.,.F.,.F.,(4,3,3,3,3,3,3,3,4),(-92.0566178209628,-91.7831431990654,
-90.7855003382059,-89.7878574773465,-88.7902146164871,-87.7925717556277,
-86.7949288947683,-85.7972860339089,-85.7734325137832),.UNSPECIFIED.);
#401=B_SPLINE_CURVE_WITH_KNOTS('',3,(#17103,#17104,#17105,#17106,#17107,
#17108,#17109,#17110,#17111,#17112,#17113,#17114,#17115,#17116,#17117,#17118,
#17119,#17120,#17121,#17122,#17123,#17124,#17125,#17126,#17127),
 .UNSPECIFIED.,.F.,.F.,(4,3,3,3,3,3,3,3,4),(82.8041507997958,82.8375093332942,
83.8355516144183,84.8335938955423,85.8316361766664,86.8296784577904,87.8277207389144,
88.8257630200384,89.0873361069754),.UNSPECIFIED.);
#402=B_SPLINE_CURVE_WITH_KNOTS('',3,(#17132,#17133,#17134,#17135,#17136,
#17137,#17138,#17139,#17140,#17141,#17142,#17143,#17144,#17145,#17146,#17147,
#17148,#17149,#17150,#17151,#17152,#17153),.UNSPECIFIED.,.F.,.F.,(4,3,3,
3,3,3,3,4),(-98.3398031281424,-97.7690003642218,-96.7713575033624,-95.773714642503,
-94.7760717816436,-93.7784289207842,-92.7807860599248,-92.0566178209628),
 .UNSPECIFIED.);
#403=B_SPLINE_CURVE_WITH_KNOTS('',3,(#17154,#17155,#17156,#17157,#17158,
#17159,#17160,#17161,#17162,#17163,#17164,#17165,#17166,#17167,#17168,#17169,
#17170,#17171,#17172,#17173,#17174,#17175),.UNSPECIFIED.,.F.,.F.,(4,3,3,
3,3,3,3,4),(89.0873361069754,89.8238053011624,90.8218475822865,91.8198898634105,
92.8179321445345,93.8159744256585,94.8140167067826,95.370521414155),
 .UNSPECIFIED.);
#404=B_SPLINE_CURVE_WITH_KNOTS('',3,(#17180,#17181,#17182,#17183,#17184,
#17185,#17186,#17187,#17188,#17189,#17190,#17191,#17192,#17193,#17194,#17195,
#17196,#17197,#17198,#17199,#17200,#17201),.UNSPECIFIED.,.F.,.F.,(4,3,3,
3,3,3,3,4),(-104.622988435322,-103.754857529378,-102.757214668519,-101.759571807659,
-100.7619289468,-99.7642860859406,-98.7666432250812,-98.3398031281424),
 .UNSPECIFIED.);
#405=B_SPLINE_CURVE_WITH_KNOTS('',3,(#17202,#17203,#17204,#17205,#17206,
#17207,#17208,#17209,#17210,#17211,#17212,#17213,#17214,#17215,#17216,#17217,
#17218,#17219,#17220,#17221,#17222,#17223),.UNSPECIFIED.,.F.,.F.,(4,3,3,
3,3,3,3,4),(95.370521414155,95.8120589879066,96.8101012690306,97.8081435501546,
98.8061858312787,99.8042281124027,100.802270393527,101.653706721335),
 .UNSPECIFIED.);
#406=B_SPLINE_CURVE_WITH_KNOTS('',3,(#17228,#17229,#17230,#17231,#17232,
#17233,#17234,#17235,#17236,#17237,#17238,#17239,#17240,#17241,#17242,#17243,
#17244,#17245,#17246,#17247,#17248,#17249,#17250,#17251,#17252),
 .UNSPECIFIED.,.F.,.F.,(4,3,3,3,3,3,3,3,4),(-110.906173742502,-110.738357555394,
-109.740714694535,-108.743071833675,-107.745428972816,-106.747786111956,
-105.750143251097,-104.752500390238,-104.622988435322),.UNSPECIFIED.);
#407=B_SPLINE_CURVE_WITH_KNOTS('',3,(#17253,#17254,#17255,#17256,#17257,
#17258,#17259,#17260,#17261,#17262,#17263,#17264,#17265,#17266,#17267,#17268,
#17269,#17270,#17271,#17272,#17273,#17274,#17275,#17276,#17277),
 .UNSPECIFIED.,.F.,.F.,(4,3,3,3,3,3,3,3,4),(101.653706721335,101.800312674651,
102.798354955775,103.796397236899,104.794439518023,105.792481799147,106.790524080271,
107.788566361395,107.936892028514),.UNSPECIFIED.);
#408=B_SPLINE_CURVE_WITH_KNOTS('',3,(#17282,#17283,#17284,#17285,#17286,
#17287,#17288,#17289,#17290,#17291,#17292,#17293,#17294,#17295,#17296,#17297,
#17298,#17299,#17300,#17301,#17302,#17303),.UNSPECIFIED.,.F.,.F.,(4,3,3,
3,3,3,3,4),(-117.189359049681,-116.724214720551,-115.726571859691,-114.728928998832,
-113.731286137972,-112.733643277113,-111.736000416253,-110.906173742502),
 .UNSPECIFIED.);
#409=B_SPLINE_CURVE_WITH_KNOTS('',3,(#17304,#17305,#17306,#17307,#17308,
#17309,#17310,#17311,#17312,#17313,#17314,#17315,#17316,#17317,#17318,#17319,
#17320,#17321,#17322,#17323,#17324,#17325),.UNSPECIFIED.,.F.,.F.,(4,3,3,
3,3,3,3,4),(107.936892028514,108.786608642519,109.784650923643,110.782693204767,
111.780735485891,112.778777767015,113.776820048139,114.220077335694),
 .UNSPECIFIED.);
#410=B_SPLINE_CURVE_WITH_KNOTS('',3,(#17330,#17331,#17332,#17333,#17334,
#17335,#17336,#17337,#17338,#17339,#17340,#17341,#17342,#17343,#17344,#17345,
#17346,#17347,#17348,#17349,#17350,#17351),.UNSPECIFIED.,.F.,.F.,(4,3,3,
3,3,3,3,4),(-123.472544356861,-122.710071885707,-121.712429024848,-120.714786163988,
-119.717143303129,-118.719500442269,-117.72185758141,-117.189359049681),
 .UNSPECIFIED.);
#411=B_SPLINE_CURVE_WITH_KNOTS('',3,(#17352,#17353,#17354,#17355,#17356,
#17357,#17358,#17359,#17360,#17361,#17362,#17363,#17364,#17365,#17366,#17367,
#17368,#17369,#17370,#17371,#17372,#17373),.UNSPECIFIED.,.F.,.F.,(4,3,3,
3,3,3,3,4),(114.220077335694,114.774862329263,115.772904610387,116.770946891511,
117.768989172635,118.767031453759,119.765073734883,120.503262642873),
 .UNSPECIFIED.);
#412=B_SPLINE_CURVE_WITH_KNOTS('',3,(#17378,#17379,#17380,#17381,#17382,
#17383,#17384,#17385,#17386,#17387,#17388,#17389,#17390,#17391,#17392,#17393,
#17394,#17395,#17396,#17397,#17398,#17399,#17400,#17401,#17402),
 .UNSPECIFIED.,.F.,.F.,(4,3,3,3,3,3,3,3,4),(-129.75572966404,-129.693571911723,
-128.695929050863,-127.698286190004,-126.700643329145,-125.703000468285,
-124.705357607426,-123.707714746566,-123.472544356861),.UNSPECIFIED.);
#413=B_SPLINE_CURVE_WITH_KNOTS('',3,(#17403,#17404,#17405,#17406,#17407,
#17408,#17409,#17410,#17411,#17412,#17413,#17414,#17415,#17416,#17417,#17418,
#17419,#17420,#17421,#17422,#17423,#17424,#17425,#17426,#17427),
 .UNSPECIFIED.,.F.,.F.,(4,3,3,3,3,3,3,3,4),(120.503262642873,120.763116016007,
121.761158297131,122.759200578255,123.757242859379,124.755285140503,125.753327421627,
126.751369702751,126.786447950053),.UNSPECIFIED.);
#414=B_SPLINE_CURVE_WITH_KNOTS('',3,(#17432,#17433,#17434,#17435,#17436,
#17437,#17438,#17439,#17440,#17441,#17442,#17443,#17444,#17445,#17446,#17447,
#17448,#17449,#17450,#17451,#17452,#17453),.UNSPECIFIED.,.F.,.F.,(4,3,3,
3,3,3,3,4),(-136.03891497122,-135.679429076879,-134.68178621602,-133.68414335516,
-132.686500494301,-131.688857633442,-130.691214772582,-129.75572966404),
 .UNSPECIFIED.);
#415=B_SPLINE_CURVE_WITH_KNOTS('',3,(#17454,#17455,#17456,#17457,#17458,
#17459,#17460,#17461,#17462,#17463,#17464,#17465,#17466,#17467,#17468,#17469,
#17470,#17471,#17472,#17473,#17474,#17475),.UNSPECIFIED.,.F.,.F.,(4,3,3,
3,3,3,3,4),(126.786447950053,127.749411983875,128.747454265,129.745496546124,
130.743538827248,131.741581108372,132.739623389496,133.069633257233),
 .UNSPECIFIED.);
#416=B_SPLINE_CURVE_WITH_KNOTS('',3,(#17480,#17481,#17482,#17483,#17484,
#17485,#17486,#17487,#17488,#17489,#17490,#17491,#17492,#17493,#17494,#17495,
#17496,#17497,#17498,#17499,#17500,#17501),.UNSPECIFIED.,.F.,.F.,(4,3,3,
3,3,3,3,4),(-142.322100278399,-141.665286242036,-140.667643381176,-139.670000520317,
-138.672357659457,-137.674714798598,-136.677071937739,-136.03891497122),
 .UNSPECIFIED.);
#417=B_SPLINE_CURVE_WITH_KNOTS('',3,(#17502,#17503,#17504,#17505,#17506,
#17507,#17508,#17509,#17510,#17511,#17512,#17513,#17514,#17515,#17516,#17517,
#17518,#17519,#17520,#17521,#17522,#17523),.UNSPECIFIED.,.F.,.F.,(4,3,3,
3,3,3,3,4),(133.069633257233,133.73766567062,134.735707951744,135.733750232868,
136.731792513992,137.729834795116,138.72787707624,139.352818564412),
 .UNSPECIFIED.);
#418=B_SPLINE_CURVE_WITH_KNOTS('',3,(#17528,#17529,#17530,#17531,#17532,
#17533,#17534,#17535,#17536,#17537,#17538,#17539,#17540,#17541,#17542,#17543,
#17544,#17545,#17546,#17547,#17548,#17549),.UNSPECIFIED.,.F.,.F.,(4,3,3,
3,3,3,3,4),(-148.605285585579,-147.651143407192,-146.653500546333,-145.655857685473,
-144.658214824614,-143.660571963754,-142.662929102895,-142.322100278399),
 .UNSPECIFIED.);
#419=B_SPLINE_CURVE_WITH_KNOTS('',3,(#17550,#17551,#17552,#17553,#17554,
#17555,#17556,#17557,#17558,#17559,#17560,#17561,#17562,#17563,#17564,#17565,
#17566,#17567,#17568,#17569,#17570,#17571),.UNSPECIFIED.,.F.,.F.,(4,3,3,
3,3,3,3,4),(139.352818564412,139.725919357364,140.723961638488,141.722003919612,
142.720046200736,143.71808848186,144.716130762984,145.636003871592),
 .UNSPECIFIED.);
#420=B_SPLINE_CURVE_WITH_KNOTS('',3,(#17576,#17577,#17578,#17579,#17580,
#17581,#17582,#17583,#17584,#17585,#17586,#17587,#17588,#17589,#17590,#17591,
#17592,#17593,#17594,#17595,#17596,#17597,#17598,#17599,#17600),
 .UNSPECIFIED.,.F.,.F.,(4,3,3,3,3,3,3,3,4),(-154.888470892759,-154.634643433208,
-153.637000572349,-152.639357711489,-151.64171485063,-150.64407198977,-149.646429128911,
-148.648786268052,-148.605285585579),.UNSPECIFIED.);
#421=B_SPLINE_CURVE_WITH_KNOTS('',3,(#17601,#17602,#17603,#17604,#17605,
#17606,#17607,#17608,#17609,#17610,#17611,#17612,#17613,#17614,#17615,#17616,
#17617,#17618,#17619,#17620,#17621,#17622,#17623,#17624,#17625),
 .UNSPECIFIED.,.F.,.F.,(4,3,3,3,3,3,3,3,4),(145.636003871592,145.714173044108,
146.712215325232,147.710257606356,148.70829988748,149.706342168604,150.704384449728,
151.702426730852,151.919189178771),.UNSPECIFIED.);
#422=B_SPLINE_CURVE_WITH_KNOTS('',3,(#17630,#17631,#17632,#17633,#17634,
#17635,#17636,#17637,#17638,#17639,#17640,#17641,#17642,#17643,#17644,#17645,
#17646,#17647,#17648,#17649,#17650,#17651),.UNSPECIFIED.,.F.,.F.,(4,3,3,
3,3,3,3,4),(-161.171656199938,-160.620500598364,-159.622857737505,-158.625214876646,
-157.627572015786,-156.629929154927,-155.632286294067,-154.888470892759),
 .UNSPECIFIED.);
#423=B_SPLINE_CURVE_WITH_KNOTS('',3,(#17652,#17653,#17654,#17655,#17656,
#17657,#17658,#17659,#17660,#17661,#17662,#17663,#17664,#17665,#17666,#17667,
#17668,#17669,#17670,#17671,#17672,#17673),.UNSPECIFIED.,.F.,.F.,(4,3,3,
3,3,3,3,4),(151.919189178771,152.700469011976,153.6985112931,154.696553574224,
155.694595855348,156.692638136472,157.690680417596,158.202374485951),
 .UNSPECIFIED.);
#424=B_SPLINE_CURVE_WITH_KNOTS('',3,(#17678,#17679,#17680,#17681,#17682,
#17683,#17684,#17685,#17686,#17687,#17688,#17689,#17690,#17691,#17692,#17693,
#17694,#17695,#17696,#17697,#17698,#17699),.UNSPECIFIED.,.F.,.F.,(4,3,3,
3,3,3,3,4),(-167.454841507118,-166.606357763521,-165.608714902661,-164.611072041802,
-163.613429180943,-162.615786320083,-161.618143459224,-161.171656199938),
 .UNSPECIFIED.);
#425=B_SPLINE_CURVE_WITH_KNOTS('',3,(#17700,#17701,#17702,#17703,#17704,
#17705,#17706,#17707,#17708,#17709,#17710,#17711,#17712,#17713,#17714,#17715,
#17716,#17717,#17718,#17719,#17720,#17721),.UNSPECIFIED.,.F.,.F.,(4,3,3,
3,3,3,3,4),(158.202374485951,158.68872269872,159.686764979844,160.684807260968,
161.682849542092,162.680891823216,163.67893410434,164.48555979313),
 .UNSPECIFIED.);
#426=B_SPLINE_CURVE_WITH_KNOTS('',3,(#17726,#17727,#17728,#17729,#17730,
#17731,#17732,#17733,#17734,#17735,#17736,#17737,#17738,#17739,#17740,#17741,
#17742,#17743,#17744,#17745,#17746,#17747,#17748,#17749,#17750),
 .UNSPECIFIED.,.F.,.F.,(4,3,3,3,3,3,3,3,4),(-173.738026814297,-173.589857789537,
-172.592214928677,-171.594572067818,-170.596929206958,-169.599286346099,
-168.60164348524,-167.60400062438,-167.454841507118),.UNSPECIFIED.);
#427=B_SPLINE_CURVE_WITH_KNOTS('',3,(#17751,#17752,#17753,#17754,#17755,
#17756,#17757,#17758,#17759,#17760,#17761,#17762,#17763,#17764,#17765,#17766,
#17767,#17768,#17769,#17770,#17771,#17772,#17773,#17774,#17775),
 .UNSPECIFIED.,.F.,.F.,(4,3,3,3,3,3,3,3,4),(164.48555979313,164.676976385465,
165.675018666588,166.673060947713,167.671103228837,168.669145509961,169.667187791085,
170.665230072209,170.76874510031),.UNSPECIFIED.);
#428=B_SPLINE_CURVE_WITH_KNOTS('',3,(#17780,#17781,#17782,#17783,#17784,
#17785,#17786,#17787,#17788,#17789,#17790,#17791,#17792,#17793,#17794,#17795,
#17796,#17797,#17798,#17799,#17800,#17801),.UNSPECIFIED.,.F.,.F.,(4,3,3,
3,3,3,3,4),(-180.021212121477,-179.575714954693,-178.578072093834,-177.580429232974,
-176.582786372115,-175.585143511255,-174.587500650396,-173.738026814297),
 .UNSPECIFIED.);
#429=B_SPLINE_CURVE_WITH_KNOTS('',3,(#17802,#17803,#17804,#17805,#17806,
#17807,#17808,#17809,#17810,#17811,#17812,#17813,#17814,#17815,#17816,#17817,
#17818,#17819,#17820,#17821,#17822,#17823),.UNSPECIFIED.,.F.,.F.,(4,3,3,
3,3,3,3,4),(170.76874510031,171.663272353333,172.661314634457,173.659356915581,
174.657399196705,175.655441477829,176.653483758953,177.051930407489),
 .UNSPECIFIED.);
#430=B_SPLINE_CURVE_WITH_KNOTS('',3,(#17828,#17829,#17830,#17831,#17832,
#17833,#17834,#17835,#17836,#17837,#17838,#17839,#17840,#17841,#17842,#17843,
#17844,#17845,#17846,#17847,#17848,#17849),.UNSPECIFIED.,.F.,.F.,(4,3,3,
3,3,3,3,4),(-186.304397428656,-185.56157211985,-184.56392925899,-183.566286398131,
-182.568643537271,-181.571000676412,-180.573357815553,-180.021212121477),
 .UNSPECIFIED.);
#431=B_SPLINE_CURVE_WITH_KNOTS('',3,(#17850,#17851,#17852,#17853,#17854,
#17855,#17856,#17857,#17858,#17859,#17860,#17861,#17862,#17863,#17864,#17865,
#17866,#17867,#17868,#17869,#17870,#17871),.UNSPECIFIED.,.F.,.F.,(4,3,3,
3,3,3,3,4),(177.051930407489,177.651526040077,178.649568321201,179.647610602325,
180.645652883449,181.643695164573,182.641737445697,183.335115714669),
 .UNSPECIFIED.);
#432=B_SPLINE_CURVE_WITH_KNOTS('',3,(#17877,#17878,#17879,#17880,#17881,
#17882,#17883,#17884,#17885,#17886),.UNSPECIFIED.,.F.,.F.,(4,1,1,1,1,1,
1,4),(197.920337176157,198.17515472821,199.172797589069,200.170440449928,
201.168083310788,202.165726171647,203.163369032507,204.161011893366),
 .UNSPECIFIED.);
#433=B_SPLINE_CURVE_WITH_KNOTS('',3,(#17889,#17890,#17891,#17892,#17893,
#17894,#17895,#17896,#17897),.UNSPECIFIED.,.F.,.F.,(4,1,1,1,1,1,4),(197.920337176157,
197.930069567874,198.928111848998,199.926154130122,200.924196411246,201.92223869237,
202.920280973494),.UNSPECIFIED.);
#434=B_SPLINE_CURVE_WITH_KNOTS('',3,(#17902,#17903,#17904,#17905,#17906,
#17907,#17908,#17909,#17910,#17911),.UNSPECIFIED.,.F.,.F.,(4,1,1,1,1,1,
1,4),(191.637151868977,192.189297563053,193.186940423913,194.184583284772,
195.182226145631,196.179869006491,197.17751186735,197.920337176157),
 .UNSPECIFIED.);
#435=B_SPLINE_CURVE_WITH_KNOTS('',3,(#17912,#17913,#17914,#17915,#17916,
#17917,#17918,#17919,#17920,#17921),.UNSPECIFIED.,.F.,.F.,(4,1,1,1,1,1,
1,4),(191.637151868977,191.94181588113,192.939858162254,193.937900443378,
194.935942724502,195.933985005626,196.93202728675,197.920337176157),
 .UNSPECIFIED.);
#436=B_SPLINE_CURVE_WITH_KNOTS('',3,(#17926,#17927,#17928,#17929,#17930,
#17931,#17932,#17933,#17934,#17935),.UNSPECIFIED.,.F.,.F.,(4,1,1,1,1,1,
1,4),(185.353966561798,186.203440397897,187.201083258756,188.198726119616,
189.196368980475,190.194011841334,191.191654702194,191.637151868977),
 .UNSPECIFIED.);
#437=B_SPLINE_CURVE_WITH_KNOTS('',3,(#17936,#17937,#17938,#17939,#17940,
#17941,#17942,#17943,#17944,#17945),.UNSPECIFIED.,.F.,.F.,(4,1,1,1,1,1,
1,4),(185.353966561798,185.953562194385,186.951604475509,187.949646756633,
188.947689037757,189.945731318881,190.943773600006,191.637151868977),
 .UNSPECIFIED.);
#438=B_SPLINE_CURVE_WITH_KNOTS('',3,(#17950,#17951,#17952,#17953,#17954,
#17955,#17956,#17957,#17958,#17959,#17960),.UNSPECIFIED.,.F.,.F.,(4,1,1,
1,1,1,1,1,4),(179.070781254618,179.219940371881,180.21758323274,181.2152260936,
182.212868954459,183.210511815318,184.208154676178,185.205797537037,185.353966561798),
 .UNSPECIFIED.);
#439=B_SPLINE_CURVE_WITH_KNOTS('',3,(#17961,#17962,#17963,#17964,#17965,
#17966,#17967,#17968,#17969,#17970),.UNSPECIFIED.,.F.,.F.,(4,1,1,1,1,1,
1,4),(179.070781254618,179.965308507641,180.963350788765,181.961393069889,
182.959435351013,183.957477632137,184.955519913261,185.353966561798),
 .UNSPECIFIED.);
#440=B_SPLINE_CURVE_WITH_KNOTS('',3,(#17975,#17976,#17977,#17978,#17979,
#17980,#17981,#17982,#17983,#17984),.UNSPECIFIED.,.F.,.F.,(4,1,1,1,1,1,
1,4),(172.787595947439,173.234083206724,174.231726067584,175.229368928443,
176.227011789303,177.224654650162,178.222297511021,179.070781254618),
 .UNSPECIFIED.);
#441=B_SPLINE_CURVE_WITH_KNOTS('',3,(#17985,#17986,#17987,#17988,#17989,
#17990,#17991,#17992,#17993,#17994,#17995),.UNSPECIFIED.,.F.,.F.,(4,1,1,
1,1,1,1,1,4),(172.787595947439,172.979012539773,173.977054820897,174.975097102021,
175.973139383145,176.971181664269,177.969223945393,178.967266226517,179.070781254618),
 .UNSPECIFIED.);
#442=B_SPLINE_CURVE_WITH_KNOTS('',3,(#18000,#18001,#18002,#18003,#18004,
#18005,#18006,#18007,#18008,#18009),.UNSPECIFIED.,.F.,.F.,(4,1,1,1,1,1,
1,4),(166.504410640259,167.248226041568,168.245868902427,169.243511763287,
170.241154624146,171.238797485006,172.236440345865,172.787595947439),
 .UNSPECIFIED.);
#443=B_SPLINE_CURVE_WITH_KNOTS('',3,(#18010,#18011,#18012,#18013,#18014,
#18015,#18016,#18017,#18018,#18019),.UNSPECIFIED.,.F.,.F.,(4,1,1,1,1,1,
1,4),(166.504410640259,166.990758853029,167.988801134153,168.986843415277,
169.984885696401,170.982927977525,171.980970258649,172.787595947439),
 .UNSPECIFIED.);
#444=B_SPLINE_CURVE_WITH_KNOTS('',3,(#18024,#18025,#18026,#18027,#18028,
#18029,#18030,#18031,#18032,#18033,#18034),.UNSPECIFIED.,.F.,.F.,(4,1,1,
1,1,1,1,1,4),(160.22122533308,160.264726015552,161.262368876412,162.260011737271,
163.25765459813,164.25529745899,165.252940319849,166.250583180709,166.504410640259),
 .UNSPECIFIED.);
#445=B_SPLINE_CURVE_WITH_KNOTS('',3,(#18035,#18036,#18037,#18038,#18039,
#18040,#18041,#18042,#18043,#18044),.UNSPECIFIED.,.F.,.F.,(4,1,1,1,1,1,
1,4),(160.22122533308,161.002505166285,162.000547447409,162.998589728533,
163.996632009657,164.994674290781,165.992716571905,166.504410640259),
 .UNSPECIFIED.);
#446=B_SPLINE_CURVE_WITH_KNOTS('',3,(#18049,#18050,#18051,#18052,#18053,
#18054,#18055,#18056,#18057,#18058),.UNSPECIFIED.,.F.,.F.,(4,1,1,1,1,1,
1,4),(153.9380400259,154.278868850396,155.276511711255,156.274154572115,
157.271797432974,158.269440293833,159.267083154693,160.22122533308),
 .UNSPECIFIED.);
#447=B_SPLINE_CURVE_WITH_KNOTS('',3,(#18059,#18060,#18061,#18062,#18063,
#18064,#18065,#18066,#18067,#18068,#18069),.UNSPECIFIED.,.F.,.F.,(4,1,1,
1,1,1,1,1,4),(153.9380400259,154.016209198417,155.014251479541,156.012293760665,
157.010336041789,158.008378322913,159.006420604037,160.004462885161,160.22122533308),
 .UNSPECIFIED.);
#448=B_SPLINE_CURVE_WITH_KNOTS('',3,(#18074,#18075,#18076,#18077,#18078,
#18079,#18080,#18081,#18082,#18083),.UNSPECIFIED.,.F.,.F.,(4,1,1,1,1,1,
1,4),(147.65485471872,148.293011685239,149.290654546099,150.288297406958,
151.285940267817,152.283583128677,153.281225989536,153.9380400259),
 .UNSPECIFIED.);
#449=B_SPLINE_CURVE_WITH_KNOTS('',3,(#18084,#18085,#18086,#18087,#18088,
#18089,#18090,#18091,#18092,#18093),.UNSPECIFIED.,.F.,.F.,(4,1,1,1,1,1,
1,4),(147.65485471872,148.027955511672,149.025997792796,150.02404007392,
151.022082355044,152.020124636168,153.018166917292,153.9380400259),
 .UNSPECIFIED.);
#450=B_SPLINE_CURVE_WITH_KNOTS('',3,(#18098,#18099,#18100,#18101,#18102,
#18103,#18104,#18105,#18106,#18107),.UNSPECIFIED.,.F.,.F.,(4,1,1,1,1,1,
1,4),(141.371669411541,142.307154520083,143.304797380942,144.302440241802,
145.300083102661,146.29772596352,147.29536882438,147.65485471872),
 .UNSPECIFIED.);
#451=B_SPLINE_CURVE_WITH_KNOTS('',3,(#18108,#18109,#18110,#18111,#18112,
#18113,#18114,#18115,#18116,#18117),.UNSPECIFIED.,.F.,.F.,(4,1,1,1,1,1,
1,4),(141.371669411541,142.039701824928,143.037744106052,144.035786387176,
145.0338286683,146.031870949424,147.029913230548,147.65485471872),
 .UNSPECIFIED.);
#452=B_SPLINE_CURVE_WITH_KNOTS('',3,(#18122,#18123,#18124,#18125,#18126,
#18127,#18128,#18129,#18130,#18131,#18132),.UNSPECIFIED.,.F.,.F.,(4,1,1,
1,1,1,1,1,4),(135.088484104361,135.323654494067,136.321297354926,137.318940215786,
138.316583076645,139.314225937505,140.311868798364,141.309511659223,141.371669411541),
 .UNSPECIFIED.);
#453=B_SPLINE_CURVE_WITH_KNOTS('',3,(#18133,#18134,#18135,#18136,#18137,
#18138,#18139,#18140,#18141,#18142),.UNSPECIFIED.,.F.,.F.,(4,1,1,1,1,1,
1,4),(135.088484104361,136.051448138184,137.049490419308,138.047532700432,
139.045574981556,140.04361726268,141.041659543804,141.371669411541),
 .UNSPECIFIED.);
#454=B_SPLINE_CURVE_WITH_KNOTS('',3,(#18147,#18148,#18149,#18150,#18151,
#18152,#18153,#18154,#18155,#18156),.UNSPECIFIED.,.F.,.F.,(4,1,1,1,1,1,
1,4),(128.805298797182,129.337797328911,130.33544018977,131.333083050629,
132.330725911489,133.328368772348,134.326011633208,135.088484104361),
 .UNSPECIFIED.);
#455=B_SPLINE_CURVE_WITH_KNOTS('',3,(#18157,#18158,#18159,#18160,#18161,
#18162,#18163,#18164,#18165,#18166,#18167),.UNSPECIFIED.,.F.,.F.,(4,1,1,
1,1,1,1,1,4),(128.805298797182,129.065152170316,130.06319445144,131.061236732564,
132.059279013688,133.057321294812,134.055363575936,135.05340585706,135.088484104361),
 .UNSPECIFIED.);
#456=B_SPLINE_CURVE_WITH_KNOTS('',3,(#18172,#18173,#18174,#18175,#18176,
#18177,#18178,#18179,#18180,#18181),.UNSPECIFIED.,.F.,.F.,(4,1,1,1,1,1,
1,4),(122.522113490002,123.351940163754,124.349583024614,125.347225885473,
126.344868746332,127.342511607192,128.340154468051,128.805298797182),
 .UNSPECIFIED.);
#457=B_SPLINE_CURVE_WITH_KNOTS('',3,(#18182,#18183,#18184,#18185,#18186,
#18187,#18188,#18189,#18190,#18191),.UNSPECIFIED.,.F.,.F.,(4,1,1,1,1,1,
1,4),(122.522113490002,123.076898483572,124.074940764696,125.07298304582,
126.071025326944,127.069067608068,128.067109889192,128.805298797182),
 .UNSPECIFIED.);
#458=B_SPLINE_CURVE_WITH_KNOTS('',3,(#18196,#18197,#18198,#18199,#18200,
#18201,#18202,#18203,#18204,#18205,#18206),.UNSPECIFIED.,.F.,.F.,(4,1,1,
1,1,1,1,1,4),(116.238928182823,116.368440137738,117.366082998598,118.363725859457,
119.361368720316,120.359011581176,121.356654442035,122.354297302895,122.522113490002),
 .UNSPECIFIED.);
#459=B_SPLINE_CURVE_WITH_KNOTS('',3,(#18207,#18208,#18209,#18210,#18211,
#18212,#18213,#18214,#18215,#18216),.UNSPECIFIED.,.F.,.F.,(4,1,1,1,1,1,
1,4),(116.238928182823,117.088644796828,118.086687077952,119.084729359076,
120.0827716402,121.080813921324,122.078856202448,122.522113490002),
 .UNSPECIFIED.);
#460=B_SPLINE_CURVE_WITH_KNOTS('',3,(#18221,#18222,#18223,#18224,#18225,
#18226,#18227,#18228,#18229,#18230),.UNSPECIFIED.,.F.,.F.,(4,1,1,1,1,1,
1,4),(109.955742875643,110.382582972582,111.380225833441,112.377868694301,
113.37551155516,114.373154416019,115.370797276879,116.238928182823),
 .UNSPECIFIED.);
#461=B_SPLINE_CURVE_WITH_KNOTS('',3,(#18231,#18232,#18233,#18234,#18235,
#18236,#18237,#18238,#18239,#18240,#18241),.UNSPECIFIED.,.F.,.F.,(4,1,1,
1,1,1,1,1,4),(109.955742875643,110.102348828959,111.100391110083,112.098433391207,
113.096475672331,114.094517953455,115.092560234579,116.090602515703,116.238928182823),
 .UNSPECIFIED.);
#462=B_SPLINE_CURVE_WITH_KNOTS('',3,(#18246,#18247,#18248,#18249,#18250,
#18251,#18252,#18253,#18254,#18255),.UNSPECIFIED.,.F.,.F.,(4,1,1,1,1,1,
1,4),(103.672557568463,104.396725807425,105.394368668285,106.392011529144,
107.389654390004,108.387297250863,109.384940111722,109.955742875643),
 .UNSPECIFIED.);
#463=B_SPLINE_CURVE_WITH_KNOTS('',3,(#18256,#18257,#18258,#18259,#18260,
#18261,#18262,#18263,#18264,#18265),.UNSPECIFIED.,.F.,.F.,(4,1,1,1,1,1,
1,4),(103.672557568463,104.114095142215,105.112137423339,106.110179704463,
107.108221985587,108.106264266711,109.104306547835,109.955742875643),
 .UNSPECIFIED.);
#464=B_SPLINE_CURVE_WITH_KNOTS('',3,(#18270,#18271,#18272,#18273,#18274,
#18275,#18276,#18277,#18278,#18279,#18280),.UNSPECIFIED.,.F.,.F.,(4,1,1,
1,1,1,1,1,4),(97.3893722612837,97.4132257814096,98.410868642269,99.4085115031284,
100.406154363988,101.403797224847,102.401440085707,103.399082946566,103.672557568463),
 .UNSPECIFIED.);
#465=B_SPLINE_CURVE_WITH_KNOTS('',3,(#18281,#18282,#18283,#18284,#18285,
#18286,#18287,#18288,#18289,#18290),.UNSPECIFIED.,.F.,.F.,(4,1,1,1,1,1,
1,4),(97.3893722612838,98.125841455471,99.123883736595,100.121926017719,
101.119968298843,102.118010579967,103.116052861091,103.672557568463),
 .UNSPECIFIED.);
#466=B_SPLINE_CURVE_WITH_KNOTS('',3,(#18295,#18296,#18297,#18298,#18299,
#18300,#18301,#18302,#18303,#18304),.UNSPECIFIED.,.F.,.F.,(4,1,1,1,1,1,
1,4),(91.1061869541041,91.4273686162531,92.4250114771125,93.4226543379719,
94.4202971988313,95.4179400596907,96.4155829205502,97.3893722612837),
 .UNSPECIFIED.);
#467=B_SPLINE_CURVE_WITH_KNOTS('',3,(#18305,#18306,#18307,#18308,#18309,
#18310,#18311,#18312,#18313,#18314,#18315),.UNSPECIFIED.,.F.,.F.,(4,1,1,
1,1,1,1,1,4),(91.1061869541042,91.1395454876028,92.1375877687268,93.1356300498508,
94.1336723309749,95.1317146120989,96.1297568932229,97.127799174347,97.3893722612838),
 .UNSPECIFIED.);
#468=B_SPLINE_CURVE_WITH_KNOTS('',3,(#18320,#18321,#18322,#18323,#18324,
#18325,#18326,#18327,#18328,#18329),.UNSPECIFIED.,.F.,.F.,(4,1,1,1,1,1,
1,4),(84.8230016469245,85.4415114510967,86.4391543119561,87.4367971728155,
88.4344400336749,89.4320828945343,90.4297257553937,91.1061869541041),
 .UNSPECIFIED.);
#469=B_SPLINE_CURVE_WITH_KNOTS('',3,(#18330,#18331,#18332,#18333,#18334,
#18335,#18336,#18337,#18338,#18339),.UNSPECIFIED.,.F.,.F.,(4,1,1,1,1,1,
1,4),(84.8230016469246,85.1512918008586,86.1493340819827,87.1473763631067,
88.1454186442307,89.1434609253548,90.1415032064788,91.1061869541042),
 .UNSPECIFIED.);
#470=B_SPLINE_CURVE_WITH_KNOTS('',3,(#18344,#18345,#18346,#18347,#18348,
#18349,#18350,#18351,#18352,#18353),.UNSPECIFIED.,.F.,.F.,(4,1,1,1,1,1,
1,4),(78.539816339745,79.4556542859402,80.4532971467996,81.4509400076591,
82.4485828685185,83.4462257293779,84.4438685902373,84.8230016469245),
 .UNSPECIFIED.);
#471=B_SPLINE_CURVE_WITH_KNOTS('',3,(#18354,#18355,#18356,#18357,#18358,
#18359,#18360,#18361,#18362,#18363),.UNSPECIFIED.,.F.,.F.,(4,1,1,1,1,1,
1,4),(78.539816339745,79.1630381141145,80.1610803952385,81.1591226763625,
82.1571649574865,83.1552072386106,84.1532495197346,84.8230016469246),
 .UNSPECIFIED.);
#472=B_SPLINE_CURVE_WITH_KNOTS('',3,(#18368,#18369,#18370,#18371,#18372,
#18373,#18374,#18375,#18376,#18377,#18378),.UNSPECIFIED.,.F.,.F.,(4,1,1,
1,1,1,1,1,4),(72.2566310325654,72.4721542599244,73.4697971207838,74.4674399816432,
75.4650828425026,76.462725703362,77.4603685642214,78.4580114250808,78.539816339745),
 .UNSPECIFIED.);
#473=B_SPLINE_CURVE_WITH_KNOTS('',3,(#18379,#18380,#18381,#18382,#18383,
#18384,#18385,#18386,#18387,#18388),.UNSPECIFIED.,.F.,.F.,(4,1,1,1,1,1,
1,4),(72.2566310325654,73.1747844273703,74.1728267084943,75.1708689896184,
76.1689112707424,77.1669535518664,78.1649958329905,78.539816339745),
 .UNSPECIFIED.);
#474=B_SPLINE_CURVE_WITH_KNOTS('',3,(#18393,#18394,#18395,#18396,#18397,
#18398,#18399,#18400,#18401,#18402),.UNSPECIFIED.,.F.,.F.,(4,1,1,1,1,1,
1,4),(65.9734457253858,66.486297094768,67.4839399556274,68.4815828164868,
69.4792256773462,70.4768685382056,71.474511399065,72.2566310325654),
 .UNSPECIFIED.);
#475=B_SPLINE_CURVE_WITH_KNOTS('',3,(#18403,#18404,#18405,#18406,#18407,
#18408,#18409,#18410,#18411,#18412,#18413),.UNSPECIFIED.,.F.,.F.,(4,1,1,
1,1,1,1,1,4),(65.9734457253858,66.1884884595021,67.1865307406262,68.1845730217502,
69.1826153028742,70.1806575839982,71.1786998651223,72.1767421462463,72.2566310325654),
 .UNSPECIFIED.);
#476=B_SPLINE_CURVE_WITH_KNOTS('',3,(#18418,#18419,#18420,#18421,#18422,
#18423,#18424,#18425,#18426,#18427),.UNSPECIFIED.,.F.,.F.,(4,1,1,1,1,1,
1,4),(59.6902604182062,60.5004399296115,61.4980827904709,62.4957256513303,
63.4933685121897,64.4910113730492,65.4886542339086,65.9734457253858),
 .UNSPECIFIED.);
#477=B_SPLINE_CURVE_WITH_KNOTS('',3,(#18428,#18429,#18430,#18431,#18432,
#18433,#18434,#18435,#18436,#18437),.UNSPECIFIED.,.F.,.F.,(4,1,1,1,1,1,
1,4),(59.6902604182062,60.200234772758,61.198277053882,62.196319335006,
63.19436161613,64.1924038972541,65.1904461783781,65.9734457253858),
 .UNSPECIFIED.);
#478=B_SPLINE_CURVE_WITH_KNOTS('',3,(#18442,#18443,#18444,#18445,#18446,
#18447,#18448,#18449,#18450,#18451,#18452),.UNSPECIFIED.,.F.,.F.,(4,1,1,
1,1,1,1,1,4),(53.4070751110266,53.5169399035957,54.5145827644551,55.5122256253145,
56.5098684861739,57.5075113470333,58.5051542078927,59.5027970687521,59.6902604182062),
 .UNSPECIFIED.);
#479=B_SPLINE_CURVE_WITH_KNOTS('',3,(#18453,#18454,#18455,#18456,#18457,
#18458,#18459,#18460,#18461,#18462),.UNSPECIFIED.,.F.,.F.,(4,1,1,1,1,1,
1,4),(53.4070751110266,54.2119810860138,55.2100233671378,56.2080656482619,
57.2061079293859,58.2041502105099,59.2021924916339,59.6902604182062),
 .UNSPECIFIED.);
#480=B_SPLINE_CURVE_WITH_KNOTS('',3,(#18467,#18468,#18469,#18470,#18471,
#18472,#18473,#18474,#18475,#18476),.UNSPECIFIED.,.F.,.F.,(4,1,1,1,1,1,
1,4),(47.123889803847,47.5310827384393,48.5287255992987,49.5263684601581,
50.5240113210175,51.5216541818769,52.5192970427363,53.4070751110266),
 .UNSPECIFIED.);
#481=B_SPLINE_CURVE_WITH_KNOTS('',3,(#18477,#18478,#18479,#18480,#18481,
#18482,#18483,#18484,#18485,#18486,#18487),.UNSPECIFIED.,.F.,.F.,(4,1,1,
1,1,1,1,1,4),(47.123889803847,47.2256851181456,48.2237273992696,49.2217696803937,
50.2198119615177,51.2178542426417,52.2158965237657,53.2139388048898,53.4070751110266),
 .UNSPECIFIED.);
#482=B_SPLINE_CURVE_WITH_KNOTS('',3,(#18492,#18493,#18494,#18495,#18496,
#18497,#18498,#18499,#18500,#18501),.UNSPECIFIED.,.F.,.F.,(4,1,1,1,1,1,
1,4),(40.8407044966674,41.5452255732828,42.5428684341422,43.5405112950016,
44.538154155861,45.5357970167204,46.5334398775799,47.123889803847),
 .UNSPECIFIED.);
#483=B_SPLINE_CURVE_WITH_KNOTS('',3,(#18502,#18503,#18504,#18505,#18506,
#18507,#18508,#18509,#18510,#18511),.UNSPECIFIED.,.F.,.F.,(4,1,1,1,1,1,
1,4),(40.8407044966675,41.2374314314014,42.2354737125255,43.2335159936495,
44.2315582747735,45.2296005558975,46.2276428370216,47.123889803847),
 .UNSPECIFIED.);
#484=B_SPLINE_CURVE_WITH_KNOTS('',3,(#18516,#18517,#18518,#18519,#18520,
#18521,#18522,#18523,#18524,#18525,#18526),.UNSPECIFIED.,.F.,.F.,(4,1,1,
1,1,1,1,1,4),(34.5575191894878,34.561725547267,35.5593684081264,36.5570112689858,
37.5546541298452,38.5522969907046,39.549939851564,40.5475827124234,40.8407044966674),
 .UNSPECIFIED.);
#485=B_SPLINE_CURVE_WITH_KNOTS('',3,(#18527,#18528,#18529,#18530,#18531,
#18532,#18533,#18534,#18535,#18536),.UNSPECIFIED.,.F.,.F.,(4,1,1,1,1,1,
1,4),(34.5575191894879,35.2491777446573,36.2472200257813,37.2452623069053,
38.2433045880294,39.2413468691534,40.2393891502774,40.8407044966675),
 .UNSPECIFIED.);
#486=B_SPLINE_CURVE_WITH_KNOTS('',3,(#18541,#18542,#18543,#18544,#18545,
#18546,#18547,#18548,#18549,#18550),.UNSPECIFIED.,.F.,.F.,(4,1,1,1,1,1,
1,4),(28.2743338823082,28.5758683821105,29.5735112429699,30.5711541038294,
31.5687969646888,32.5664398255482,33.5640826864076,34.5575191894878),
 .UNSPECIFIED.);
#487=B_SPLINE_CURVE_WITH_KNOTS('',3,(#18551,#18552,#18553,#18554,#18555,
#18556,#18557,#18558,#18559,#18560),.UNSPECIFIED.,.F.,.F.,(4,1,1,1,1,1,
1,4),(28.2743338823083,29.2609240579131,30.2589663390371,31.2570086201612,
32.2550509012852,33.2530931824092,34.2511354635333,34.5575191894879),
 .UNSPECIFIED.);
#488=B_SPLINE_CURVE_WITH_KNOTS('',3,(#18565,#18566,#18567,#18568,#18569,
#18570,#18571,#18572,#18573,#18574),.UNSPECIFIED.,.F.,.F.,(4,1,1,1,1,1,
1,4),(21.9911485751286,22.5900112169541,23.5876540778135,24.5852969386729,
25.5829397995323,26.5805826603917,27.5782255212511,28.2743338823082),
 .UNSPECIFIED.);
#489=B_SPLINE_CURVE_WITH_KNOTS('',3,(#18575,#18576,#18577,#18578,#18579,
#18580,#18581,#18582,#18583,#18584,#18585),.UNSPECIFIED.,.F.,.F.,(4,1,1,
1,1,1,1,1,4),(21.9911485751287,22.2746280900449,23.272670371169,24.270712652293,
25.268754933417,26.266797214541,27.2648394956651,28.2628817767891,28.2743338823083),
 .UNSPECIFIED.);
#490=B_SPLINE_CURVE_WITH_KNOTS('',3,(#18590,#18591,#18592,#18593,#18594,
#18595,#18596,#18597,#18598,#18599),.UNSPECIFIED.,.F.,.F.,(4,1,1,1,1,1,
1,4),(15.707963267949,16.6041540517977,17.6017969126571,18.5994397735165,
19.5970826343759,20.5947254952353,21.5923683560947,21.9911485751286),
 .UNSPECIFIED.);
#491=B_SPLINE_CURVE_WITH_KNOTS('',3,(#18600,#18601,#18602,#18603,#18604,
#18605,#18606,#18607,#18608,#18609),.UNSPECIFIED.,.F.,.F.,(4,1,1,1,1,1,
1,4),(15.7079632679491,16.2863744033008,17.2844166844248,18.2824589655488,
19.2805012466728,20.2785435277969,21.2765858089209,21.9911485751287),
 .UNSPECIFIED.);
#492=B_SPLINE_CURVE_WITH_KNOTS('',3,(#18612,#18613,#18614,#18615,#18616,
#18617,#18618,#18619,#18620,#18621,#18622,#18623,#18624,#18625,#18626,#18627,
#18628,#18629,#18630,#18631,#18632,#18633,#18634,#18635,#18636,#18637,#18638,
#18639,#18640,#18641,#18642,#18643,#18644,#18645,#18646,#18647,#18648,#18649,
#18650,#18651,#18652,#18653,#18654,#18655,#18656,#18657,#18658,#18659,#18660,
#18661,#18662,#18663,#18664,#18665,#18666,#18667,#18668,#18669,#18670,#18671,
#18672,#18673,#18674,#18675,#18676,#18677,#18678,#18679,#18680,#18681,#18682,
#18683,#18684,#18685,#18686,#18687,#18688,#18689,#18690,#18691,#18692,#18693,
#18694,#18695,#18696,#18697,#18698,#18699,#18700,#18701,#18702,#18703,#18704,
#18705,#18706,#18707,#18708,#18709,#18710,#18711,#18712,#18713,#18714,#18715,
#18716,#18717,#18718,#18719,#18720,#18721,#18722,#18723,#18724,#18725,#18726,
#18727,#18728,#18729,#18730,#18731,#18732),.UNSPECIFIED.,.F.,.F.,(4,3,3,
3,3,3,3,3,3,3,3,3,3,3,3,3,3,3,3,3,3,3,3,3,3,3,3,3,3,3,3,3,3,3,3,3,3,3,3,
3,4),(-0.753008129282056,-0.726412283548368,-0.715911613874471,-0.694893371653716,
-0.683361029549332,-0.673826434412814,-0.652889016486892,-0.639679181765185,
-0.63195159856097,-0.60480408471638,-0.59150990338668,-0.582561183693184,
-0.554067746128576,-0.540494882749548,-0.528208608719221,-0.505843484121927,
-0.4921308028701,-0.483102814228457,-0.456032674248847,-0.436199115577779,
-0.427073928162626,-0.400948091236321,-0.382860905241332,-0.374822254310016,
-0.34584221065474,-0.333939649620793,-0.324058619604945,-0.29393738163796,
-0.278576588250954,-0.269234263278142,-0.238815915606663,-0.225742435796944,
-0.216239773488962,-0.18666367230127,-0.170750005528772,-0.161294486761502,
-0.129614927749849,-0.114924930935507,-0.106250072717365,-0.0979353687381955,
-0.0965360155478562),.UNSPECIFIED.);
#493=B_SPLINE_CURVE_WITH_KNOTS('',3,(#18734,#18735,#18736,#18737,#18738,
#18739,#18740,#18741,#18742,#18743,#18744,#18745,#18746,#18747,#18748,#18749,
#18750,#18751,#18752,#18753,#18754,#18755,#18756,#18757,#18758,#18759,#18760,
#18761,#18762,#18763,#18764,#18765,#18766,#18767,#18768,#18769,#18770),
 .UNSPECIFIED.,.F.,.F.,(4,3,3,3,3,3,3,3,3,3,3,3,4),(-0.204609524178132,
-0.173922074105667,-0.152149392827302,-0.142793959810126,-0.12983323009626,
-0.11308637627832,-0.0998536142809363,-0.090547498816978,-0.0679106241127335,
-0.0514558350659385,-0.042025593252969,-0.0155529233063705,0.),
 .UNSPECIFIED.);
#494=B_SPLINE_CURVE_WITH_KNOTS('',3,(#18773,#18774,#18775,#18776,#18777,
#18778,#18779,#18780,#18781,#18782,#18783,#18784,#18785,#18786,#18787,#18788),
 .UNSPECIFIED.,.F.,.F.,(4,3,3,3,3,4),(-0.0965360155478562,-0.0724020116608921,
-0.0590232605257019,-0.050388474335024,-0.0186937936910934,0.),
 .UNSPECIFIED.);
#495=B_SPLINE_CURVE_WITH_KNOTS('',3,(#19577,#19578,#19579,#19580,#19581,
#19582,#19583,#19584),.UNSPECIFIED.,.F.,.F.,(4,1,1,1,1,4),(11.6159397475006,
12.61358260836,13.6112254692194,14.6088683300789,15.6065111909383,15.707963267949),
 .UNSPECIFIED.);
#496=B_SPLINE_CURVE_WITH_KNOTS('',3,(#19585,#19586,#19587,#19588,#19589,
#19590,#19591,#19592,#19593,#19594,#19595,#19596,#19597,#19598,#19599,#19600,
#19601,#19602,#19603,#19604,#19605,#19606,#19607,#19608,#19609,#19610,#19611,
#19612,#19613,#19614,#19615,#19616,#19617,#19618,#19619,#19620,#19621,#19622,
#19623,#19624,#19625,#19626,#19627,#19628,#19629,#19630,#19631,#19632,#19633),
 .UNSPECIFIED.,.F.,.F.,(4,3,3,3,3,3,3,3,3,3,3,3,3,3,3,3,4),(-0.275362278356892,
-0.263988733943187,-0.242277787653762,-0.228409792083558,-0.208856161945484,
-0.197709057767663,-0.168075464588018,-0.150222803571495,-0.140083955862437,
-0.125365894046572,-0.0997819296507484,-0.0889593225835958,-0.0667194919376969,
-0.0511923416312717,-0.0404361839568205,-0.0141940669149386,0.),
 .UNSPECIFIED.);
#497=B_SPLINE_CURVE_WITH_KNOTS('',3,(#19634,#19635,#19636,#19637,#19638,
#19639,#19640,#19641,#19642,#19643,#19644,#19645,#19646,#19647,#19648,#19649,
#19650,#19651,#19652),.UNSPECIFIED.,.F.,.F.,(4,3,3,3,3,3,4),(-191.027404416132,
-190.549786424147,-189.552143563287,-188.554500702428,-187.556857841568,
-186.559214980709,-186.304397428656),.UNSPECIFIED.);
#498=B_SPLINE_CURVE_WITH_KNOTS('',3,(#19655,#19656,#19657,#19658,#19659,
#19660,#19661,#19662,#19663),.UNSPECIFIED.,.F.,.F.,(4,1,1,1,1,1,4),(10.3752088276283,
11.2961629976806,12.2942052788047,13.2922475599287,14.2902898410527,15.2883321221767,
15.7079632679491),.UNSPECIFIED.);
#499=B_SPLINE_CURVE_WITH_KNOTS('',3,(#20457,#20458,#20459,#20460,#20461,
#20462,#20463,#20464,#20465,#20466,#20467,#20468,#20469,#20470,#20471,#20472,
#20473,#20474,#20475,#20476,#20477,#20478),.UNSPECIFIED.,.F.,.F.,(4,3,3,
3,3,3,3,4),(183.335115714669,183.639779726821,184.637822007945,185.635864289069,
186.633906570193,187.631948851317,188.629991132441,188.954231742812),
 .UNSPECIFIED.);
#500=B_SPLINE_CURVE_WITH_KNOTS('',3,(#20479,#20480,#20481,#20482,#20483,
#20484,#20485,#20486,#20487,#20488,#20489,#20490,#20491,#20492,#20493,#20494,
#20495,#20496,#20497,#20498,#20499,#20500,#20501,#20502,#20503,#20504,#20505,
#20506,#20507,#20508,#20509,#20510,#20511,#20512,#20513,#20514,#20515,#20516,
#20517,#20518,#20519,#20520,#20521,#20522,#20523,#20524,#20525,#20526,#20527,
#20528,#20529,#20530),.UNSPECIFIED.,.F.,.F.,(4,3,3,3,3,3,3,3,3,3,3,3,3,
3,3,3,3,4),(-0.276631791712714,-0.267404104599176,-0.245529112929484,-0.233826742508505,
-0.212230201958684,-0.201819484750363,-0.173281546649687,-0.162756755581661,
-0.152537502224722,-0.140478169692516,-0.120739781640826,-0.110641775261762,
-0.100726383882944,-0.0755447879122082,-0.0587891884452614,-0.0493012364577666,
-0.0182848522583483,0.),.UNSPECIFIED.);
#559=SHAPE_REPRESENTATION_RELATIONSHIP('SRR','None',#22179,#568);
#568=ADVANCED_BREP_SHAPE_REPRESENTATION('',(#586),#22125);
#577=STYLED_ITEM('',(#22234),#586);
#586=MANIFOLD_SOLID_BREP('Body1',#8808);
#633=FACE_BOUND('',#1847,.T.);
#634=FACE_BOUND('',#1850,.T.);
#871=PLANE('',#9383);
#872=PLANE('',#9384);
#873=PLANE('',#9385);
#874=PLANE('',#9386);
#875=PLANE('',#9387);
#876=PLANE('',#9388);
#877=PLANE('',#9389);
#878=PLANE('',#9390);
#879=PLANE('',#9394);
#880=PLANE('',#9395);
#1248=FACE_OUTER_BOUND('',#1774,.T.);
#1249=FACE_OUTER_BOUND('',#1775,.T.);
#1250=FACE_OUTER_BOUND('',#1776,.T.);
#1251=FACE_OUTER_BOUND('',#1777,.T.);
#1252=FACE_OUTER_BOUND('',#1778,.T.);
#1253=FACE_OUTER_BOUND('',#1779,.T.);
#1254=FACE_OUTER_BOUND('',#1780,.T.);
#1255=FACE_OUTER_BOUND('',#1781,.T.);
#1256=FACE_OUTER_BOUND('',#1782,.T.);
#1257=FACE_OUTER_BOUND('',#1783,.T.);
#1258=FACE_OUTER_BOUND('',#1784,.T.);
#1259=FACE_OUTER_BOUND('',#1785,.T.);
#1260=FACE_OUTER_BOUND('',#1786,.T.);
#1261=FACE_OUTER_BOUND('',#1787,.T.);
#1262=FACE_OUTER_BOUND('',#1788,.T.);
#1263=FACE_OUTER_BOUND('',#1789,.T.);
#1264=FACE_OUTER_BOUND('',#1790,.T.);
#1265=FACE_OUTER_BOUND('',#1791,.T.);
#1266=FACE_OUTER_BOUND('',#1792,.T.);
#1267=FACE_OUTER_BOUND('',#1793,.T.);
#1268=FACE_OUTER_BOUND('',#1794,.T.);
#1269=FACE_OUTER_BOUND('',#1795,.T.);
#1270=FACE_OUTER_BOUND('',#1796,.T.);
#1271=FACE_OUTER_BOUND('',#1797,.T.);
#1272=FACE_OUTER_BOUND('',#1798,.T.);
#1273=FACE_OUTER_BOUND('',#1799,.T.);
#1274=FACE_OUTER_BOUND('',#1800,.T.);
#1275=FACE_OUTER_BOUND('',#1801,.T.);
#1276=FACE_OUTER_BOUND('',#1802,.T.);
#1277=FACE_OUTER_BOUND('',#1803,.T.);
#1278=FACE_OUTER_BOUND('',#1804,.T.);
#1279=FACE_OUTER_BOUND('',#1805,.T.);
#1280=FACE_OUTER_BOUND('',#1806,.T.);
#1281=FACE_OUTER_BOUND('',#1807,.T.);
#1282=FACE_OUTER_BOUND('',#1808,.T.);
#1283=FACE_OUTER_BOUND('',#1809,.T.);
#1284=FACE_OUTER_BOUND('',#1810,.T.);
#1285=FACE_OUTER_BOUND('',#1811,.T.);
#1286=FACE_OUTER_BOUND('',#1812,.T.);
#1287=FACE_OUTER_BOUND('',#1813,.T.);
#1288=FACE_OUTER_BOUND('',#1814,.T.);
#1289=FACE_OUTER_BOUND('',#1815,.T.);
#1290=FACE_OUTER_BOUND('',#1816,.T.);
#1291=FACE_OUTER_BOUND('',#1817,.T.);
#1292=FACE_OUTER_BOUND('',#1818,.T.);
#1293=FACE_OUTER_BOUND('',#1819,.T.);
#1294=FACE_OUTER_BOUND('',#1820,.T.);
#1295=FACE_OUTER_BOUND('',#1821,.T.);
#1296=FACE_OUTER_BOUND('',#1822,.T.);
#1297=FACE_OUTER_BOUND('',#1823,.T.);
#1298=FACE_OUTER_BOUND('',#1824,.T.);
#1299=FACE_OUTER_BOUND('',#1825,.T.);
#1300=FACE_OUTER_BOUND('',#1826,.T.);
#1301=FACE_OUTER_BOUND('',#1827,.T.);
#1302=FACE_OUTER_BOUND('',#1828,.T.);
#1303=FACE_OUTER_BOUND('',#1829,.T.);
#1304=FACE_OUTER_BOUND('',#1830,.T.);
#1305=FACE_OUTER_BOUND('',#1831,.T.);
#1306=FACE_OUTER_BOUND('',#1832,.T.);
#1307=FACE_OUTER_BOUND('',#1833,.T.);
#1308=FACE_OUTER_BOUND('',#1834,.T.);
#1309=FACE_OUTER_BOUND('',#1835,.T.);
#1310=FACE_OUTER_BOUND('',#1836,.T.);
#1311=FACE_OUTER_BOUND('',#1837,.T.);
#1312=FACE_OUTER_BOUND('',#1838,.T.);
#1313=FACE_OUTER_BOUND('',#1839,.T.);
#1314=FACE_OUTER_BOUND('',#1840,.T.);
#1315=FACE_OUTER_BOUND('',#1841,.T.);
#1316=FACE_OUTER_BOUND('',#1842,.T.);
#1317=FACE_OUTER_BOUND('',#1843,.T.);
#1318=FACE_OUTER_BOUND('',#1844,.T.);
#1319=FACE_OUTER_BOUND('',#1845,.T.);
#1320=FACE_OUTER_BOUND('',#1846,.T.);
#1321=FACE_OUTER_BOUND('',#1848,.T.);
#1322=FACE_OUTER_BOUND('',#1849,.T.);
#1323=FACE_OUTER_BOUND('',#1851,.T.);
#1774=EDGE_LOOP('',(#7482,#7483,#7484,#7485));
#1775=EDGE_LOOP('',(#7486,#7487,#7488,#7489));
#1776=EDGE_LOOP('',(#7490,#7491,#7492,#7493));
#1777=EDGE_LOOP('',(#7494,#7495,#7496,#7497));
#1778=EDGE_LOOP('',(#7498,#7499,#7500,#7501));
#1779=EDGE_LOOP('',(#7502,#7503,#7504,#7505));
#1780=EDGE_LOOP('',(#7506,#7507,#7508,#7509));
#1781=EDGE_LOOP('',(#7510,#7511,#7512,#7513));
#1782=EDGE_LOOP('',(#7514,#7515,#7516,#7517));
#1783=EDGE_LOOP('',(#7518,#7519,#7520,#7521));
#1784=EDGE_LOOP('',(#7522,#7523,#7524,#7525));
#1785=EDGE_LOOP('',(#7526,#7527,#7528,#7529));
#1786=EDGE_LOOP('',(#7530,#7531,#7532,#7533));
#1787=EDGE_LOOP('',(#7534,#7535,#7536,#7537));
#1788=EDGE_LOOP('',(#7538,#7539,#7540,#7541));
#1789=EDGE_LOOP('',(#7542,#7543,#7544,#7545));
#1790=EDGE_LOOP('',(#7546,#7547,#7548,#7549));
#1791=EDGE_LOOP('',(#7550,#7551,#7552,#7553));
#1792=EDGE_LOOP('',(#7554,#7555,#7556,#7557));
#1793=EDGE_LOOP('',(#7558,#7559,#7560,#7561));
#1794=EDGE_LOOP('',(#7562,#7563,#7564,#7565));
#1795=EDGE_LOOP('',(#7566,#7567,#7568,#7569));
#1796=EDGE_LOOP('',(#7570,#7571,#7572,#7573));
#1797=EDGE_LOOP('',(#7574,#7575,#7576,#7577));
#1798=EDGE_LOOP('',(#7578,#7579,#7580,#7581));
#1799=EDGE_LOOP('',(#7582,#7583,#7584,#7585));
#1800=EDGE_LOOP('',(#7586,#7587,#7588,#7589));
#1801=EDGE_LOOP('',(#7590,#7591,#7592,#7593));
#1802=EDGE_LOOP('',(#7594,#7595,#7596,#7597));
#1803=EDGE_LOOP('',(#7598,#7599,#7600,#7601));
#1804=EDGE_LOOP('',(#7602,#7603,#7604,#7605));
#1805=EDGE_LOOP('',(#7606,#7607,#7608,#7609));
#1806=EDGE_LOOP('',(#7610,#7611,#7612,#7613));
#1807=EDGE_LOOP('',(#7614,#7615,#7616,#7617));
#1808=EDGE_LOOP('',(#7618,#7619,#7620,#7621));
#1809=EDGE_LOOP('',(#7622,#7623,#7624,#7625));
#1810=EDGE_LOOP('',(#7626,#7627,#7628,#7629));
#1811=EDGE_LOOP('',(#7630,#7631,#7632,#7633));
#1812=EDGE_LOOP('',(#7634,#7635,#7636,#7637));
#1813=EDGE_LOOP('',(#7638,#7639,#7640,#7641));
#1814=EDGE_LOOP('',(#7642,#7643,#7644,#7645));
#1815=EDGE_LOOP('',(#7646,#7647,#7648,#7649));
#1816=EDGE_LOOP('',(#7650,#7651,#7652,#7653));
#1817=EDGE_LOOP('',(#7654,#7655,#7656,#7657));
#1818=EDGE_LOOP('',(#7658,#7659,#7660,#7661));
#1819=EDGE_LOOP('',(#7662,#7663,#7664,#7665));
#1820=EDGE_LOOP('',(#7666,#7667,#7668,#7669));
#1821=EDGE_LOOP('',(#7670,#7671,#7672,#7673));
#1822=EDGE_LOOP('',(#7674,#7675,#7676,#7677));
#1823=EDGE_LOOP('',(#7678,#7679,#7680,#7681));
#1824=EDGE_LOOP('',(#7682,#7683,#7684,#7685));
#1825=EDGE_LOOP('',(#7686,#7687,#7688,#7689));
#1826=EDGE_LOOP('',(#7690,#7691,#7692,#7693));
#1827=EDGE_LOOP('',(#7694,#7695,#7696,#7697));
#1828=EDGE_LOOP('',(#7698,#7699,#7700,#7701));
#1829=EDGE_LOOP('',(#7702,#7703,#7704,#7705));
#1830=EDGE_LOOP('',(#7706,#7707,#7708,#7709));
#1831=EDGE_LOOP('',(#7710,#7711,#7712,#7713));
#1832=EDGE_LOOP('',(#7714,#7715,#7716,#7717));
#1833=EDGE_LOOP('',(#7718,#7719,#7720,#7721));
#1834=EDGE_LOOP('',(#7722,#7723,#7724,#7725,#7726,#7727,#7728,#7729));
#1835=EDGE_LOOP('',(#7730,#7731,#7732,#7733,#7734,#7735,#7736,#7737,#7738,
#7739,#7740,#7741,#7742,#7743,#7744,#7745,#7746,#7747,#7748,#7749,#7750,
#7751,#7752,#7753,#7754,#7755,#7756,#7757,#7758,#7759,#7760,#7761,#7762,
#7763,#7764,#7765,#7766,#7767,#7768,#7769,#7770,#7771,#7772,#7773,#7774,
#7775,#7776,#7777,#7778,#7779,#7780,#7781,#7782,#7783,#7784,#7785,#7786,
#7787,#7788,#7789,#7790,#7791,#7792,#7793));
#1836=EDGE_LOOP('',(#7794,#7795,#7796,#7797));
#1837=EDGE_LOOP('',(#7798,#7799,#7800,#7801,#7802,#7803,#7804,#7805,#7806,
#7807,#7808,#7809,#7810,#7811,#7812,#7813,#7814,#7815,#7816,#7817,#7818,
#7819,#7820,#7821,#7822,#7823,#7824,#7825,#7826,#7827,#7828,#7829,#7830,
#7831,#7832,#7833,#7834,#7835,#7836,#7837,#7838,#7839,#7840,#7841,#7842,
#7843,#7844,#7845,#7846,#7847,#7848,#7849,#7850,#7851,#7852,#7853,#7854,
#7855,#7856,#7857,#7858,#7859,#7860,#7861,#7862));
#1838=EDGE_LOOP('',(#7863,#7864,#7865,#7866));
#1839=EDGE_LOOP('',(#7867,#7868,#7869,#7870));
#1840=EDGE_LOOP('',(#7871,#7872,#7873,#7874));
#1841=EDGE_LOOP('',(#7875,#7876,#7877,#7878));
#1842=EDGE_LOOP('',(#7879,#7880,#7881,#7882));
#1843=EDGE_LOOP('',(#7883,#7884,#7885,#7886));
#1844=EDGE_LOOP('',(#7887,#7888,#7889,#7890));
#1845=EDGE_LOOP('',(#7891,#7892,#7893,#7894,#7895,#7896));
#1846=EDGE_LOOP('',(#7897));
#1847=EDGE_LOOP('',(#7898,#7899,#7900,#7901));
#1848=EDGE_LOOP('',(#7902,#7903,#7904,#7905));
#1849=EDGE_LOOP('',(#7906));
#1850=EDGE_LOOP('',(#7907,#7908,#7909,#7910,#7911,#7912));
#1851=EDGE_LOOP('',(#7913));
#2534=LINE('',#16414,#3264);
#2535=LINE('',#16438,#3265);
#2536=LINE('',#16486,#3266);
#2537=LINE('',#16534,#3267);
#2538=LINE('',#16585,#3268);
#2539=LINE('',#16633,#3269);
#2540=LINE('',#16681,#3270);
#2541=LINE('',#16729,#3271);
#2542=LINE('',#16783,#3272);
#2543=LINE('',#16831,#3273);
#2544=LINE('',#16879,#3274);
#2545=LINE('',#16933,#3275);
#2546=LINE('',#16981,#3276);
#2547=LINE('',#17029,#3277);
#2548=LINE('',#17077,#3278);
#2549=LINE('',#17131,#3279);
#2550=LINE('',#17179,#3280);
#2551=LINE('',#17227,#3281);
#2552=LINE('',#17281,#3282);
#2553=LINE('',#17329,#3283);
#2554=LINE('',#17377,#3284);
#2555=LINE('',#17431,#3285);
#2556=LINE('',#17479,#3286);
#2557=LINE('',#17527,#3287);
#2558=LINE('',#17575,#3288);
#2559=LINE('',#17629,#3289);
#2560=LINE('',#17677,#3290);
#2561=LINE('',#17725,#3291);
#2562=LINE('',#17779,#3292);
#2563=LINE('',#17827,#3293);
#2564=LINE('',#17875,#3294);
#2565=LINE('',#17901,#3295);
#2566=LINE('',#17925,#3296);
#2567=LINE('',#17949,#3297);
#2568=LINE('',#17974,#3298);
#2569=LINE('',#17999,#3299);
#2570=LINE('',#18023,#3300);
#2571=LINE('',#18048,#3301);
#2572=LINE('',#18073,#3302);
#2573=LINE('',#18097,#3303);
#2574=LINE('',#18121,#3304);
#2575=LINE('',#18146,#3305);
#2576=LINE('',#18171,#3306);
#2577=LINE('',#18195,#3307);
#2578=LINE('',#18220,#3308);
#2579=LINE('',#18245,#3309);
#2580=LINE('',#18269,#3310);
#2581=LINE('',#18294,#3311);
#2582=LINE('',#18319,#3312);
#2583=LINE('',#18343,#3313);
#2584=LINE('',#18367,#3314);
#2585=LINE('',#18392,#3315);
#2586=LINE('',#18417,#3316);
#2587=LINE('',#18441,#3317);
#2588=LINE('',#18466,#3318);
#2589=LINE('',#18491,#3319);
#2590=LINE('',#18515,#3320);
#2591=LINE('',#18540,#3321);
#2592=LINE('',#18564,#3322);
#2593=LINE('',#18589,#3323);
#2594=LINE('',#18790,#3324);
#2595=LINE('',#20535,#3325);
#2596=LINE('',#20537,#3326);
#2597=LINE('',#20539,#3327);
#2598=LINE('',#20540,#3328);
#2599=LINE('',#20543,#3329);
#2600=LINE('',#20545,#3330);
#2601=LINE('',#20546,#3331);
#2602=LINE('',#20549,#3332);
#2603=LINE('',#20551,#3333);
#2604=LINE('',#20552,#3334);
#2605=LINE('',#20555,#3335);
#2606=LINE('',#20557,#3336);
#2607=LINE('',#20558,#3337);
#2608=LINE('',#20561,#3338);
#2609=LINE('',#20563,#3339);
#2610=LINE('',#20564,#3340);
#2611=LINE('',#20566,#3341);
#2612=LINE('',#20567,#3342);
#2613=LINE('',#20574,#3343);
#3264=VECTOR('',#10912,0.15);
#3265=VECTOR('',#10917,0.15);
#3266=VECTOR('',#10920,0.15);
#3267=VECTOR('',#10923,0.15);
#3268=VECTOR('',#10926,0.15);
#3269=VECTOR('',#10929,0.15);
#3270=VECTOR('',#10932,0.15);
#3271=VECTOR('',#10935,0.15);
#3272=VECTOR('',#10938,0.15);
#3273=VECTOR('',#10941,0.15);
#3274=VECTOR('',#10944,0.15);
#3275=VECTOR('',#10947,0.15);
#3276=VECTOR('',#10950,0.15);
#3277=VECTOR('',#10953,0.15);
#3278=VECTOR('',#10956,0.15);
#3279=VECTOR('',#10959,0.15);
#3280=VECTOR('',#10962,0.15);
#3281=VECTOR('',#10965,0.15);
#3282=VECTOR('',#10968,0.15);
#3283=VECTOR('',#10971,0.15);
#3284=VECTOR('',#10974,0.15);
#3285=VECTOR('',#10977,0.15);
#3286=VECTOR('',#10980,0.15);
#3287=VECTOR('',#10983,0.15);
#3288=VECTOR('',#10986,0.15);
#3289=VECTOR('',#10989,0.15);
#3290=VECTOR('',#10992,0.15);
#3291=VECTOR('',#10995,0.15);
#3292=VECTOR('',#10998,0.15);
#3293=VECTOR('',#11001,0.15);
#3294=VECTOR('',#11004,0.117775);
#3295=VECTOR('',#11009,0.117775);
#3296=VECTOR('',#11012,0.117775);
#3297=VECTOR('',#11015,0.117775);
#3298=VECTOR('',#11018,0.117775);
#3299=VECTOR('',#11021,0.117775);
#3300=VECTOR('',#11024,0.117775);
#3301=VECTOR('',#11027,0.117775);
#3302=VECTOR('',#11030,0.117775);
#3303=VECTOR('',#11033,0.117775);
#3304=VECTOR('',#11036,0.117775);
#3305=VECTOR('',#11039,0.117775);
#3306=VECTOR('',#11042,0.117775);
#3307=VECTOR('',#11045,0.117775);
#3308=VECTOR('',#11048,0.117775);
#3309=VECTOR('',#11051,0.117775);
#3310=VECTOR('',#11054,0.117775);
#3311=VECTOR('',#11057,0.117775);
#3312=VECTOR('',#11060,0.117775);
#3313=VECTOR('',#11063,0.117775);
#3314=VECTOR('',#11066,0.117775);
#3315=VECTOR('',#11069,0.117775);
#3316=VECTOR('',#11072,0.117775);
#3317=VECTOR('',#11075,0.117775);
#3318=VECTOR('',#11078,0.117775);
#3319=VECTOR('',#11081,0.117775);
#3320=VECTOR('',#11084,0.117775);
#3321=VECTOR('',#11087,0.117775);
#3322=VECTOR('',#11090,0.117775);
#3323=VECTOR('',#11093,0.117775);
#3324=VECTOR('',#11098,0.1);
#3325=VECTOR('',#11109,1.);
#3326=VECTOR('',#11110,1.);
#3327=VECTOR('',#11111,1.);
#3328=VECTOR('',#11112,1.);
#3329=VECTOR('',#11115,1.);
#3330=VECTOR('',#11116,1.);
#3331=VECTOR('',#11117,1.);
#3332=VECTOR('',#11120,1.);
#3333=VECTOR('',#11121,1.);
#3334=VECTOR('',#11122,1.);
#3335=VECTOR('',#11125,1.);
#3336=VECTOR('',#11126,1.);
#3337=VECTOR('',#11127,1.);
#3338=VECTOR('',#11130,1.);
#3339=VECTOR('',#11131,1.);
#3340=VECTOR('',#11132,1.);
#3341=VECTOR('',#11135,1.);
#3342=VECTOR('',#11136,1.);
#3343=VECTOR('',#11145,0.275);
#3504=CIRCLE('',#9316,0.14635);
#3505=CIRCLE('',#9347,0.117775);
#3506=CIRCLE('',#9378,0.14635);
#3507=CIRCLE('',#9379,0.05);
#3508=CIRCLE('',#9381,0.117775);
#3509=CIRCLE('',#9391,0.275);
#3510=CIRCLE('',#9393,0.275);
#4144=VERTEX_POINT('',#16412);
#4145=VERTEX_POINT('',#16413);
#4146=VERTEX_POINT('',#16415);
#4147=VERTEX_POINT('',#16426);
#4148=VERTEX_POINT('',#16436);
#4149=VERTEX_POINT('',#16437);
#4150=VERTEX_POINT('',#16484);
#4151=VERTEX_POINT('',#16485);
#4152=VERTEX_POINT('',#16532);
#4153=VERTEX_POINT('',#16533);
#4154=VERTEX_POINT('',#16583);
#4155=VERTEX_POINT('',#16584);
#4156=VERTEX_POINT('',#16631);
#4157=VERTEX_POINT('',#16632);
#4158=VERTEX_POINT('',#16679);
#4159=VERTEX_POINT('',#16680);
#4160=VERTEX_POINT('',#16727);
#4161=VERTEX_POINT('',#16728);
#4162=VERTEX_POINT('',#16781);
#4163=VERTEX_POINT('',#16782);
#4164=VERTEX_POINT('',#16829);
#4165=VERTEX_POINT('',#16830);
#4166=VERTEX_POINT('',#16877);
#4167=VERTEX_POINT('',#16878);
#4168=VERTEX_POINT('',#16931);
#4169=VERTEX_POINT('',#16932);
#4170=VERTEX_POINT('',#16979);
#4171=VERTEX_POINT('',#16980);
#4172=VERTEX_POINT('',#17027);
#4173=VERTEX_POINT('',#17028);
#4174=VERTEX_POINT('',#17075);
#4175=VERTEX_POINT('',#17076);
#4176=VERTEX_POINT('',#17129);
#4177=VERTEX_POINT('',#17130);
#4178=VERTEX_POINT('',#17177);
#4179=VERTEX_POINT('',#17178);
#4180=VERTEX_POINT('',#17225);
#4181=VERTEX_POINT('',#17226);
#4182=VERTEX_POINT('',#17279);
#4183=VERTEX_POINT('',#17280);
#4184=VERTEX_POINT('',#17327);
#4185=VERTEX_POINT('',#17328);
#4186=VERTEX_POINT('',#17375);
#4187=VERTEX_POINT('',#17376);
#4188=VERTEX_POINT('',#17429);
#4189=VERTEX_POINT('',#17430);
#4190=VERTEX_POINT('',#17477);
#4191=VERTEX_POINT('',#17478);
#4192=VERTEX_POINT('',#17525);
#4193=VERTEX_POINT('',#17526);
#4194=VERTEX_POINT('',#17573);
#4195=VERTEX_POINT('',#17574);
#4196=VERTEX_POINT('',#17627);
#4197=VERTEX_POINT('',#17628);
#4198=VERTEX_POINT('',#17675);
#4199=VERTEX_POINT('',#17676);
#4200=VERTEX_POINT('',#17723);
#4201=VERTEX_POINT('',#17724);
#4202=VERTEX_POINT('',#17777);
#4203=VERTEX_POINT('',#17778);
#4204=VERTEX_POINT('',#17825);
#4205=VERTEX_POINT('',#17826);
#4206=VERTEX_POINT('',#17873);
#4207=VERTEX_POINT('',#17874);
#4208=VERTEX_POINT('',#17876);
#4209=VERTEX_POINT('',#17887);
#4210=VERTEX_POINT('',#17899);
#4211=VERTEX_POINT('',#17900);
#4212=VERTEX_POINT('',#17923);
#4213=VERTEX_POINT('',#17924);
#4214=VERTEX_POINT('',#17947);
#4215=VERTEX_POINT('',#17948);
#4216=VERTEX_POINT('',#17972);
#4217=VERTEX_POINT('',#17973);
#4218=VERTEX_POINT('',#17997);
#4219=VERTEX_POINT('',#17998);
#4220=VERTEX_POINT('',#18021);
#4221=VERTEX_POINT('',#18022);
#4222=VERTEX_POINT('',#18046);
#4223=VERTEX_POINT('',#18047);
#4224=VERTEX_POINT('',#18071);
#4225=VERTEX_POINT('',#18072);
#4226=VERTEX_POINT('',#18095);
#4227=VERTEX_POINT('',#18096);
#4228=VERTEX_POINT('',#18119);
#4229=VERTEX_POINT('',#18120);
#4230=VERTEX_POINT('',#18144);
#4231=VERTEX_POINT('',#18145);
#4232=VERTEX_POINT('',#18169);
#4233=VERTEX_POINT('',#18170);
#4234=VERTEX_POINT('',#18193);
#4235=VERTEX_POINT('',#18194);
#4236=VERTEX_POINT('',#18218);
#4237=VERTEX_POINT('',#18219);
#4238=VERTEX_POINT('',#18243);
#4239=VERTEX_POINT('',#18244);
#4240=VERTEX_POINT('',#18267);
#4241=VERTEX_POINT('',#18268);
#4242=VERTEX_POINT('',#18292);
#4243=VERTEX_POINT('',#18293);
#4244=VERTEX_POINT('',#18317);
#4245=VERTEX_POINT('',#18318);
#4246=VERTEX_POINT('',#18341);
#4247=VERTEX_POINT('',#18342);
#4248=VERTEX_POINT('',#18365);
#4249=VERTEX_POINT('',#18366);
#4250=VERTEX_POINT('',#18390);
#4251=VERTEX_POINT('',#18391);
#4252=VERTEX_POINT('',#18415);
#4253=VERTEX_POINT('',#18416);
#4254=VERTEX_POINT('',#18439);
#4255=VERTEX_POINT('',#18440);
#4256=VERTEX_POINT('',#18464);
#4257=VERTEX_POINT('',#18465);
#4258=VERTEX_POINT('',#18489);
#4259=VERTEX_POINT('',#18490);
#4260=VERTEX_POINT('',#18513);
#4261=VERTEX_POINT('',#18514);
#4262=VERTEX_POINT('',#18538);
#4263=VERTEX_POINT('',#18539);
#4264=VERTEX_POINT('',#18562);
#4265=VERTEX_POINT('',#18563);
#4266=VERTEX_POINT('',#18587);
#4267=VERTEX_POINT('',#18588);
#4268=VERTEX_POINT('',#18611);
#4269=VERTEX_POINT('',#18733);
#4270=VERTEX_POINT('',#18771);
#4271=VERTEX_POINT('',#18789);
#4272=VERTEX_POINT('',#19576);
#4273=VERTEX_POINT('',#19654);
#4274=VERTEX_POINT('',#20533);
#4275=VERTEX_POINT('',#20534);
#4276=VERTEX_POINT('',#20536);
#4277=VERTEX_POINT('',#20538);
#4278=VERTEX_POINT('',#20542);
#4279=VERTEX_POINT('',#20544);
#4280=VERTEX_POINT('',#20548);
#4281=VERTEX_POINT('',#20550);
#4282=VERTEX_POINT('',#20554);
#4283=VERTEX_POINT('',#20556);
#4284=VERTEX_POINT('',#20560);
#4285=VERTEX_POINT('',#20562);
#4286=VERTEX_POINT('',#20570);
#4287=VERTEX_POINT('',#20573);
#5294=EDGE_CURVE('',#4144,#4145,#2534,.T.);
#5295=EDGE_CURVE('',#4144,#4146,#372,.T.);
#5296=EDGE_CURVE('',#4146,#4147,#3504,.F.);
#5297=EDGE_CURVE('',#4147,#4145,#373,.T.);
#5298=EDGE_CURVE('',#4148,#4149,#2535,.T.);
#5299=EDGE_CURVE('',#4148,#4144,#374,.T.);
#5300=EDGE_CURVE('',#4145,#4149,#375,.T.);
#5301=EDGE_CURVE('',#4150,#4151,#2536,.T.);
#5302=EDGE_CURVE('',#4150,#4148,#376,.T.);
#5303=EDGE_CURVE('',#4149,#4151,#377,.T.);
#5304=EDGE_CURVE('',#4152,#4153,#2537,.T.);
#5305=EDGE_CURVE('',#4152,#4150,#378,.T.);
#5306=EDGE_CURVE('',#4151,#4153,#379,.T.);
#5307=EDGE_CURVE('',#4154,#4155,#2538,.T.);
#5308=EDGE_CURVE('',#4154,#4152,#380,.T.);
#5309=EDGE_CURVE('',#4153,#4155,#381,.T.);
#5310=EDGE_CURVE('',#4156,#4157,#2539,.T.);
#5311=EDGE_CURVE('',#4156,#4154,#382,.T.);
#5312=EDGE_CURVE('',#4155,#4157,#383,.T.);
#5313=EDGE_CURVE('',#4158,#4159,#2540,.T.);
#5314=EDGE_CURVE('',#4158,#4156,#384,.T.);
#5315=EDGE_CURVE('',#4157,#4159,#385,.T.);
#5316=EDGE_CURVE('',#4160,#4161,#2541,.T.);
#5317=EDGE_CURVE('',#4160,#4158,#386,.T.);
#5318=EDGE_CURVE('',#4159,#4161,#387,.T.);
#5319=EDGE_CURVE('',#4162,#4163,#2542,.T.);
#5320=EDGE_CURVE('',#4162,#4160,#388,.T.);
#5321=EDGE_CURVE('',#4161,#4163,#389,.T.);
#5322=EDGE_CURVE('',#4164,#4165,#2543,.T.);
#5323=EDGE_CURVE('',#4164,#4162,#390,.T.);
#5324=EDGE_CURVE('',#4163,#4165,#391,.T.);
#5325=EDGE_CURVE('',#4166,#4167,#2544,.T.);
#5326=EDGE_CURVE('',#4166,#4164,#392,.T.);
#5327=EDGE_CURVE('',#4165,#4167,#393,.T.);
#5328=EDGE_CURVE('',#4168,#4169,#2545,.T.);
#5329=EDGE_CURVE('',#4168,#4166,#394,.T.);
#5330=EDGE_CURVE('',#4167,#4169,#395,.T.);
#5331=EDGE_CURVE('',#4170,#4171,#2546,.T.);
#5332=EDGE_CURVE('',#4170,#4168,#396,.T.);
#5333=EDGE_CURVE('',#4169,#4171,#397,.T.);
#5334=EDGE_CURVE('',#4172,#4173,#2547,.T.);
#5335=EDGE_CURVE('',#4172,#4170,#398,.T.);
#5336=EDGE_CURVE('',#4171,#4173,#399,.T.);
#5337=EDGE_CURVE('',#4174,#4175,#2548,.T.);
#5338=EDGE_CURVE('',#4174,#4172,#400,.T.);
#5339=EDGE_CURVE('',#4173,#4175,#401,.T.);
#5340=EDGE_CURVE('',#4176,#4177,#2549,.T.);
#5341=EDGE_CURVE('',#4176,#4174,#402,.T.);
#5342=EDGE_CURVE('',#4175,#4177,#403,.T.);
#5343=EDGE_CURVE('',#4178,#4179,#2550,.T.);
#5344=EDGE_CURVE('',#4178,#4176,#404,.T.);
#5345=EDGE_CURVE('',#4177,#4179,#405,.T.);
#5346=EDGE_CURVE('',#4180,#4181,#2551,.T.);
#5347=EDGE_CURVE('',#4180,#4178,#406,.T.);
#5348=EDGE_CURVE('',#4179,#4181,#407,.T.);
#5349=EDGE_CURVE('',#4182,#4183,#2552,.T.);
#5350=EDGE_CURVE('',#4182,#4180,#408,.T.);
#5351=EDGE_CURVE('',#4181,#4183,#409,.T.);
#5352=EDGE_CURVE('',#4184,#4185,#2553,.T.);
#5353=EDGE_CURVE('',#4184,#4182,#410,.T.);
#5354=EDGE_CURVE('',#4183,#4185,#411,.T.);
#5355=EDGE_CURVE('',#4186,#4187,#2554,.T.);
#5356=EDGE_CURVE('',#4186,#4184,#412,.T.);
#5357=EDGE_CURVE('',#4185,#4187,#413,.T.);
#5358=EDGE_CURVE('',#4188,#4189,#2555,.T.);
#5359=EDGE_CURVE('',#4188,#4186,#414,.T.);
#5360=EDGE_CURVE('',#4187,#4189,#415,.T.);
#5361=EDGE_CURVE('',#4190,#4191,#2556,.T.);
#5362=EDGE_CURVE('',#4190,#4188,#416,.T.);
#5363=EDGE_CURVE('',#4189,#4191,#417,.T.);
#5364=EDGE_CURVE('',#4192,#4193,#2557,.T.);
#5365=EDGE_CURVE('',#4192,#4190,#418,.T.);
#5366=EDGE_CURVE('',#4191,#4193,#419,.T.);
#5367=EDGE_CURVE('',#4194,#4195,#2558,.T.);
#5368=EDGE_CURVE('',#4194,#4192,#420,.T.);
#5369=EDGE_CURVE('',#4193,#4195,#421,.T.);
#5370=EDGE_CURVE('',#4196,#4197,#2559,.T.);
#5371=EDGE_CURVE('',#4196,#4194,#422,.T.);
#5372=EDGE_CURVE('',#4195,#4197,#423,.T.);
#5373=EDGE_CURVE('',#4198,#4199,#2560,.T.);
#5374=EDGE_CURVE('',#4198,#4196,#424,.T.);
#5375=EDGE_CURVE('',#4197,#4199,#425,.T.);
#5376=EDGE_CURVE('',#4200,#4201,#2561,.T.);
#5377=EDGE_CURVE('',#4200,#4198,#426,.T.);
#5378=EDGE_CURVE('',#4199,#4201,#427,.T.);
#5379=EDGE_CURVE('',#4202,#4203,#2562,.T.);
#5380=EDGE_CURVE('',#4202,#4200,#428,.T.);
#5381=EDGE_CURVE('',#4201,#4203,#429,.T.);
#5382=EDGE_CURVE('',#4204,#4205,#2563,.T.);
#5383=EDGE_CURVE('',#4204,#4202,#430,.T.);
#5384=EDGE_CURVE('',#4203,#4205,#431,.T.);
#5385=EDGE_CURVE('',#4206,#4207,#2564,.T.);
#5386=EDGE_CURVE('',#4206,#4208,#432,.T.);
#5387=EDGE_CURVE('',#4208,#4209,#3505,.T.);
#5388=EDGE_CURVE('',#4207,#4209,#433,.T.);
#5389=EDGE_CURVE('',#4210,#4211,#2565,.T.);
#5390=EDGE_CURVE('',#4210,#4206,#434,.T.);
#5391=EDGE_CURVE('',#4211,#4207,#435,.T.);
#5392=EDGE_CURVE('',#4212,#4213,#2566,.T.);
#5393=EDGE_CURVE('',#4212,#4210,#436,.T.);
#5394=EDGE_CURVE('',#4213,#4211,#437,.T.);
#5395=EDGE_CURVE('',#4214,#4215,#2567,.T.);
#5396=EDGE_CURVE('',#4214,#4212,#438,.T.);
#5397=EDGE_CURVE('',#4215,#4213,#439,.T.);
#5398=EDGE_CURVE('',#4216,#4217,#2568,.T.);
#5399=EDGE_CURVE('',#4216,#4214,#440,.T.);
#5400=EDGE_CURVE('',#4217,#4215,#441,.T.);
#5401=EDGE_CURVE('',#4218,#4219,#2569,.T.);
#5402=EDGE_CURVE('',#4218,#4216,#442,.T.);
#5403=EDGE_CURVE('',#4219,#4217,#443,.T.);
#5404=EDGE_CURVE('',#4220,#4221,#2570,.T.);
#5405=EDGE_CURVE('',#4220,#4218,#444,.T.);
#5406=EDGE_CURVE('',#4221,#4219,#445,.T.);
#5407=EDGE_CURVE('',#4222,#4223,#2571,.T.);
#5408=EDGE_CURVE('',#4222,#4220,#446,.T.);
#5409=EDGE_CURVE('',#4223,#4221,#447,.T.);
#5410=EDGE_CURVE('',#4224,#4225,#2572,.T.);
#5411=EDGE_CURVE('',#4224,#4222,#448,.T.);
#5412=EDGE_CURVE('',#4225,#4223,#449,.T.);
#5413=EDGE_CURVE('',#4226,#4227,#2573,.T.);
#5414=EDGE_CURVE('',#4226,#4224,#450,.T.);
#5415=EDGE_CURVE('',#4227,#4225,#451,.T.);
#5416=EDGE_CURVE('',#4228,#4229,#2574,.T.);
#5417=EDGE_CURVE('',#4228,#4226,#452,.T.);
#5418=EDGE_CURVE('',#4229,#4227,#453,.T.);
#5419=EDGE_CURVE('',#4230,#4231,#2575,.T.);
#5420=EDGE_CURVE('',#4230,#4228,#454,.T.);
#5421=EDGE_CURVE('',#4231,#4229,#455,.T.);
#5422=EDGE_CURVE('',#4232,#4233,#2576,.T.);
#5423=EDGE_CURVE('',#4232,#4230,#456,.T.);
#5424=EDGE_CURVE('',#4233,#4231,#457,.T.);
#5425=EDGE_CURVE('',#4234,#4235,#2577,.T.);
#5426=EDGE_CURVE('',#4234,#4232,#458,.T.);
#5427=EDGE_CURVE('',#4235,#4233,#459,.T.);
#5428=EDGE_CURVE('',#4236,#4237,#2578,.T.);
#5429=EDGE_CURVE('',#4236,#4234,#460,.T.);
#5430=EDGE_CURVE('',#4237,#4235,#461,.T.);
#5431=EDGE_CURVE('',#4238,#4239,#2579,.T.);
#5432=EDGE_CURVE('',#4238,#4236,#462,.T.);
#5433=EDGE_CURVE('',#4239,#4237,#463,.T.);
#5434=EDGE_CURVE('',#4240,#4241,#2580,.T.);
#5435=EDGE_CURVE('',#4240,#4238,#464,.T.);
#5436=EDGE_CURVE('',#4241,#4239,#465,.T.);
#5437=EDGE_CURVE('',#4242,#4243,#2581,.T.);
#5438=EDGE_CURVE('',#4242,#4240,#466,.T.);
#5439=EDGE_CURVE('',#4243,#4241,#467,.T.);
#5440=EDGE_CURVE('',#4244,#4245,#2582,.T.);
#5441=EDGE_CURVE('',#4244,#4242,#468,.T.);
#5442=EDGE_CURVE('',#4245,#4243,#469,.T.);
#5443=EDGE_CURVE('',#4246,#4247,#2583,.T.);
#5444=EDGE_CURVE('',#4246,#4244,#470,.T.);
#5445=EDGE_CURVE('',#4247,#4245,#471,.T.);
#5446=EDGE_CURVE('',#4248,#4249,#2584,.T.);
#5447=EDGE_CURVE('',#4248,#4246,#472,.T.);
#5448=EDGE_CURVE('',#4249,#4247,#473,.T.);
#5449=EDGE_CURVE('',#4250,#4251,#2585,.T.);
#5450=EDGE_CURVE('',#4250,#4248,#474,.T.);
#5451=EDGE_CURVE('',#4251,#4249,#475,.T.);
#5452=EDGE_CURVE('',#4252,#4253,#2586,.T.);
#5453=EDGE_CURVE('',#4252,#4250,#476,.T.);
#5454=EDGE_CURVE('',#4253,#4251,#477,.T.);
#5455=EDGE_CURVE('',#4254,#4255,#2587,.T.);
#5456=EDGE_CURVE('',#4254,#4252,#478,.T.);
#5457=EDGE_CURVE('',#4255,#4253,#479,.T.);
#5458=EDGE_CURVE('',#4256,#4257,#2588,.T.);
#5459=EDGE_CURVE('',#4256,#4254,#480,.T.);
#5460=EDGE_CURVE('',#4257,#4255,#481,.T.);
#5461=EDGE_CURVE('',#4258,#4259,#2589,.T.);
#5462=EDGE_CURVE('',#4258,#4256,#482,.T.);
#5463=EDGE_CURVE('',#4259,#4257,#483,.T.);
#5464=EDGE_CURVE('',#4260,#4261,#2590,.T.);
#5465=EDGE_CURVE('',#4260,#4258,#484,.T.);
#5466=EDGE_CURVE('',#4261,#4259,#485,.T.);
#5467=EDGE_CURVE('',#4262,#4263,#2591,.T.);
#5468=EDGE_CURVE('',#4262,#4260,#486,.T.);
#5469=EDGE_CURVE('',#4263,#4261,#487,.T.);
#5470=EDGE_CURVE('',#4264,#4265,#2592,.T.);
#5471=EDGE_CURVE('',#4264,#4262,#488,.T.);
#5472=EDGE_CURVE('',#4265,#4263,#489,.T.);
#5473=EDGE_CURVE('',#4266,#4267,#2593,.T.);
#5474=EDGE_CURVE('',#4266,#4264,#490,.T.);
#5475=EDGE_CURVE('',#4267,#4265,#491,.T.);
#5476=EDGE_CURVE('',#4209,#4268,#492,.T.);
#5477=EDGE_CURVE('',#4269,#4208,#493,.T.);
#5478=EDGE_CURVE('',#4270,#4269,#3506,.T.);
#5479=EDGE_CURVE('',#4268,#4270,#494,.T.);
#5480=EDGE_CURVE('',#4268,#4271,#2594,.T.);
#5481=EDGE_CURVE('',#4271,#4271,#3507,.T.);
#5482=EDGE_CURVE('',#4272,#4266,#495,.T.);
#5483=EDGE_CURVE('',#4146,#4272,#496,.T.);
#5484=EDGE_CURVE('',#4269,#4204,#497,.T.);
#5485=EDGE_CURVE('',#4273,#4267,#498,.T.);
#5486=EDGE_CURVE('',#4272,#4273,#3508,.T.);
#5487=EDGE_CURVE('',#4205,#4270,#499,.T.);
#5488=EDGE_CURVE('',#4273,#4147,#500,.T.);
#5489=EDGE_CURVE('',#4274,#4275,#2595,.T.);
#5490=EDGE_CURVE('',#4274,#4276,#2596,.T.);
#5491=EDGE_CURVE('',#4276,#4277,#2597,.T.);
#5492=EDGE_CURVE('',#4275,#4277,#2598,.T.);
#5493=EDGE_CURVE('',#4278,#4274,#2599,.T.);
#5494=EDGE_CURVE('',#4278,#4279,#2600,.T.);
#5495=EDGE_CURVE('',#4279,#4276,#2601,.T.);
#5496=EDGE_CURVE('',#4280,#4278,#2602,.T.);
#5497=EDGE_CURVE('',#4280,#4281,#2603,.T.);
#5498=EDGE_CURVE('',#4281,#4279,#2604,.T.);
#5499=EDGE_CURVE('',#4282,#4280,#2605,.T.);
#5500=EDGE_CURVE('',#4282,#4283,#2606,.T.);
#5501=EDGE_CURVE('',#4283,#4281,#2607,.T.);
#5502=EDGE_CURVE('',#4284,#4282,#2608,.T.);
#5503=EDGE_CURVE('',#4284,#4285,#2609,.T.);
#5504=EDGE_CURVE('',#4285,#4283,#2610,.T.);
#5505=EDGE_CURVE('',#4275,#4284,#2611,.T.);
#5506=EDGE_CURVE('',#4277,#4285,#2612,.T.);
#5507=EDGE_CURVE('',#4286,#4286,#3509,.T.);
#5508=EDGE_CURVE('',#4286,#4287,#2613,.T.);
#5509=EDGE_CURVE('',#4287,#4287,#3510,.T.);
#7482=ORIENTED_EDGE('',*,*,#5294,.F.);
#7483=ORIENTED_EDGE('',*,*,#5295,.T.);
#7484=ORIENTED_EDGE('',*,*,#5296,.T.);
#7485=ORIENTED_EDGE('',*,*,#5297,.T.);
#7486=ORIENTED_EDGE('',*,*,#5298,.F.);
#7487=ORIENTED_EDGE('',*,*,#5299,.T.);
#7488=ORIENTED_EDGE('',*,*,#5294,.T.);
#7489=ORIENTED_EDGE('',*,*,#5300,.T.);
#7490=ORIENTED_EDGE('',*,*,#5301,.F.);
#7491=ORIENTED_EDGE('',*,*,#5302,.T.);
#7492=ORIENTED_EDGE('',*,*,#5298,.T.);
#7493=ORIENTED_EDGE('',*,*,#5303,.T.);
#7494=ORIENTED_EDGE('',*,*,#5304,.F.);
#7495=ORIENTED_EDGE('',*,*,#5305,.T.);
#7496=ORIENTED_EDGE('',*,*,#5301,.T.);
#7497=ORIENTED_EDGE('',*,*,#5306,.T.);
#7498=ORIENTED_EDGE('',*,*,#5307,.F.);
#7499=ORIENTED_EDGE('',*,*,#5308,.T.);
#7500=ORIENTED_EDGE('',*,*,#5304,.T.);
#7501=ORIENTED_EDGE('',*,*,#5309,.T.);
#7502=ORIENTED_EDGE('',*,*,#5310,.F.);
#7503=ORIENTED_EDGE('',*,*,#5311,.T.);
#7504=ORIENTED_EDGE('',*,*,#5307,.T.);
#7505=ORIENTED_EDGE('',*,*,#5312,.T.);
#7506=ORIENTED_EDGE('',*,*,#5313,.F.);
#7507=ORIENTED_EDGE('',*,*,#5314,.T.);
#7508=ORIENTED_EDGE('',*,*,#5310,.T.);
#7509=ORIENTED_EDGE('',*,*,#5315,.T.);
#7510=ORIENTED_EDGE('',*,*,#5316,.F.);
#7511=ORIENTED_EDGE('',*,*,#5317,.T.);
#7512=ORIENTED_EDGE('',*,*,#5313,.T.);
#7513=ORIENTED_EDGE('',*,*,#5318,.T.);
#7514=ORIENTED_EDGE('',*,*,#5319,.F.);
#7515=ORIENTED_EDGE('',*,*,#5320,.T.);
#7516=ORIENTED_EDGE('',*,*,#5316,.T.);
#7517=ORIENTED_EDGE('',*,*,#5321,.T.);
#7518=ORIENTED_EDGE('',*,*,#5322,.F.);
#7519=ORIENTED_EDGE('',*,*,#5323,.T.);
#7520=ORIENTED_EDGE('',*,*,#5319,.T.);
#7521=ORIENTED_EDGE('',*,*,#5324,.T.);
#7522=ORIENTED_EDGE('',*,*,#5325,.F.);
#7523=ORIENTED_EDGE('',*,*,#5326,.T.);
#7524=ORIENTED_EDGE('',*,*,#5322,.T.);
#7525=ORIENTED_EDGE('',*,*,#5327,.T.);
#7526=ORIENTED_EDGE('',*,*,#5328,.F.);
#7527=ORIENTED_EDGE('',*,*,#5329,.T.);
#7528=ORIENTED_EDGE('',*,*,#5325,.T.);
#7529=ORIENTED_EDGE('',*,*,#5330,.T.);
#7530=ORIENTED_EDGE('',*,*,#5331,.F.);
#7531=ORIENTED_EDGE('',*,*,#5332,.T.);
#7532=ORIENTED_EDGE('',*,*,#5328,.T.);
#7533=ORIENTED_EDGE('',*,*,#5333,.T.);
#7534=ORIENTED_EDGE('',*,*,#5334,.F.);
#7535=ORIENTED_EDGE('',*,*,#5335,.T.);
#7536=ORIENTED_EDGE('',*,*,#5331,.T.);
#7537=ORIENTED_EDGE('',*,*,#5336,.T.);
#7538=ORIENTED_EDGE('',*,*,#5337,.F.);
#7539=ORIENTED_EDGE('',*,*,#5338,.T.);
#7540=ORIENTED_EDGE('',*,*,#5334,.T.);
#7541=ORIENTED_EDGE('',*,*,#5339,.T.);
#7542=ORIENTED_EDGE('',*,*,#5340,.F.);
#7543=ORIENTED_EDGE('',*,*,#5341,.T.);
#7544=ORIENTED_EDGE('',*,*,#5337,.T.);
#7545=ORIENTED_EDGE('',*,*,#5342,.T.);
#7546=ORIENTED_EDGE('',*,*,#5343,.F.);
#7547=ORIENTED_EDGE('',*,*,#5344,.T.);
#7548=ORIENTED_EDGE('',*,*,#5340,.T.);
#7549=ORIENTED_EDGE('',*,*,#5345,.T.);
#7550=ORIENTED_EDGE('',*,*,#5346,.F.);
#7551=ORIENTED_EDGE('',*,*,#5347,.T.);
#7552=ORIENTED_EDGE('',*,*,#5343,.T.);
#7553=ORIENTED_EDGE('',*,*,#5348,.T.);
#7554=ORIENTED_EDGE('',*,*,#5349,.F.);
#7555=ORIENTED_EDGE('',*,*,#5350,.T.);
#7556=ORIENTED_EDGE('',*,*,#5346,.T.);
#7557=ORIENTED_EDGE('',*,*,#5351,.T.);
#7558=ORIENTED_EDGE('',*,*,#5352,.F.);
#7559=ORIENTED_EDGE('',*,*,#5353,.T.);
#7560=ORIENTED_EDGE('',*,*,#5349,.T.);
#7561=ORIENTED_EDGE('',*,*,#5354,.T.);
#7562=ORIENTED_EDGE('',*,*,#5355,.F.);
#7563=ORIENTED_EDGE('',*,*,#5356,.T.);
#7564=ORIENTED_EDGE('',*,*,#5352,.T.);
#7565=ORIENTED_EDGE('',*,*,#5357,.T.);
#7566=ORIENTED_EDGE('',*,*,#5358,.F.);
#7567=ORIENTED_EDGE('',*,*,#5359,.T.);
#7568=ORIENTED_EDGE('',*,*,#5355,.T.);
#7569=ORIENTED_EDGE('',*,*,#5360,.T.);
#7570=ORIENTED_EDGE('',*,*,#5361,.F.);
#7571=ORIENTED_EDGE('',*,*,#5362,.T.);
#7572=ORIENTED_EDGE('',*,*,#5358,.T.);
#7573=ORIENTED_EDGE('',*,*,#5363,.T.);
#7574=ORIENTED_EDGE('',*,*,#5364,.F.);
#7575=ORIENTED_EDGE('',*,*,#5365,.T.);
#7576=ORIENTED_EDGE('',*,*,#5361,.T.);
#7577=ORIENTED_EDGE('',*,*,#5366,.T.);
#7578=ORIENTED_EDGE('',*,*,#5367,.F.);
#7579=ORIENTED_EDGE('',*,*,#5368,.T.);
#7580=ORIENTED_EDGE('',*,*,#5364,.T.);
#7581=ORIENTED_EDGE('',*,*,#5369,.T.);
#7582=ORIENTED_EDGE('',*,*,#5370,.F.);
#7583=ORIENTED_EDGE('',*,*,#5371,.T.);
#7584=ORIENTED_EDGE('',*,*,#5367,.T.);
#7585=ORIENTED_EDGE('',*,*,#5372,.T.);
#7586=ORIENTED_EDGE('',*,*,#5373,.F.);
#7587=ORIENTED_EDGE('',*,*,#5374,.T.);
#7588=ORIENTED_EDGE('',*,*,#5370,.T.);
#7589=ORIENTED_EDGE('',*,*,#5375,.T.);
#7590=ORIENTED_EDGE('',*,*,#5376,.F.);
#7591=ORIENTED_EDGE('',*,*,#5377,.T.);
#7592=ORIENTED_EDGE('',*,*,#5373,.T.);
#7593=ORIENTED_EDGE('',*,*,#5378,.T.);
#7594=ORIENTED_EDGE('',*,*,#5379,.F.);
#7595=ORIENTED_EDGE('',*,*,#5380,.T.);
#7596=ORIENTED_EDGE('',*,*,#5376,.T.);
#7597=ORIENTED_EDGE('',*,*,#5381,.T.);
#7598=ORIENTED_EDGE('',*,*,#5382,.F.);
#7599=ORIENTED_EDGE('',*,*,#5383,.T.);
#7600=ORIENTED_EDGE('',*,*,#5379,.T.);
#7601=ORIENTED_EDGE('',*,*,#5384,.T.);
#7602=ORIENTED_EDGE('',*,*,#5385,.F.);
#7603=ORIENTED_EDGE('',*,*,#5386,.T.);
#7604=ORIENTED_EDGE('',*,*,#5387,.T.);
#7605=ORIENTED_EDGE('',*,*,#5388,.F.);
#7606=ORIENTED_EDGE('',*,*,#5389,.F.);
#7607=ORIENTED_EDGE('',*,*,#5390,.T.);
#7608=ORIENTED_EDGE('',*,*,#5385,.T.);
#7609=ORIENTED_EDGE('',*,*,#5391,.F.);
#7610=ORIENTED_EDGE('',*,*,#5392,.F.);
#7611=ORIENTED_EDGE('',*,*,#5393,.T.);
#7612=ORIENTED_EDGE('',*,*,#5389,.T.);
#7613=ORIENTED_EDGE('',*,*,#5394,.F.);
#7614=ORIENTED_EDGE('',*,*,#5395,.F.);
#7615=ORIENTED_EDGE('',*,*,#5396,.T.);
#7616=ORIENTED_EDGE('',*,*,#5392,.T.);
#7617=ORIENTED_EDGE('',*,*,#5397,.F.);
#7618=ORIENTED_EDGE('',*,*,#5398,.F.);
#7619=ORIENTED_EDGE('',*,*,#5399,.T.);
#7620=ORIENTED_EDGE('',*,*,#5395,.T.);
#7621=ORIENTED_EDGE('',*,*,#5400,.F.);
#7622=ORIENTED_EDGE('',*,*,#5401,.F.);
#7623=ORIENTED_EDGE('',*,*,#5402,.T.);
#7624=ORIENTED_EDGE('',*,*,#5398,.T.);
#7625=ORIENTED_EDGE('',*,*,#5403,.F.);
#7626=ORIENTED_EDGE('',*,*,#5404,.F.);
#7627=ORIENTED_EDGE('',*,*,#5405,.T.);
#7628=ORIENTED_EDGE('',*,*,#5401,.T.);
#7629=ORIENTED_EDGE('',*,*,#5406,.F.);
#7630=ORIENTED_EDGE('',*,*,#5407,.F.);
#7631=ORIENTED_EDGE('',*,*,#5408,.T.);
#7632=ORIENTED_EDGE('',*,*,#5404,.T.);
#7633=ORIENTED_EDGE('',*,*,#5409,.F.);
#7634=ORIENTED_EDGE('',*,*,#5410,.F.);
#7635=ORIENTED_EDGE('',*,*,#5411,.T.);
#7636=ORIENTED_EDGE('',*,*,#5407,.T.);
#7637=ORIENTED_EDGE('',*,*,#5412,.F.);
#7638=ORIENTED_EDGE('',*,*,#5413,.F.);
#7639=ORIENTED_EDGE('',*,*,#5414,.T.);
#7640=ORIENTED_EDGE('',*,*,#5410,.T.);
#7641=ORIENTED_EDGE('',*,*,#5415,.F.);
#7642=ORIENTED_EDGE('',*,*,#5416,.F.);
#7643=ORIENTED_EDGE('',*,*,#5417,.T.);
#7644=ORIENTED_EDGE('',*,*,#5413,.T.);
#7645=ORIENTED_EDGE('',*,*,#5418,.F.);
#7646=ORIENTED_EDGE('',*,*,#5419,.F.);
#7647=ORIENTED_EDGE('',*,*,#5420,.T.);
#7648=ORIENTED_EDGE('',*,*,#5416,.T.);
#7649=ORIENTED_EDGE('',*,*,#5421,.F.);
#7650=ORIENTED_EDGE('',*,*,#5422,.F.);
#7651=ORIENTED_EDGE('',*,*,#5423,.T.);
#7652=ORIENTED_EDGE('',*,*,#5419,.T.);
#7653=ORIENTED_EDGE('',*,*,#5424,.F.);
#7654=ORIENTED_EDGE('',*,*,#5425,.F.);
#7655=ORIENTED_EDGE('',*,*,#5426,.T.);
#7656=ORIENTED_EDGE('',*,*,#5422,.T.);
#7657=ORIENTED_EDGE('',*,*,#5427,.F.);
#7658=ORIENTED_EDGE('',*,*,#5428,.F.);
#7659=ORIENTED_EDGE('',*,*,#5429,.T.);
#7660=ORIENTED_EDGE('',*,*,#5425,.T.);
#7661=ORIENTED_EDGE('',*,*,#5430,.F.);
#7662=ORIENTED_EDGE('',*,*,#5431,.F.);
#7663=ORIENTED_EDGE('',*,*,#5432,.T.);
#7664=ORIENTED_EDGE('',*,*,#5428,.T.);
#7665=ORIENTED_EDGE('',*,*,#5433,.F.);
#7666=ORIENTED_EDGE('',*,*,#5434,.F.);
#7667=ORIENTED_EDGE('',*,*,#5435,.T.);
#7668=ORIENTED_EDGE('',*,*,#5431,.T.);
#7669=ORIENTED_EDGE('',*,*,#5436,.F.);
#7670=ORIENTED_EDGE('',*,*,#5437,.F.);
#7671=ORIENTED_EDGE('',*,*,#5438,.T.);
#7672=ORIENTED_EDGE('',*,*,#5434,.T.);
#7673=ORIENTED_EDGE('',*,*,#5439,.F.);
#7674=ORIENTED_EDGE('',*,*,#5440,.F.);
#7675=ORIENTED_EDGE('',*,*,#5441,.T.);
#7676=ORIENTED_EDGE('',*,*,#5437,.T.);
#7677=ORIENTED_EDGE('',*,*,#5442,.F.);
#7678=ORIENTED_EDGE('',*,*,#5443,.F.);
#7679=ORIENTED_EDGE('',*,*,#5444,.T.);
#7680=ORIENTED_EDGE('',*,*,#5440,.T.);
#7681=ORIENTED_EDGE('',*,*,#5445,.F.);
#7682=ORIENTED_EDGE('',*,*,#5446,.F.);
#7683=ORIENTED_EDGE('',*,*,#5447,.T.);
#7684=ORIENTED_EDGE('',*,*,#5443,.T.);
#7685=ORIENTED_EDGE('',*,*,#5448,.F.);
#7686=ORIENTED_EDGE('',*,*,#5449,.F.);
#7687=ORIENTED_EDGE('',*,*,#5450,.T.);
#7688=ORIENTED_EDGE('',*,*,#5446,.T.);
#7689=ORIENTED_EDGE('',*,*,#5451,.F.);
#7690=ORIENTED_EDGE('',*,*,#5452,.F.);
#7691=ORIENTED_EDGE('',*,*,#5453,.T.);
#7692=ORIENTED_EDGE('',*,*,#5449,.T.);
#7693=ORIENTED_EDGE('',*,*,#5454,.F.);
#7694=ORIENTED_EDGE('',*,*,#5455,.F.);
#7695=ORIENTED_EDGE('',*,*,#5456,.T.);
#7696=ORIENTED_EDGE('',*,*,#5452,.T.);
#7697=ORIENTED_EDGE('',*,*,#5457,.F.);
#7698=ORIENTED_EDGE('',*,*,#5458,.F.);
#7699=ORIENTED_EDGE('',*,*,#5459,.T.);
#7700=ORIENTED_EDGE('',*,*,#5455,.T.);
#7701=ORIENTED_EDGE('',*,*,#5460,.F.);
#7702=ORIENTED_EDGE('',*,*,#5461,.F.);
#7703=ORIENTED_EDGE('',*,*,#5462,.T.);
#7704=ORIENTED_EDGE('',*,*,#5458,.T.);
#7705=ORIENTED_EDGE('',*,*,#5463,.F.);
#7706=ORIENTED_EDGE('',*,*,#5464,.F.);
#7707=ORIENTED_EDGE('',*,*,#5465,.T.);
#7708=ORIENTED_EDGE('',*,*,#5461,.T.);
#7709=ORIENTED_EDGE('',*,*,#5466,.F.);
#7710=ORIENTED_EDGE('',*,*,#5467,.F.);
#7711=ORIENTED_EDGE('',*,*,#5468,.T.);
#7712=ORIENTED_EDGE('',*,*,#5464,.T.);
#7713=ORIENTED_EDGE('',*,*,#5469,.F.);
#7714=ORIENTED_EDGE('',*,*,#5470,.F.);
#7715=ORIENTED_EDGE('',*,*,#5471,.T.);
#7716=ORIENTED_EDGE('',*,*,#5467,.T.);
#7717=ORIENTED_EDGE('',*,*,#5472,.F.);
#7718=ORIENTED_EDGE('',*,*,#5473,.F.);
#7719=ORIENTED_EDGE('',*,*,#5474,.T.);
#7720=ORIENTED_EDGE('',*,*,#5470,.T.);
#7721=ORIENTED_EDGE('',*,*,#5475,.F.);
#7722=ORIENTED_EDGE('',*,*,#5476,.F.);
#7723=ORIENTED_EDGE('',*,*,#5387,.F.);
#7724=ORIENTED_EDGE('',*,*,#5477,.F.);
#7725=ORIENTED_EDGE('',*,*,#5478,.F.);
#7726=ORIENTED_EDGE('',*,*,#5479,.F.);
#7727=ORIENTED_EDGE('',*,*,#5480,.T.);
#7728=ORIENTED_EDGE('',*,*,#5481,.F.);
#7729=ORIENTED_EDGE('',*,*,#5480,.F.);
#7730=ORIENTED_EDGE('',*,*,#5477,.T.);
#7731=ORIENTED_EDGE('',*,*,#5386,.F.);
#7732=ORIENTED_EDGE('',*,*,#5390,.F.);
#7733=ORIENTED_EDGE('',*,*,#5393,.F.);
#7734=ORIENTED_EDGE('',*,*,#5396,.F.);
#7735=ORIENTED_EDGE('',*,*,#5399,.F.);
#7736=ORIENTED_EDGE('',*,*,#5402,.F.);
#7737=ORIENTED_EDGE('',*,*,#5405,.F.);
#7738=ORIENTED_EDGE('',*,*,#5408,.F.);
#7739=ORIENTED_EDGE('',*,*,#5411,.F.);
#7740=ORIENTED_EDGE('',*,*,#5414,.F.);
#7741=ORIENTED_EDGE('',*,*,#5417,.F.);
#7742=ORIENTED_EDGE('',*,*,#5420,.F.);
#7743=ORIENTED_EDGE('',*,*,#5423,.F.);
#7744=ORIENTED_EDGE('',*,*,#5426,.F.);
#7745=ORIENTED_EDGE('',*,*,#5429,.F.);
#7746=ORIENTED_EDGE('',*,*,#5432,.F.);
#7747=ORIENTED_EDGE('',*,*,#5435,.F.);
#7748=ORIENTED_EDGE('',*,*,#5438,.F.);
#7749=ORIENTED_EDGE('',*,*,#5441,.F.);
#7750=ORIENTED_EDGE('',*,*,#5444,.F.);
#7751=ORIENTED_EDGE('',*,*,#5447,.F.);
#7752=ORIENTED_EDGE('',*,*,#5450,.F.);
#7753=ORIENTED_EDGE('',*,*,#5453,.F.);
#7754=ORIENTED_EDGE('',*,*,#5456,.F.);
#7755=ORIENTED_EDGE('',*,*,#5459,.F.);
#7756=ORIENTED_EDGE('',*,*,#5462,.F.);
#7757=ORIENTED_EDGE('',*,*,#5465,.F.);
#7758=ORIENTED_EDGE('',*,*,#5468,.F.);
#7759=ORIENTED_EDGE('',*,*,#5471,.F.);
#7760=ORIENTED_EDGE('',*,*,#5474,.F.);
#7761=ORIENTED_EDGE('',*,*,#5482,.F.);
#7762=ORIENTED_EDGE('',*,*,#5483,.F.);
#7763=ORIENTED_EDGE('',*,*,#5295,.F.);
#7764=ORIENTED_EDGE('',*,*,#5299,.F.);
#7765=ORIENTED_EDGE('',*,*,#5302,.F.);
#7766=ORIENTED_EDGE('',*,*,#5305,.F.);
#7767=ORIENTED_EDGE('',*,*,#5308,.F.);
#7768=ORIENTED_EDGE('',*,*,#5311,.F.);
#7769=ORIENTED_EDGE('',*,*,#5314,.F.);
#7770=ORIENTED_EDGE('',*,*,#5317,.F.);
#7771=ORIENTED_EDGE('',*,*,#5320,.F.);
#7772=ORIENTED_EDGE('',*,*,#5323,.F.);
#7773=ORIENTED_EDGE('',*,*,#5326,.F.);
#7774=ORIENTED_EDGE('',*,*,#5329,.F.);
#7775=ORIENTED_EDGE('',*,*,#5332,.F.);
#7776=ORIENTED_EDGE('',*,*,#5335,.F.);
#7777=ORIENTED_EDGE('',*,*,#5338,.F.);
#7778=ORIENTED_EDGE('',*,*,#5341,.F.);
#7779=ORIENTED_EDGE('',*,*,#5344,.F.);
#7780=ORIENTED_EDGE('',*,*,#5347,.F.);
#7781=ORIENTED_EDGE('',*,*,#5350,.F.);
#7782=ORIENTED_EDGE('',*,*,#5353,.F.);
#7783=ORIENTED_EDGE('',*,*,#5356,.F.);
#7784=ORIENTED_EDGE('',*,*,#5359,.F.);
#7785=ORIENTED_EDGE('',*,*,#5362,.F.);
#7786=ORIENTED_EDGE('',*,*,#5365,.F.);
#7787=ORIENTED_EDGE('',*,*,#5368,.F.);
#7788=ORIENTED_EDGE('',*,*,#5371,.F.);
#7789=ORIENTED_EDGE('',*,*,#5374,.F.);
#7790=ORIENTED_EDGE('',*,*,#5377,.F.);
#7791=ORIENTED_EDGE('',*,*,#5380,.F.);
#7792=ORIENTED_EDGE('',*,*,#5383,.F.);
#7793=ORIENTED_EDGE('',*,*,#5484,.F.);
#7794=ORIENTED_EDGE('',*,*,#5473,.T.);
#7795=ORIENTED_EDGE('',*,*,#5485,.F.);
#7796=ORIENTED_EDGE('',*,*,#5486,.F.);
#7797=ORIENTED_EDGE('',*,*,#5482,.T.);
#7798=ORIENTED_EDGE('',*,*,#5476,.T.);
#7799=ORIENTED_EDGE('',*,*,#5479,.T.);
#7800=ORIENTED_EDGE('',*,*,#5487,.F.);
#7801=ORIENTED_EDGE('',*,*,#5384,.F.);
#7802=ORIENTED_EDGE('',*,*,#5381,.F.);
#7803=ORIENTED_EDGE('',*,*,#5378,.F.);
#7804=ORIENTED_EDGE('',*,*,#5375,.F.);
#7805=ORIENTED_EDGE('',*,*,#5372,.F.);
#7806=ORIENTED_EDGE('',*,*,#5369,.F.);
#7807=ORIENTED_EDGE('',*,*,#5366,.F.);
#7808=ORIENTED_EDGE('',*,*,#5363,.F.);
#7809=ORIENTED_EDGE('',*,*,#5360,.F.);
#7810=ORIENTED_EDGE('',*,*,#5357,.F.);
#7811=ORIENTED_EDGE('',*,*,#5354,.F.);
#7812=ORIENTED_EDGE('',*,*,#5351,.F.);
#7813=ORIENTED_EDGE('',*,*,#5348,.F.);
#7814=ORIENTED_EDGE('',*,*,#5345,.F.);
#7815=ORIENTED_EDGE('',*,*,#5342,.F.);
#7816=ORIENTED_EDGE('',*,*,#5339,.F.);
#7817=ORIENTED_EDGE('',*,*,#5336,.F.);
#7818=ORIENTED_EDGE('',*,*,#5333,.F.);
#7819=ORIENTED_EDGE('',*,*,#5330,.F.);
#7820=ORIENTED_EDGE('',*,*,#5327,.F.);
#7821=ORIENTED_EDGE('',*,*,#5324,.F.);
#7822=ORIENTED_EDGE('',*,*,#5321,.F.);
#7823=ORIENTED_EDGE('',*,*,#5318,.F.);
#7824=ORIENTED_EDGE('',*,*,#5315,.F.);
#7825=ORIENTED_EDGE('',*,*,#5312,.F.);
#7826=ORIENTED_EDGE('',*,*,#5309,.F.);
#7827=ORIENTED_EDGE('',*,*,#5306,.F.);
#7828=ORIENTED_EDGE('',*,*,#5303,.F.);
#7829=ORIENTED_EDGE('',*,*,#5300,.F.);
#7830=ORIENTED_EDGE('',*,*,#5297,.F.);
#7831=ORIENTED_EDGE('',*,*,#5488,.F.);
#7832=ORIENTED_EDGE('',*,*,#5485,.T.);
#7833=ORIENTED_EDGE('',*,*,#5475,.T.);
#7834=ORIENTED_EDGE('',*,*,#5472,.T.);
#7835=ORIENTED_EDGE('',*,*,#5469,.T.);
#7836=ORIENTED_EDGE('',*,*,#5466,.T.);
#7837=ORIENTED_EDGE('',*,*,#5463,.T.);
#7838=ORIENTED_EDGE('',*,*,#5460,.T.);
#7839=ORIENTED_EDGE('',*,*,#5457,.T.);
#7840=ORIENTED_EDGE('',*,*,#5454,.T.);
#7841=ORIENTED_EDGE('',*,*,#5451,.T.);
#7842=ORIENTED_EDGE('',*,*,#5448,.T.);
#7843=ORIENTED_EDGE('',*,*,#5445,.T.);
#7844=ORIENTED_EDGE('',*,*,#5442,.T.);
#7845=ORIENTED_EDGE('',*,*,#5439,.T.);
#7846=ORIENTED_EDGE('',*,*,#5436,.T.);
#7847=ORIENTED_EDGE('',*,*,#5433,.T.);
#7848=ORIENTED_EDGE('',*,*,#5430,.T.);
#7849=ORIENTED_EDGE('',*,*,#5427,.T.);
#7850=ORIENTED_EDGE('',*,*,#5424,.T.);
#7851=ORIENTED_EDGE('',*,*,#5421,.T.);
#7852=ORIENTED_EDGE('',*,*,#5418,.T.);
#7853=ORIENTED_EDGE('',*,*,#5415,.T.);
#7854=ORIENTED_EDGE('',*,*,#5412,.T.);
#7855=ORIENTED_EDGE('',*,*,#5409,.T.);
#7856=ORIENTED_EDGE('',*,*,#5406,.T.);
#7857=ORIENTED_EDGE('',*,*,#5403,.T.);
#7858=ORIENTED_EDGE('',*,*,#5400,.T.);
#7859=ORIENTED_EDGE('',*,*,#5397,.T.);
#7860=ORIENTED_EDGE('',*,*,#5394,.T.);
#7861=ORIENTED_EDGE('',*,*,#5391,.T.);
#7862=ORIENTED_EDGE('',*,*,#5388,.T.);
#7863=ORIENTED_EDGE('',*,*,#5382,.T.);
#7864=ORIENTED_EDGE('',*,*,#5487,.T.);
#7865=ORIENTED_EDGE('',*,*,#5478,.T.);
#7866=ORIENTED_EDGE('',*,*,#5484,.T.);
#7867=ORIENTED_EDGE('',*,*,#5489,.F.);
#7868=ORIENTED_EDGE('',*,*,#5490,.T.);
#7869=ORIENTED_EDGE('',*,*,#5491,.T.);
#7870=ORIENTED_EDGE('',*,*,#5492,.F.);
#7871=ORIENTED_EDGE('',*,*,#5493,.F.);
#7872=ORIENTED_EDGE('',*,*,#5494,.T.);
#7873=ORIENTED_EDGE('',*,*,#5495,.T.);
#7874=ORIENTED_EDGE('',*,*,#5490,.F.);
#7875=ORIENTED_EDGE('',*,*,#5496,.F.);
#7876=ORIENTED_EDGE('',*,*,#5497,.T.);
#7877=ORIENTED_EDGE('',*,*,#5498,.T.);
#7878=ORIENTED_EDGE('',*,*,#5494,.F.);
#7879=ORIENTED_EDGE('',*,*,#5499,.F.);
#7880=ORIENTED_EDGE('',*,*,#5500,.T.);
#7881=ORIENTED_EDGE('',*,*,#5501,.T.);
#7882=ORIENTED_EDGE('',*,*,#5497,.F.);
#7883=ORIENTED_EDGE('',*,*,#5502,.F.);
#7884=ORIENTED_EDGE('',*,*,#5503,.T.);
#7885=ORIENTED_EDGE('',*,*,#5504,.T.);
#7886=ORIENTED_EDGE('',*,*,#5500,.F.);
#7887=ORIENTED_EDGE('',*,*,#5505,.F.);
#7888=ORIENTED_EDGE('',*,*,#5492,.T.);
#7889=ORIENTED_EDGE('',*,*,#5506,.T.);
#7890=ORIENTED_EDGE('',*,*,#5503,.F.);
#7891=ORIENTED_EDGE('',*,*,#5506,.F.);
#7892=ORIENTED_EDGE('',*,*,#5491,.F.);
#7893=ORIENTED_EDGE('',*,*,#5495,.F.);
#7894=ORIENTED_EDGE('',*,*,#5498,.F.);
#7895=ORIENTED_EDGE('',*,*,#5501,.F.);
#7896=ORIENTED_EDGE('',*,*,#5504,.F.);
#7897=ORIENTED_EDGE('',*,*,#5507,.T.);
#7898=ORIENTED_EDGE('',*,*,#5483,.T.);
#7899=ORIENTED_EDGE('',*,*,#5486,.T.);
#7900=ORIENTED_EDGE('',*,*,#5488,.T.);
#7901=ORIENTED_EDGE('',*,*,#5296,.F.);
#7902=ORIENTED_EDGE('',*,*,#5507,.F.);
#7903=ORIENTED_EDGE('',*,*,#5508,.T.);
#7904=ORIENTED_EDGE('',*,*,#5509,.T.);
#7905=ORIENTED_EDGE('',*,*,#5508,.F.);
#7906=ORIENTED_EDGE('',*,*,#5509,.F.);
#7907=ORIENTED_EDGE('',*,*,#5489,.T.);
#7908=ORIENTED_EDGE('',*,*,#5505,.T.);
#7909=ORIENTED_EDGE('',*,*,#5502,.T.);
#7910=ORIENTED_EDGE('',*,*,#5499,.T.);
#7911=ORIENTED_EDGE('',*,*,#5496,.T.);
#7912=ORIENTED_EDGE('',*,*,#5493,.T.);
#7913=ORIENTED_EDGE('',*,*,#5481,.T.);
#8231=CYLINDRICAL_SURFACE('',#9315,0.14635);
#8232=CYLINDRICAL_SURFACE('',#9317,0.14635);
#8233=CYLINDRICAL_SURFACE('',#9318,0.14635);
#8234=CYLINDRICAL_SURFACE('',#9319,0.14635);
#8235=CYLINDRICAL_SURFACE('',#9320,0.14635);
#8236=CYLINDRICAL_SURFACE('',#9321,0.14635);
#8237=CYLINDRICAL_SURFACE('',#9322,0.14635);
#8238=CYLINDRICAL_SURFACE('',#9323,0.14635);
#8239=CYLINDRICAL_SURFACE('',#9324,0.14635);
#8240=CYLINDRICAL_SURFACE('',#9325,0.14635);
#8241=CYLINDRICAL_SURFACE('',#9326,0.14635);
#8242=CYLINDRICAL_SURFACE('',#9327,0.14635);
#8243=CYLINDRICAL_SURFACE('',#9328,0.14635);
#8244=CYLINDRICAL_SURFACE('',#9329,0.14635);
#8245=CYLINDRICAL_SURFACE('',#9330,0.14635);
#8246=CYLINDRICAL_SURFACE('',#9331,0.14635);
#8247=CYLINDRICAL_SURFACE('',#9332,0.14635);
#8248=CYLINDRICAL_SURFACE('',#9333,0.14635);
#8249=CYLINDRICAL_SURFACE('',#9334,0.14635);
#8250=CYLINDRICAL_SURFACE('',#9335,0.14635);
#8251=CYLINDRICAL_SURFACE('',#9336,0.14635);
#8252=CYLINDRICAL_SURFACE('',#9337,0.14635);
#8253=CYLINDRICAL_SURFACE('',#9338,0.14635);
#8254=CYLINDRICAL_SURFACE('',#9339,0.14635);
#8255=CYLINDRICAL_SURFACE('',#9340,0.14635);
#8256=CYLINDRICAL_SURFACE('',#9341,0.14635);
#8257=CYLINDRICAL_SURFACE('',#9342,0.14635);
#8258=CYLINDRICAL_SURFACE('',#9343,0.14635);
#8259=CYLINDRICAL_SURFACE('',#9344,0.14635);
#8260=CYLINDRICAL_SURFACE('',#9345,0.14635);
#8261=CYLINDRICAL_SURFACE('',#9346,0.117775);
#8262=CYLINDRICAL_SURFACE('',#9348,0.117775);
#8263=CYLINDRICAL_SURFACE('',#9349,0.117775);
#8264=CYLINDRICAL_SURFACE('',#9350,0.117775);
#8265=CYLINDRICAL_SURFACE('',#9351,0.117775);
#8266=CYLINDRICAL_SURFACE('',#9352,0.117775);
#8267=CYLINDRICAL_SURFACE('',#9353,0.117775);
#8268=CYLINDRICAL_SURFACE('',#9354,0.117775);
#8269=CYLINDRICAL_SURFACE('',#9355,0.117775);
#8270=CYLINDRICAL_SURFACE('',#9356,0.117775);
#8271=CYLINDRICAL_SURFACE('',#9357,0.117775);
#8272=CYLINDRICAL_SURFACE('',#9358,0.117775);
#8273=CYLINDRICAL_SURFACE('',#9359,0.117775);
#8274=CYLINDRICAL_SURFACE('',#9360,0.117775);
#8275=CYLINDRICAL_SURFACE('',#9361,0.117775);
#8276=CYLINDRICAL_SURFACE('',#9362,0.117775);
#8277=CYLINDRICAL_SURFACE('',#9363,0.117775);
#8278=CYLINDRICAL_SURFACE('',#9364,0.117775);
#8279=CYLINDRICAL_SURFACE('',#9365,0.117775);
#8280=CYLINDRICAL_SURFACE('',#9366,0.117775);
#8281=CYLINDRICAL_SURFACE('',#9367,0.117775);
#8282=CYLINDRICAL_SURFACE('',#9368,0.117775);
#8283=CYLINDRICAL_SURFACE('',#9369,0.117775);
#8284=CYLINDRICAL_SURFACE('',#9370,0.117775);
#8285=CYLINDRICAL_SURFACE('',#9371,0.117775);
#8286=CYLINDRICAL_SURFACE('',#9372,0.117775);
#8287=CYLINDRICAL_SURFACE('',#9373,0.117775);
#8288=CYLINDRICAL_SURFACE('',#9374,0.117775);
#8289=CYLINDRICAL_SURFACE('',#9375,0.117775);
#8290=CYLINDRICAL_SURFACE('',#9376,0.117775);
#8291=CYLINDRICAL_SURFACE('',#9380,0.117775);
#8292=CYLINDRICAL_SURFACE('',#9382,0.14635);
#8293=CYLINDRICAL_SURFACE('',#9392,0.275);
#8665=ADVANCED_FACE('',(#1248),#8231,.T.);
#8666=ADVANCED_FACE('',(#1249),#8232,.T.);
#8667=ADVANCED_FACE('',(#1250),#8233,.T.);
#8668=ADVANCED_FACE('',(#1251),#8234,.T.);
#8669=ADVANCED_FACE('',(#1252),#8235,.T.);
#8670=ADVANCED_FACE('',(#1253),#8236,.T.);
#8671=ADVANCED_FACE('',(#1254),#8237,.T.);
#8672=ADVANCED_FACE('',(#1255),#8238,.T.);
#8673=ADVANCED_FACE('',(#1256),#8239,.T.);
#8674=ADVANCED_FACE('',(#1257),#8240,.T.);
#8675=ADVANCED_FACE('',(#1258),#8241,.T.);
#8676=ADVANCED_FACE('',(#1259),#8242,.T.);
#8677=ADVANCED_FACE('',(#1260),#8243,.T.);
#8678=ADVANCED_FACE('',(#1261),#8244,.T.);
#8679=ADVANCED_FACE('',(#1262),#8245,.T.);
#8680=ADVANCED_FACE('',(#1263),#8246,.T.);
#8681=ADVANCED_FACE('',(#1264),#8247,.T.);
#8682=ADVANCED_FACE('',(#1265),#8248,.T.);
#8683=ADVANCED_FACE('',(#1266),#8249,.T.);
#8684=ADVANCED_FACE('',(#1267),#8250,.T.);
#8685=ADVANCED_FACE('',(#1268),#8251,.T.);
#8686=ADVANCED_FACE('',(#1269),#8252,.T.);
#8687=ADVANCED_FACE('',(#1270),#8253,.T.);
#8688=ADVANCED_FACE('',(#1271),#8254,.T.);
#8689=ADVANCED_FACE('',(#1272),#8255,.T.);
#8690=ADVANCED_FACE('',(#1273),#8256,.T.);
#8691=ADVANCED_FACE('',(#1274),#8257,.T.);
#8692=ADVANCED_FACE('',(#1275),#8258,.T.);
#8693=ADVANCED_FACE('',(#1276),#8259,.T.);
#8694=ADVANCED_FACE('',(#1277),#8260,.T.);
#8695=ADVANCED_FACE('',(#1278),#8261,.T.);
#8696=ADVANCED_FACE('',(#1279),#8262,.T.);
#8697=ADVANCED_FACE('',(#1280),#8263,.T.);
#8698=ADVANCED_FACE('',(#1281),#8264,.T.);
#8699=ADVANCED_FACE('',(#1282),#8265,.T.);
#8700=ADVANCED_FACE('',(#1283),#8266,.T.);
#8701=ADVANCED_FACE('',(#1284),#8267,.T.);
#8702=ADVANCED_FACE('',(#1285),#8268,.T.);
#8703=ADVANCED_FACE('',(#1286),#8269,.T.);
#8704=ADVANCED_FACE('',(#1287),#8270,.T.);
#8705=ADVANCED_FACE('',(#1288),#8271,.T.);
#8706=ADVANCED_FACE('',(#1289),#8272,.T.);
#8707=ADVANCED_FACE('',(#1290),#8273,.T.);
#8708=ADVANCED_FACE('',(#1291),#8274,.T.);
#8709=ADVANCED_FACE('',(#1292),#8275,.T.);
#8710=ADVANCED_FACE('',(#1293),#8276,.T.);
#8711=ADVANCED_FACE('',(#1294),#8277,.T.);
#8712=ADVANCED_FACE('',(#1295),#8278,.T.);
#8713=ADVANCED_FACE('',(#1296),#8279,.T.);
#8714=ADVANCED_FACE('',(#1297),#8280,.T.);
#8715=ADVANCED_FACE('',(#1298),#8281,.T.);
#8716=ADVANCED_FACE('',(#1299),#8282,.T.);
#8717=ADVANCED_FACE('',(#1300),#8283,.T.);
#8718=ADVANCED_FACE('',(#1301),#8284,.T.);
#8719=ADVANCED_FACE('',(#1302),#8285,.T.);
#8720=ADVANCED_FACE('',(#1303),#8286,.T.);
#8721=ADVANCED_FACE('',(#1304),#8287,.T.);
#8722=ADVANCED_FACE('',(#1305),#8288,.T.);
#8723=ADVANCED_FACE('',(#1306),#8289,.T.);
#8724=ADVANCED_FACE('',(#1307),#8290,.T.);
#8725=ADVANCED_FACE('',(#1308),#75,.T.);
#8726=ADVANCED_FACE('',(#1309),#156,.F.);
#8727=ADVANCED_FACE('',(#1310),#8291,.T.);
#8728=ADVANCED_FACE('',(#1311),#157,.F.);
#8729=ADVANCED_FACE('',(#1312),#8292,.T.);
#8730=ADVANCED_FACE('',(#1313),#871,.F.);
#8731=ADVANCED_FACE('',(#1314),#872,.F.);
#8732=ADVANCED_FACE('',(#1315),#873,.F.);
#8733=ADVANCED_FACE('',(#1316),#874,.F.);
#8734=ADVANCED_FACE('',(#1317),#875,.F.);
#8735=ADVANCED_FACE('',(#1318),#876,.F.);
#8736=ADVANCED_FACE('',(#1319),#877,.F.);
#8737=ADVANCED_FACE('',(#1320,#633),#878,.T.);
#8738=ADVANCED_FACE('',(#1321),#8293,.T.);
#8739=ADVANCED_FACE('',(#1322,#634),#879,.F.);
#8740=ADVANCED_FACE('',(#1323),#880,.T.);
#8808=CLOSED_SHELL('',(#8665,#8666,#8667,#8668,#8669,#8670,#8671,#8672,
#8673,#8674,#8675,#8676,#8677,#8678,#8679,#8680,#8681,#8682,#8683,#8684,
#8685,#8686,#8687,#8688,#8689,#8690,#8691,#8692,#8693,#8694,#8695,#8696,
#8697,#8698,#8699,#8700,#8701,#8702,#8703,#8704,#8705,#8706,#8707,#8708,
#8709,#8710,#8711,#8712,#8713,#8714,#8715,#8716,#8717,#8718,#8719,#8720,
#8721,#8722,#8723,#8724,#8725,#8726,#8727,#8728,#8729,#8730,#8731,#8732,
#8733,#8734,#8735,#8736,#8737,#8738,#8739,#8740));
#9314=AXIS2_PLACEMENT_3D('',#16410,#10908,#10909);
#9315=AXIS2_PLACEMENT_3D('',#16411,#10910,#10911);
#9316=AXIS2_PLACEMENT_3D('',#16427,#10913,#10914);
#9317=AXIS2_PLACEMENT_3D('',#16435,#10915,#10916);
#9318=AXIS2_PLACEMENT_3D('',#16483,#10918,#10919);
#9319=AXIS2_PLACEMENT_3D('',#16531,#10921,#10922);
#9320=AXIS2_PLACEMENT_3D('',#16582,#10924,#10925);
#9321=AXIS2_PLACEMENT_3D('',#16630,#10927,#10928);
#9322=AXIS2_PLACEMENT_3D('',#16678,#10930,#10931);
#9323=AXIS2_PLACEMENT_3D('',#16726,#10933,#10934);
#9324=AXIS2_PLACEMENT_3D('',#16780,#10936,#10937);
#9325=AXIS2_PLACEMENT_3D('',#16828,#10939,#10940);
#9326=AXIS2_PLACEMENT_3D('',#16876,#10942,#10943);
#9327=AXIS2_PLACEMENT_3D('',#16930,#10945,#10946);
#9328=AXIS2_PLACEMENT_3D('',#16978,#10948,#10949);
#9329=AXIS2_PLACEMENT_3D('',#17026,#10951,#10952);
#9330=AXIS2_PLACEMENT_3D('',#17074,#10954,#10955);
#9331=AXIS2_PLACEMENT_3D('',#17128,#10957,#10958);
#9332=AXIS2_PLACEMENT_3D('',#17176,#10960,#10961);
#9333=AXIS2_PLACEMENT_3D('',#17224,#10963,#10964);
#9334=AXIS2_PLACEMENT_3D('',#17278,#10966,#10967);
#9335=AXIS2_PLACEMENT_3D('',#17326,#10969,#10970);
#9336=AXIS2_PLACEMENT_3D('',#17374,#10972,#10973);
#9337=AXIS2_PLACEMENT_3D('',#17428,#10975,#10976);
#9338=AXIS2_PLACEMENT_3D('',#17476,#10978,#10979);
#9339=AXIS2_PLACEMENT_3D('',#17524,#10981,#10982);
#9340=AXIS2_PLACEMENT_3D('',#17572,#10984,#10985);
#9341=AXIS2_PLACEMENT_3D('',#17626,#10987,#10988);
#9342=AXIS2_PLACEMENT_3D('',#17674,#10990,#10991);
#9343=AXIS2_PLACEMENT_3D('',#17722,#10993,#10994);
#9344=AXIS2_PLACEMENT_3D('',#17776,#10996,#10997);
#9345=AXIS2_PLACEMENT_3D('',#17824,#10999,#11000);
#9346=AXIS2_PLACEMENT_3D('',#17872,#11002,#11003);
#9347=AXIS2_PLACEMENT_3D('',#17888,#11005,#11006);
#9348=AXIS2_PLACEMENT_3D('',#17898,#11007,#11008);
#9349=AXIS2_PLACEMENT_3D('',#17922,#11010,#11011);
#9350=AXIS2_PLACEMENT_3D('',#17946,#11013,#11014);
#9351=AXIS2_PLACEMENT_3D('',#17971,#11016,#11017);
#9352=AXIS2_PLACEMENT_3D('',#17996,#11019,#11020);
#9353=AXIS2_PLACEMENT_3D('',#18020,#11022,#11023);
#9354=AXIS2_PLACEMENT_3D('',#18045,#11025,#11026);
#9355=AXIS2_PLACEMENT_3D('',#18070,#11028,#11029);
#9356=AXIS2_PLACEMENT_3D('',#18094,#11031,#11032);
#9357=AXIS2_PLACEMENT_3D('',#18118,#11034,#11035);
#9358=AXIS2_PLACEMENT_3D('',#18143,#11037,#11038);
#9359=AXIS2_PLACEMENT_3D('',#18168,#11040,#11041);
#9360=AXIS2_PLACEMENT_3D('',#18192,#11043,#11044);
#9361=AXIS2_PLACEMENT_3D('',#18217,#11046,#11047);
#9362=AXIS2_PLACEMENT_3D('',#18242,#11049,#11050);
#9363=AXIS2_PLACEMENT_3D('',#18266,#11052,#11053);
#9364=AXIS2_PLACEMENT_3D('',#18291,#11055,#11056);
#9365=AXIS2_PLACEMENT_3D('',#18316,#11058,#11059);
#9366=AXIS2_PLACEMENT_3D('',#18340,#11061,#11062);
#9367=AXIS2_PLACEMENT_3D('',#18364,#11064,#11065);
#9368=AXIS2_PLACEMENT_3D('',#18389,#11067,#11068);
#9369=AXIS2_PLACEMENT_3D('',#18414,#11070,#11071);
#9370=AXIS2_PLACEMENT_3D('',#18438,#11073,#11074);
#9371=AXIS2_PLACEMENT_3D('',#18463,#11076,#11077);
#9372=AXIS2_PLACEMENT_3D('',#18488,#11079,#11080);
#9373=AXIS2_PLACEMENT_3D('',#18512,#11082,#11083);
#9374=AXIS2_PLACEMENT_3D('',#18537,#11085,#11086);
#9375=AXIS2_PLACEMENT_3D('',#18561,#11088,#11089);
#9376=AXIS2_PLACEMENT_3D('',#18586,#11091,#11092);
#9377=AXIS2_PLACEMENT_3D('',#18610,#11094,#11095);
#9378=AXIS2_PLACEMENT_3D('',#18772,#11096,#11097);
#9379=AXIS2_PLACEMENT_3D('',#18791,#11099,#11100);
#9380=AXIS2_PLACEMENT_3D('',#19653,#11101,#11102);
#9381=AXIS2_PLACEMENT_3D('',#19664,#11103,#11104);
#9382=AXIS2_PLACEMENT_3D('',#20531,#11105,#11106);
#9383=AXIS2_PLACEMENT_3D('',#20532,#11107,#11108);
#9384=AXIS2_PLACEMENT_3D('',#20541,#11113,#11114);
#9385=AXIS2_PLACEMENT_3D('',#20547,#11118,#11119);
#9386=AXIS2_PLACEMENT_3D('',#20553,#11123,#11124);
#9387=AXIS2_PLACEMENT_3D('',#20559,#11128,#11129);
#9388=AXIS2_PLACEMENT_3D('',#20565,#11133,#11134);
#9389=AXIS2_PLACEMENT_3D('',#20568,#11137,#11138);
#9390=AXIS2_PLACEMENT_3D('',#20569,#11139,#11140);
#9391=AXIS2_PLACEMENT_3D('',#20571,#11141,#11142);
#9392=AXIS2_PLACEMENT_3D('',#20572,#11143,#11144);
#9393=AXIS2_PLACEMENT_3D('',#20575,#11146,#11147);
#9394=AXIS2_PLACEMENT_3D('',#20576,#11148,#11149);
#9395=AXIS2_PLACEMENT_3D('',#20577,#11150,#11151);
#10908=DIRECTION('axis',(0.,0.,1.));
#10909=DIRECTION('refdir',(1.,0.,0.));
#10910=DIRECTION('center_axis',(0.,0.,1.));
#10911=DIRECTION('ref_axis',(1.,0.,0.));
#10912=DIRECTION('',(0.,0.,-1.));
#10913=DIRECTION('center_axis',(0.,0.,-1.));
#10914=DIRECTION('ref_axis',(1.,0.,0.));
#10915=DIRECTION('center_axis',(0.,0.,1.));
#10916=DIRECTION('ref_axis',(1.,0.,0.));
#10917=DIRECTION('',(0.,0.,-1.));
#10918=DIRECTION('center_axis',(0.,0.,1.));
#10919=DIRECTION('ref_axis',(1.,0.,0.));
#10920=DIRECTION('',(0.,0.,-1.));
#10921=DIRECTION('center_axis',(0.,0.,1.));
#10922=DIRECTION('ref_axis',(1.,0.,0.));
#10923=DIRECTION('',(0.,0.,-1.));
#10924=DIRECTION('center_axis',(0.,0.,1.));
#10925=DIRECTION('ref_axis',(1.,0.,0.));
#10926=DIRECTION('',(0.,0.,-1.));
#10927=DIRECTION('center_axis',(0.,0.,1.));
#10928=DIRECTION('ref_axis',(1.,0.,0.));
#10929=DIRECTION('',(0.,0.,-1.));
#10930=DIRECTION('center_axis',(0.,0.,1.));
#10931=DIRECTION('ref_axis',(1.,0.,0.));
#10932=DIRECTION('',(0.,0.,-1.));
#10933=DIRECTION('center_axis',(0.,0.,1.));
#10934=DIRECTION('ref_axis',(1.,0.,0.));
#10935=DIRECTION('',(0.,0.,-1.));
#10936=DIRECTION('center_axis',(0.,0.,1.));
#10937=DIRECTION('ref_axis',(1.,0.,0.));
#10938=DIRECTION('',(0.,0.,-1.));
#10939=DIRECTION('center_axis',(0.,0.,1.));
#10940=DIRECTION('ref_axis',(1.,0.,0.));
#10941=DIRECTION('',(0.,0.,-1.));
#10942=DIRECTION('center_axis',(0.,0.,1.));
#10943=DIRECTION('ref_axis',(1.,0.,0.));
#10944=DIRECTION('',(0.,0.,-1.));
#10945=DIRECTION('center_axis',(0.,0.,1.));
#10946=DIRECTION('ref_axis',(1.,0.,0.));
#10947=DIRECTION('',(0.,0.,-1.));
#10948=DIRECTION('center_axis',(0.,0.,1.));
#10949=DIRECTION('ref_axis',(1.,0.,0.));
#10950=DIRECTION('',(0.,0.,-1.));
#10951=DIRECTION('center_axis',(0.,0.,1.));
#10952=DIRECTION('ref_axis',(1.,0.,0.));
#10953=DIRECTION('',(0.,0.,-1.));
#10954=DIRECTION('center_axis',(0.,0.,1.));
#10955=DIRECTION('ref_axis',(1.,0.,0.));
#10956=DIRECTION('',(0.,0.,-1.));
#10957=DIRECTION('center_axis',(0.,0.,1.));
#10958=DIRECTION('ref_axis',(1.,0.,0.));
#10959=DIRECTION('',(0.,0.,-1.));
#10960=DIRECTION('center_axis',(0.,0.,1.));
#10961=DIRECTION('ref_axis',(1.,0.,0.));
#10962=DIRECTION('',(0.,0.,-1.));
#10963=DIRECTION('center_axis',(0.,0.,1.));
#10964=DIRECTION('ref_axis',(1.,0.,0.));
#10965=DIRECTION('',(0.,0.,-1.));
#10966=DIRECTION('center_axis',(0.,0.,1.));
#10967=DIRECTION('ref_axis',(1.,0.,0.));
#10968=DIRECTION('',(0.,0.,-1.));
#10969=DIRECTION('center_axis',(0.,0.,1.));
#10970=DIRECTION('ref_axis',(1.,0.,0.));
#10971=DIRECTION('',(0.,0.,-1.));
#10972=DIRECTION('center_axis',(0.,0.,1.));
#10973=DIRECTION('ref_axis',(1.,0.,0.));
#10974=DIRECTION('',(0.,0.,-1.));
#10975=DIRECTION('center_axis',(0.,0.,1.));
#10976=DIRECTION('ref_axis',(1.,0.,0.));
#10977=DIRECTION('',(0.,0.,-1.));
#10978=DIRECTION('center_axis',(0.,0.,1.));
#10979=DIRECTION('ref_axis',(1.,0.,0.));
#10980=DIRECTION('',(0.,0.,-1.));
#10981=DIRECTION('center_axis',(0.,0.,1.));
#10982=DIRECTION('ref_axis',(1.,0.,0.));
#10983=DIRECTION('',(0.,0.,-1.));
#10984=DIRECTION('center_axis',(0.,0.,1.));
#10985=DIRECTION('ref_axis',(1.,0.,0.));
#10986=DIRECTION('',(0.,0.,-1.));
#10987=DIRECTION('center_axis',(0.,0.,1.));
#10988=DIRECTION('ref_axis',(1.,0.,0.));
#10989=DIRECTION('',(0.,0.,-1.));
#10990=DIRECTION('center_axis',(0.,0.,1.));
#10991=DIRECTION('ref_axis',(1.,0.,0.));
#10992=DIRECTION('',(0.,0.,-1.));
#10993=DIRECTION('center_axis',(0.,0.,1.));
#10994=DIRECTION('ref_axis',(1.,0.,0.));
#10995=DIRECTION('',(0.,0.,-1.));
#10996=DIRECTION('center_axis',(0.,0.,1.));
#10997=DIRECTION('ref_axis',(1.,0.,0.));
#10998=DIRECTION('',(0.,0.,-1.));
#10999=DIRECTION('center_axis',(0.,0.,1.));
#11000=DIRECTION('ref_axis',(1.,0.,0.));
#11001=DIRECTION('',(0.,0.,-1.));
#11002=DIRECTION('center_axis',(0.,0.,1.));
#11003=DIRECTION('ref_axis',(1.,-2.42503376499884E-13,0.));
#11004=DIRECTION('',(0.,0.,1.));
#11005=DIRECTION('center_axis',(0.,0.,-1.));
#11006=DIRECTION('ref_axis',(1.,-2.42503376499884E-13,0.));
#11007=DIRECTION('center_axis',(0.,0.,1.));
#11008=DIRECTION('ref_axis',(1.,-2.42503376499884E-13,0.));
#11009=DIRECTION('',(0.,0.,1.));
#11010=DIRECTION('center_axis',(0.,0.,1.));
#11011=DIRECTION('ref_axis',(1.,-2.42503376499884E-13,0.));
#11012=DIRECTION('',(0.,0.,1.));
#11013=DIRECTION('center_axis',(0.,0.,1.));
#11014=DIRECTION('ref_axis',(1.,-2.42503376499884E-13,0.));
#11015=DIRECTION('',(0.,0.,1.));
#11016=DIRECTION('center_axis',(0.,0.,1.));
#11017=DIRECTION('ref_axis',(1.,-2.42503376499884E-13,0.));
#11018=DIRECTION('',(0.,0.,1.));
#11019=DIRECTION('center_axis',(0.,0.,1.));
#11020=DIRECTION('ref_axis',(1.,-2.42503376499884E-13,0.));
#11021=DIRECTION('',(0.,0.,1.));
#11022=DIRECTION('center_axis',(0.,0.,1.));
#11023=DIRECTION('ref_axis',(1.,-2.42503376499884E-13,0.));
#11024=DIRECTION('',(0.,0.,1.));
#11025=DIRECTION('center_axis',(0.,0.,1.));
#11026=DIRECTION('ref_axis',(1.,-2.42503376499884E-13,0.));
#11027=DIRECTION('',(0.,0.,1.));
#11028=DIRECTION('center_axis',(0.,0.,1.));
#11029=DIRECTION('ref_axis',(1.,-2.42503376499884E-13,0.));
#11030=DIRECTION('',(0.,0.,1.));
#11031=DIRECTION('center_axis',(0.,0.,1.));
#11032=DIRECTION('ref_axis',(1.,-2.42503376499884E-13,0.));
#11033=DIRECTION('',(0.,0.,1.));
#11034=DIRECTION('center_axis',(0.,0.,1.));
#11035=DIRECTION('ref_axis',(1.,-2.42503376499884E-13,0.));
#11036=DIRECTION('',(0.,0.,1.));
#11037=DIRECTION('center_axis',(0.,0.,1.));
#11038=DIRECTION('ref_axis',(1.,-2.42503376499884E-13,0.));
#11039=DIRECTION('',(0.,0.,1.));
#11040=DIRECTION('center_axis',(0.,0.,1.));
#11041=DIRECTION('ref_axis',(1.,-2.42503376499884E-13,0.));
#11042=DIRECTION('',(0.,0.,1.));
#11043=DIRECTION('center_axis',(0.,0.,1.));
#11044=DIRECTION('ref_axis',(1.,-2.42503376499884E-13,0.));
#11045=DIRECTION('',(0.,0.,1.));
#11046=DIRECTION('center_axis',(0.,0.,1.));
#11047=DIRECTION('ref_axis',(1.,-2.42503376499884E-13,0.));
#11048=DIRECTION('',(0.,0.,1.));
#11049=DIRECTION('center_axis',(0.,0.,1.));
#11050=DIRECTION('ref_axis',(1.,-2.42503376499884E-13,0.));
#11051=DIRECTION('',(0.,0.,1.));
#11052=DIRECTION('center_axis',(0.,0.,1.));
#11053=DIRECTION('ref_axis',(1.,-2.42503376499884E-13,0.));
#11054=DIRECTION('',(0.,0.,1.));
#11055=DIRECTION('center_axis',(0.,0.,1.));
#11056=DIRECTION('ref_axis',(1.,-2.42503376499884E-13,0.));
#11057=DIRECTION('',(0.,0.,1.));
#11058=DIRECTION('center_axis',(0.,0.,1.));
#11059=DIRECTION('ref_axis',(1.,-2.42503376499884E-13,0.));
#11060=DIRECTION('',(0.,0.,1.));
#11061=DIRECTION('center_axis',(0.,0.,1.));
#11062=DIRECTION('ref_axis',(1.,-2.42503376499884E-13,0.));
#11063=DIRECTION('',(0.,0.,1.));
#11064=DIRECTION('center_axis',(0.,0.,1.));
#11065=DIRECTION('ref_axis',(1.,-2.42503376499884E-13,0.));
#11066=DIRECTION('',(0.,0.,1.));
#11067=DIRECTION('center_axis',(0.,0.,1.));
#11068=DIRECTION('ref_axis',(1.,-2.42503376499884E-13,0.));
#11069=DIRECTION('',(0.,0.,1.));
#11070=DIRECTION('center_axis',(0.,0.,1.));
#11071=DIRECTION('ref_axis',(1.,-2.42503376499884E-13,0.));
#11072=DIRECTION('',(0.,0.,1.));
#11073=DIRECTION('center_axis',(0.,0.,1.));
#11074=DIRECTION('ref_axis',(1.,-2.42503376499884E-13,0.));
#11075=DIRECTION('',(0.,0.,1.));
#11076=DIRECTION('center_axis',(0.,0.,1.));
#11077=DIRECTION('ref_axis',(1.,-2.42503376499884E-13,0.));
#11078=DIRECTION('',(0.,0.,1.));
#11079=DIRECTION('center_axis',(0.,0.,1.));
#11080=DIRECTION('ref_axis',(1.,-2.42503376499884E-13,0.));
#11081=DIRECTION('',(0.,0.,1.));
#11082=DIRECTION('center_axis',(0.,0.,1.));
#11083=DIRECTION('ref_axis',(1.,-2.42503376499884E-13,0.));
#11084=DIRECTION('',(0.,0.,1.));
#11085=DIRECTION('center_axis',(0.,0.,1.));
#11086=DIRECTION('ref_axis',(1.,-2.42503376499884E-13,0.));
#11087=DIRECTION('',(0.,0.,1.));
#11088=DIRECTION('center_axis',(0.,0.,1.));
#11089=DIRECTION('ref_axis',(1.,-2.42503376499884E-13,0.));
#11090=DIRECTION('',(0.,0.,1.));
#11091=DIRECTION('center_axis',(0.,0.,1.));
#11092=DIRECTION('ref_axis',(1.,-2.42503376499884E-13,0.));
#11093=DIRECTION('',(0.,0.,1.));
#11094=DIRECTION('center_axis',(0.,0.,-1.));
#11095=DIRECTION('ref_axis',(1.,0.,0.));
#11096=DIRECTION('center_axis',(0.,0.,-1.));
#11097=DIRECTION('ref_axis',(1.,0.,0.));
#11098=DIRECTION('',(0.707106781186547,8.65956056235493E-17,0.707106781186548));
#11099=DIRECTION('center_axis',(0.,0.,1.));
#11100=DIRECTION('ref_axis',(1.,0.,0.));
#11101=DIRECTION('center_axis',(0.,0.,1.));
#11102=DIRECTION('ref_axis',(1.,-2.42503376499884E-13,0.));
#11103=DIRECTION('center_axis',(0.,0.,-1.));
#11104=DIRECTION('ref_axis',(1.,-2.42503376499884E-13,0.));
#11105=DIRECTION('center_axis',(0.,0.,1.));
#11106=DIRECTION('ref_axis',(1.,0.,0.));
#11107=DIRECTION('center_axis',(-1.92296268638356E-16,-1.,0.));
#11108=DIRECTION('ref_axis',(1.,-1.92296268638356E-16,0.));
#11109=DIRECTION('',(1.,-1.92296268638356E-16,0.));
#11110=DIRECTION('',(0.,0.,1.));
#11111=DIRECTION('',(1.,-1.92296268638356E-16,0.));
#11112=DIRECTION('',(0.,0.,1.));
#11113=DIRECTION('center_axis',(-0.866025403784439,-0.5,0.));
#11114=DIRECTION('ref_axis',(0.5,-0.866025403784439,0.));
#11115=DIRECTION('',(0.5,-0.866025403784439,0.));
#11116=DIRECTION('',(0.,0.,1.));
#11117=DIRECTION('',(0.5,-0.866025403784439,0.));
#11118=DIRECTION('center_axis',(-0.866025403784439,0.5,0.));
#11119=DIRECTION('ref_axis',(-0.5,-0.866025403784439,0.));
#11120=DIRECTION('',(-0.5,-0.866025403784439,0.));
#11121=DIRECTION('',(0.,0.,1.));
#11122=DIRECTION('',(-0.5,-0.866025403784438,0.));
#11123=DIRECTION('center_axis',(1.92296268638356E-16,1.,0.));
#11124=DIRECTION('ref_axis',(-1.,1.92296268638356E-16,0.));
#11125=DIRECTION('',(-1.,1.92296268638356E-16,0.));
#11126=DIRECTION('',(0.,0.,1.));
#11127=DIRECTION('',(-1.,1.92296268638356E-16,0.));
#11128=DIRECTION('center_axis',(0.866025403784439,0.5,0.));
#11129=DIRECTION('ref_axis',(-0.5,0.866025403784439,0.));
#11130=DIRECTION('',(-0.5,0.866025403784439,0.));
#11131=DIRECTION('',(0.,0.,1.));
#11132=DIRECTION('',(-0.5,0.866025403784439,0.));
#11133=DIRECTION('center_axis',(0.866025403784439,-0.5,0.));
#11134=DIRECTION('ref_axis',(0.5,0.866025403784439,0.));
#11135=DIRECTION('',(0.5,0.866025403784439,0.));
#11136=DIRECTION('',(0.5,0.866025403784439,0.));
#11137=DIRECTION('center_axis',(0.,0.,1.));
#11138=DIRECTION('ref_axis',(1.,0.,0.));
#11139=DIRECTION('center_axis',(0.,0.,1.));
#11140=DIRECTION('ref_axis',(1.,0.,0.));
#11141=DIRECTION('center_axis',(0.,0.,1.));
#11142=DIRECTION('ref_axis',(1.,0.,0.));
#11143=DIRECTION('center_axis',(0.,0.,1.));
#11144=DIRECTION('ref_axis',(1.,0.,0.));
#11145=DIRECTION('',(0.,0.,-1.));
#11146=DIRECTION('center_axis',(0.,0.,1.));
#11147=DIRECTION('ref_axis',(1.,0.,0.));
#11148=DIRECTION('center_axis',(0.,0.,1.));
#11149=DIRECTION('ref_axis',(1.,0.,0.));
#11150=DIRECTION('center_axis',(0.,0.,1.));
#11151=DIRECTION('ref_axis',(1.,0.,0.));
#16410=CARTESIAN_POINT('',(0.,0.,0.));
#16411=CARTESIAN_POINT('Origin',(0.,0.,0.));
#16412=CARTESIAN_POINT('',(-0.14652705620645,9.44412402177196E-5,0.0160655045842905));
#16413=CARTESIAN_POINT('',(-0.146479946776166,0.000162062070299865,0.00893449541571059));
#16414=CARTESIAN_POINT('',(-0.14635,-1.79227059055215E-17,0.));
#16415=CARTESIAN_POINT('',(0.0634007094575209,0.131904027763685,0.));
#16416=CARTESIAN_POINT('Ctrl Pts',(-0.14652705620645,9.44412402177196E-5,
0.0160655045842905));
#16417=CARTESIAN_POINT('Ctrl Pts',(-0.146560923555419,0.00502618404349199,
0.0157963945919035));
#16418=CARTESIAN_POINT('Ctrl Pts',(-0.146333578783787,0.00995455679532004,
0.0155272845995164));
#16419=CARTESIAN_POINT('Ctrl Pts',(-0.14583475180505,0.0148550342388422,
0.0152581746071293));
#16420=CARTESIAN_POINT('Ctrl Pts',(-0.140929468554047,0.0630445487404258,
0.0126118447280274));
#16421=CARTESIAN_POINT('Ctrl Pts',(-0.10977174472993,0.108536575508351,
0.0099655148489255));
#16422=CARTESIAN_POINT('Ctrl Pts',(-0.0666135938566871,0.13056551637767,
0.00731918496982359));
#16423=CARTESIAN_POINT('Ctrl Pts',(-0.0268248419338395,0.150874636338504,
0.00487945664654906));
#16424=CARTESIAN_POINT('Ctrl Pts',(0.0231637104697219,0.151241233100125,
0.00243972832327453));
#16425=CARTESIAN_POINT('Ctrl Pts',(0.0635546915223951,0.132092229195826,
-2.16840434497101E-19));
#16426=CARTESIAN_POINT('',(-0.0634007094575146,0.131904027763688,0.));
#16427=CARTESIAN_POINT('Origin',(0.,0.,0.));
#16428=CARTESIAN_POINT('Ctrl Pts',(-0.0634007094575145,0.131904027763688,
-3.88578058618805E-16));
#16429=CARTESIAN_POINT('Ctrl Pts',(-0.107282641710421,0.110811831533068,
0.00264738937425961));
#16430=CARTESIAN_POINT('Ctrl Pts',(-0.139432201149969,0.0662847592091173,
0.00529477874851962));
#16431=CARTESIAN_POINT('Ctrl Pts',(-0.145436119191498,0.0182745223106641,
0.00794216812277962));
#16432=CARTESIAN_POINT('Ctrl Pts',(-0.146186273512714,0.0122759249909008,
0.00827294388708994));
#16433=CARTESIAN_POINT('Ctrl Pts',(-0.146528267289359,0.00622295186417552,
0.00860371965140026));
#16434=CARTESIAN_POINT('Ctrl Pts',(-0.146479946776166,0.000162062070299865,
0.00893449541571059));
#16435=CARTESIAN_POINT('Origin',(0.,0.,0.));
#16436=CARTESIAN_POINT('',(-0.146148830924315,7.59978318484386E-5,0.0660655045842905));
#16437=CARTESIAN_POINT('',(-0.146133770585873,6.2751561688711E-5,0.0589344954157103));
#16438=CARTESIAN_POINT('',(-0.14635,-1.79227059055215E-17,0.));
#16439=CARTESIAN_POINT('Ctrl Pts',(-0.146148830924315,7.59978318484386E-5,
0.0660655045842905));
#16440=CARTESIAN_POINT('Ctrl Pts',(-0.146240443598182,0.0195917497831913,
0.0650077071998482));
#16441=CARTESIAN_POINT('Ctrl Pts',(-0.142607114239671,0.0390747476468127,
0.0639499098154059));
#16442=CARTESIAN_POINT('Ctrl Pts',(-0.135087779856993,0.056920264102034,
0.0628921124309636));
#16443=CARTESIAN_POINT('Ctrl Pts',(-0.116276389754784,0.10156503643559,
0.0602457825518617));
#16444=CARTESIAN_POINT('Ctrl Pts',(-0.073143724514267,0.135961331060063,
0.0575994526727599));
#16445=CARTESIAN_POINT('Ctrl Pts',(-0.025432083612881,0.144366623974243,
0.054953122793658));
#16446=CARTESIAN_POINT('Ctrl Pts',(0.0222795572885053,0.152771916888423,
0.0523067929145561));
#16447=CARTESIAN_POINT('Ctrl Pts',(0.0745701738507606,0.135186208092309,
0.0496604630354541));
#16448=CARTESIAN_POINT('Ctrl Pts',(0.107505148494886,0.0996564726649905,
0.0470141331563522));
#16449=CARTESIAN_POINT('Ctrl Pts',(0.140440123139012,0.0641267372376721,
0.0443678032772503));
#16450=CARTESIAN_POINT('Ctrl Pts',(0.154019455865009,0.010652975179149,
0.0417214733981484));
#16451=CARTESIAN_POINT('Ctrl Pts',(0.14202839331759,-0.0362847016460775,
0.0390751435190465));
#16452=CARTESIAN_POINT('Ctrl Pts',(0.130037330770172,-0.0832223784713041,
0.0364288136399446));
#16453=CARTESIAN_POINT('Ctrl Pts',(0.0924758729493388,-0.123623970063234,
0.0337824837608427));
#16454=CARTESIAN_POINT('Ctrl Pts',(0.0465351214488668,-0.139005253038876,
0.0311361538817407));
#16455=CARTESIAN_POINT('Ctrl Pts',(0.000594369948394902,-0.154386536014517,
0.0284898240026388));
#16456=CARTESIAN_POINT('Ctrl Pts',(-0.0537256752317158,-0.144747510373871,
0.025843494123537));
#16457=CARTESIAN_POINT('Ctrl Pts',(-0.0915592764828275,-0.114484496435928,
0.0231971642444351));
#16458=CARTESIAN_POINT('Ctrl Pts',(-0.125545511528741,-0.0872989822136326,
0.0208199443577202));
#16459=CARTESIAN_POINT('Ctrl Pts',(-0.146227884351973,-0.0434707826450544,
0.0184427244710054));
#16460=CARTESIAN_POINT('Ctrl Pts',(-0.14652705620645,9.44412402177196E-5,
0.0160655045842905));
#16461=CARTESIAN_POINT('Ctrl Pts',(-0.146479946776166,0.000162062070299865,
0.00893449541571059));
#16462=CARTESIAN_POINT('Ctrl Pts',(-0.146141530330399,-0.0422858476614564,
0.0112511090256603));
#16463=CARTESIAN_POINT('Ctrl Pts',(-0.126658161292025,-0.0851220706608281,
0.0135677226356099));
#16464=CARTESIAN_POINT('Ctrl Pts',(-0.0941604943243988,-0.112386678841155,
0.0158843362455596));
#16465=CARTESIAN_POINT('Ctrl Pts',(-0.0570226747722624,-0.143544241621566,
0.0185317256198196));
#16466=CARTESIAN_POINT('Ctrl Pts',(-0.00288875902448078,-0.154365965709432,
0.0211791149940796));
#16467=CARTESIAN_POINT('Ctrl Pts',(0.0434083729543798,-0.140002007265973,
0.0238265043683396));
#16468=CARTESIAN_POINT('Ctrl Pts',(0.0897055049332404,-0.125638048822514,
0.0264738937425996));
#16469=CARTESIAN_POINT('Ctrl Pts',(0.12816585314318,-0.0860884078477292,
0.0291212831168596));
#16470=CARTESIAN_POINT('Ctrl Pts',(0.141191617966992,-0.0394144013492358,
0.0317686724911196));
#16471=CARTESIAN_POINT('Ctrl Pts',(0.154217382790803,0.00725960514925768,
0.0344160618653796));
#16472=CARTESIAN_POINT('Ctrl Pts',(0.141808564228487,0.0610579771714599,
0.0370634512396396));
#16473=CARTESIAN_POINT('Ctrl Pts',(0.109639063769471,0.0973098477439542,
0.0397108406138996));
#16474=CARTESIAN_POINT('Ctrl Pts',(0.0774695633104545,0.133561718316448,
0.0423582299881596));
#16475=CARTESIAN_POINT('Ctrl Pts',(0.0255393809547383,0.152267087439235,
0.0450056193624196));
#16476=CARTESIAN_POINT('Ctrl Pts',(-0.0223595433272462,0.144872892294413,
0.0476530087366796));
#16477=CARTESIAN_POINT('Ctrl Pts',(-0.070258467609231,0.137478697149591,
0.0503003981109396));
#16478=CARTESIAN_POINT('Ctrl Pts',(-0.114126133817484,0.10398493773716,
0.0529477874851996));
#16479=CARTESIAN_POINT('Ctrl Pts',(-0.133871661545403,0.059725601630819,
0.0555951768594596));
#16480=CARTESIAN_POINT('Ctrl Pts',(-0.142173753131161,0.0411165744656389,
0.0567082830448765));
#16481=CARTESIAN_POINT('Ctrl Pts',(-0.146211489678532,0.0206043892842972,
0.0578213892302934));
#16482=CARTESIAN_POINT('Ctrl Pts',(-0.146133770585873,6.2751561688711E-5,
0.0589344954157103));
#16483=CARTESIAN_POINT('Origin',(0.,0.,0.));
#16484=CARTESIAN_POINT('',(-0.146252097264499,-0.000124487410312429,0.116065504584291));
#16485=CARTESIAN_POINT('',(-0.146276374479508,-0.000129480650117819,0.10893449541571));
#16486=CARTESIAN_POINT('',(-0.14635,-1.79227059055215E-17,0.));
#16487=CARTESIAN_POINT('Ctrl Pts',(-0.146252097264499,-0.000124487410312429,
0.116065504584291));
#16488=CARTESIAN_POINT('Ctrl Pts',(-0.145977101830714,0.0338815411246725,
0.114219019807793));
#16489=CARTESIAN_POINT('Ctrl Pts',(-0.134160879762789,0.0680598926014691,
0.112372535031295));
#16490=CARTESIAN_POINT('Ctrl Pts',(-0.112484833627769,0.0939988017516943,
0.110526050254798));
#16491=CARTESIAN_POINT('Ctrl Pts',(-0.0814193359437304,0.131173714423195,
0.107879720375696));
#16492=CARTESIAN_POINT('Ctrl Pts',(-0.0301019434218634,0.151424966146533,
0.105233390496594));
#16493=CARTESIAN_POINT('Ctrl Pts',(0.0179785702873004,0.145483266051774,
0.102587060617492));
#16494=CARTESIAN_POINT('Ctrl Pts',(0.0660590839964643,0.139541565957016,
0.0999407307383904));
#16495=CARTESIAN_POINT('Ctrl Pts',(0.110902718892925,0.107406914044162,
0.0972944008592884));
#16496=CARTESIAN_POINT('Ctrl Pts',(0.131983829661647,0.0637877973597534,
0.0946480709801865));
#16497=CARTESIAN_POINT('Ctrl Pts',(0.15306494043037,0.0201686806753445,
0.0920017411010846));
#16498=CARTESIAN_POINT('Ctrl Pts',(0.150383527071356,-0.0349349007806195,
0.0893554112219828));
#16499=CARTESIAN_POINT('Ctrl Pts',(0.125166930059577,-0.0763010783846813,
0.0867090813428809));
#16500=CARTESIAN_POINT('Ctrl Pts',(0.0999503330477985,-0.117667255988743,
0.084062751463779));
#16501=CARTESIAN_POINT('Ctrl Pts',(0.0521985523832557,-0.145296029740903,
0.081416421584677));
#16502=CARTESIAN_POINT('Ctrl Pts',(0.00376830011669856,-0.146541450754272,
0.0787700917055751));
#16503=CARTESIAN_POINT('Ctrl Pts',(-0.0446619521498586,-0.147786871767642,
0.0761237618264732));
#16504=CARTESIAN_POINT('Ctrl Pts',(-0.09377067601843,-0.122648940042221,
0.0734774319473713));
#16505=CARTESIAN_POINT('Ctrl Pts',(-0.121079980470766,-0.0826333491581908,
0.0708311020682694));
#16506=CARTESIAN_POINT('Ctrl Pts',(-0.137473143648068,-0.0586128871159229,
0.0692425695736098));
#16507=CARTESIAN_POINT('Ctrl Pts',(-0.146011252866834,-0.02923151094855,
0.0676540370789502));
#16508=CARTESIAN_POINT('Ctrl Pts',(-0.146148830924315,7.59978318484386E-5,
0.0660655045842905));
#16509=CARTESIAN_POINT('Ctrl Pts',(-0.146133770585873,6.2751561688711E-5,
0.0589344954157103));
#16510=CARTESIAN_POINT('Ctrl Pts',(-0.146026644150963,-0.0282514289199324,
0.0604687786045534));
#16511=CARTESIAN_POINT('Ctrl Pts',(-0.138100435392092,-0.0566215672018456,
0.0620030617933965));
#16512=CARTESIAN_POINT('Ctrl Pts',(-0.122745086057252,-0.0801407530065182,
0.0635373449822396));
#16513=CARTESIAN_POINT('Ctrl Pts',(-0.0962495935935968,-0.120722858737265,
0.0661847343564996));
#16514=CARTESIAN_POINT('Ctrl Pts',(-0.0476352194187008,-0.146862157398507,
0.0688321237307596));
#16515=CARTESIAN_POINT('Ctrl Pts',(0.00082938917649622,-0.146587691816784,
0.0714795131050196));
#16516=CARTESIAN_POINT('Ctrl Pts',(0.0492939977716932,-0.146313226235061,
0.0741269024792796));
#16517=CARTESIAN_POINT('Ctrl Pts',(0.0976088407871913,-0.119624996410372,
0.0767742918535397));
#16518=CARTESIAN_POINT('Ctrl Pts',(0.123643642180798,-0.0787464320231966,
0.0794216812277997));
#16519=CARTESIAN_POINT('Ctrl Pts',(0.149678443574405,-0.0378678676360213,
0.0820690706020596));
#16520=CARTESIAN_POINT('Ctrl Pts',(0.153433203346121,0.0172010313136401,
0.0847164599763195));
#16521=CARTESIAN_POINT('Ctrl Pts',(0.133187835944515,0.06123527443138,0.0873638493505795));
#16522=CARTESIAN_POINT('Ctrl Pts',(0.11294246854291,0.10526951754912,0.0900112387248395));
#16523=CARTESIAN_POINT('Ctrl Pts',(0.0686969739679828,0.138269104834938,
0.0926586280990997));
#16524=CARTESIAN_POINT('Ctrl Pts',(0.0207181735233275,0.145118849380084,
0.0953060174733597));
#16525=CARTESIAN_POINT('Ctrl Pts',(-0.027260626921328,0.151968593925229,
0.0979534068476197));
#16526=CARTESIAN_POINT('Ctrl Pts',(-0.0789727332357116,0.132668495729702,
0.10060079622188));
#16527=CARTESIAN_POINT('Ctrl Pts',(-0.110731403441959,0.0960588230543748,
0.10324818559614));
#16528=CARTESIAN_POINT('Ctrl Pts',(-0.133469481440122,0.0698475998711364,
0.105143622202663));
#16529=CARTESIAN_POINT('Ctrl Pts',(-0.145979327216774,0.0347634013028336,
0.107039058809187));
#16530=CARTESIAN_POINT('Ctrl Pts',(-0.146276374479508,-0.000129480650117819,
0.10893449541571));
#16531=CARTESIAN_POINT('Origin',(0.,0.,0.));
#16532=CARTESIAN_POINT('',(-0.146589818999335,-3.81787486967988E-6,0.166065504584291));
#16533=CARTESIAN_POINT('',(-0.146589453522336,1.04004190909306E-5,0.15893449541571));
#16534=CARTESIAN_POINT('',(-0.14635,-1.79227059055215E-17,0.));
#16535=CARTESIAN_POINT('Ctrl Pts',(-0.146589818999335,-3.81787486967988E-6,
0.166065504584291));
#16536=CARTESIAN_POINT('Ctrl Pts',(-0.146571339149733,0.0482382848470949,
0.163430332415738));
#16537=CARTESIAN_POINT('Ctrl Pts',(-0.120433071521034,0.0964975486977609,
0.160795160247185));
#16538=CARTESIAN_POINT('Ctrl Pts',(-0.0800107885095625,0.122828684230981,
0.158159988078632));
#16539=CARTESIAN_POINT('Ctrl Pts',(-0.0394173515450545,0.149271309704865,
0.15551365819953));
#16540=CARTESIAN_POINT('Ctrl Pts',(0.0155813181737399,0.153599719825856,
0.152867328320428));
#16541=CARTESIAN_POINT('Ctrl Pts',(0.0598114643267532,0.133832733731537,
0.150220998441327));
#16542=CARTESIAN_POINT('Ctrl Pts',(0.104041610479766,0.114065747637217,
0.147574668562225));
#16543=CARTESIAN_POINT('Ctrl Pts',(0.137503233066998,0.0702033653275883,
0.144928338683123));
#16544=CARTESIAN_POINT('Ctrl Pts',(0.144880420813362,0.0223220882221681,
0.142282008804021));
#16545=CARTESIAN_POINT('Ctrl Pts',(0.152257608559726,-0.0255591888832524,
0.139635678924919));
#16546=CARTESIAN_POINT('Ctrl Pts',(0.133550361465222,-0.077459360784464,
0.136989349045817));
#16547=CARTESIAN_POINT('Ctrl Pts',(0.0973212811704284,-0.109622900294719,
0.134343019166715));
#16548=CARTESIAN_POINT('Ctrl Pts',(0.0610922008756344,-0.141786439804975,
0.131696689287613));
#16549=CARTESIAN_POINT('Ctrl Pts',(0.00734128738055008,-0.154213346924274,
0.129050359408511));
#16550=CARTESIAN_POINT('Ctrl Pts',(-0.0393288211819405,-0.141215634503184,
0.126404029529409));
#16551=CARTESIAN_POINT('Ctrl Pts',(-0.0859989297444312,-0.128217922082094,
0.123757699650308));
#16552=CARTESIAN_POINT('Ctrl Pts',(-0.125588233374328,-0.0897955901206149,
0.121111369771206));
#16553=CARTESIAN_POINT('Ctrl Pts',(-0.139976083766172,-0.043535137330043,
0.118465039892104));
#16554=CARTESIAN_POINT('Ctrl Pts',(-0.144324767489921,-0.0295530571287048,
0.117665194789499));
#16555=CARTESIAN_POINT('Ctrl Pts',(-0.146371217526823,-0.0148549394177889,
0.116865349686895));
#16556=CARTESIAN_POINT('Ctrl Pts',(-0.146252097264499,-0.000124487410312429,
0.116065504584291));
#16557=CARTESIAN_POINT('Ctrl Pts',(-0.146276374479508,-0.000129480650117819,
0.10893449541571));
#16558=CARTESIAN_POINT('Ctrl Pts',(-0.14639421831063,-0.0139720956278579,
0.109686448183447));
#16559=CARTESIAN_POINT('Ctrl Pts',(-0.14458995413065,-0.0277846002915201,
0.110438400951183));
#16560=CARTESIAN_POINT('Ctrl Pts',(-0.140739671041232,-0.041001045008257,
0.11119035371892));
#16561=CARTESIAN_POINT('Ctrl Pts',(-0.127184034336146,-0.0875319932404337,
0.11383774309318));
#16562=CARTESIAN_POINT('Ctrl Pts',(-0.0882675268278623,-0.12667464254966,
0.11648513246744));
#16563=CARTESIAN_POINT('Ctrl Pts',(-0.0418159243469935,-0.140499695546946,
0.1191325218417));
#16564=CARTESIAN_POINT('Ctrl Pts',(0.00463567813387508,-0.154324748544231,
0.12177991121596));
#16565=CARTESIAN_POINT('Ctrl Pts',(0.0586223755873289,-0.142832205229577,
0.12442730059022));
#16566=CARTESIAN_POINT('Ctrl Pts',(0.0954154960694136,-0.111286216216264,
0.12707468996448));
#16567=CARTESIAN_POINT('Ctrl Pts',(0.132208616551499,-0.0797402272029501,
0.12972207933874));
#16568=CARTESIAN_POINT('Ctrl Pts',(0.151808160062214,-0.0281407924909768,
0.132369468712999));
#16569=CARTESIAN_POINT('Ctrl Pts',(0.145236524363737,0.0198768833792122,
0.135016858087259));
#16570=CARTESIAN_POINT('Ctrl Pts',(0.138664888665259,0.0678945592494009,
0.13766424746152));
#16571=CARTESIAN_POINT('Ctrl Pts',(0.105922073757589,0.112330476277805,
0.14031163683578));
#16572=CARTESIAN_POINT('Ctrl Pts',(0.062005973158836,0.132830708741579,
0.14295902621004));
#16573=CARTESIAN_POINT('Ctrl Pts',(0.0180898725600832,0.153330941205352,
0.1456064155843));
#16574=CARTESIAN_POINT('Ctrl Pts',(-0.0369995137297515,0.149895489104495,
0.14825380495856));
#16575=CARTESIAN_POINT('Ctrl Pts',(-0.0780284182758478,0.124097962381086,
0.15090119433282));
#16576=CARTESIAN_POINT('Ctrl Pts',(-0.119057322821944,0.0983004356576776,
0.153548583707079));
#16577=CARTESIAN_POINT('Ctrl Pts',(-0.146025745624302,0.0501408343117172,
0.15619597308134));
#16578=CARTESIAN_POINT('Ctrl Pts',(-0.14658076309025,0.00167873146180186,
0.1588433624556));
#16579=CARTESIAN_POINT('Ctrl Pts',(-0.146587131676737,0.00112264969450139,
0.15887374010897));
#16580=CARTESIAN_POINT('Ctrl Pts',(-0.146590022522527,0.000566528098114988,
0.15890411776234));
#16581=CARTESIAN_POINT('Ctrl Pts',(-0.146589453522336,1.04004190909306E-5,
0.15893449541571));
#16582=CARTESIAN_POINT('Origin',(0.,0.,0.));
#16583=CARTESIAN_POINT('',(-0.146263250741535,0.000126870157254357,0.21606550458429));
#16584=CARTESIAN_POINT('',(-0.146245769975643,0.000123264779366826,0.20893449541571));
#16585=CARTESIAN_POINT('',(-0.14635,-1.79227059055215E-17,0.));
#16586=CARTESIAN_POINT('Ctrl Pts',(-0.146263250741535,0.000126870157254357,
0.21606550458429));
#16587=CARTESIAN_POINT('Ctrl Pts',(-0.146381923100139,0.0144435832128767,
0.215287974902784));
#16588=CARTESIAN_POINT('Ctrl Pts',(-0.144450237714319,0.0287289633064517,
0.214510445221278));
#16589=CARTESIAN_POINT('Ctrl Pts',(-0.140337374518256,0.0423560295890773,
0.213732915539772));
#16590=CARTESIAN_POINT('Ctrl Pts',(-0.126339204386259,0.0887358830222778,
0.21108658566067));
#16591=CARTESIAN_POINT('Ctrl Pts',(-0.0870745347363382,0.127489909020004,
0.208440255781569));
#16592=CARTESIAN_POINT('Ctrl Pts',(-0.0405154226099946,0.140879780169064,
0.205793925902467));
#16593=CARTESIAN_POINT('Ctrl Pts',(0.00604368951634975,0.154269651318124,
0.203147596023365));
#16594=CARTESIAN_POINT('Ctrl Pts',(0.0598972441191175,0.142295367618517,
0.200501266144263));
#16595=CARTESIAN_POINT('Ctrl Pts',(0.0963956219934077,0.110437747119808,
0.197854936265161));
#16596=CARTESIAN_POINT('Ctrl Pts',(0.132893999867697,0.0785801266211,0.195208606386059));
#16597=CARTESIAN_POINT('Ctrl Pts',(0.15203720101351,0.0268391693232909,
0.192562276506957));
#16598=CARTESIAN_POINT('Ctrl Pts',(0.145063081087281,-0.0211024746124516,
0.189915946627855));
#16599=CARTESIAN_POINT('Ctrl Pts',(0.138088961161051,-0.0690441185481943,
0.187269616748753));
#16600=CARTESIAN_POINT('Ctrl Pts',(0.10499752016278,-0.11318644912187,0.184623286869651));
#16601=CARTESIAN_POINT('Ctrl Pts',(0.060935231264163,-0.133324827106958,
0.181976956990549));
#16602=CARTESIAN_POINT('Ctrl Pts',(0.0168729423655461,-0.153463205092045,
0.179330627111448));
#16603=CARTESIAN_POINT('Ctrl Pts',(-0.0381601944334158,-0.149597630488544,
0.176684297232346));
#16604=CARTESIAN_POINT('Ctrl Pts',(-0.0789746466099193,-0.123497437688695,
0.174037967353244));
#16605=CARTESIAN_POINT('Ctrl Pts',(-0.119961184605052,-0.0972871987457574,
0.171380479763593));
#16606=CARTESIAN_POINT('Ctrl Pts',(-0.146608455341797,-0.0486544490602708,
0.168722992173942));
#16607=CARTESIAN_POINT('Ctrl Pts',(-0.146589818999335,-3.81787486967988E-6,
0.166065504584291));
#16608=CARTESIAN_POINT('Ctrl Pts',(-0.146589453522336,1.04004190909306E-5,
0.15893449541571));
#16609=CARTESIAN_POINT('Ctrl Pts',(-0.146540434588914,-0.0478995759235739,
0.1615515071366));
#16610=CARTESIAN_POINT('Ctrl Pts',(-0.120813506558866,-0.0958546957256878,
0.16416851885749));
#16611=CARTESIAN_POINT('Ctrl Pts',(-0.0808500697395765,-0.122278388912248,
0.16678553057838));
#16612=CARTESIAN_POINT('Ctrl Pts',(-0.0404227467934142,-0.149008802082514,
0.16943291995264));
#16613=CARTESIAN_POINT('Ctrl Pts',(0.0145735112284506,-0.153705024069172,
0.1720803093269));
#16614=CARTESIAN_POINT('Ctrl Pts',(0.0589475933459444,-0.134215943447351,
0.17472769870116));
#16615=CARTESIAN_POINT('Ctrl Pts',(0.103321675463438,-0.11472686282553,
0.17737508807542));
#16616=CARTESIAN_POINT('Ctrl Pts',(0.137073581676561,-0.0710524795952304,
0.18002247744968));
#16617=CARTESIAN_POINT('Ctrl Pts',(0.144743205110219,-0.0231979049720499,
0.18266986682394));
#16618=CARTESIAN_POINT('Ctrl Pts',(0.152412828543877,0.024656669651131,
0.1853172561982));
#16619=CARTESIAN_POINT('Ctrl Pts',(0.13400016919807,0.0766914356671922,
0.18796464557246));
#16620=CARTESIAN_POINT('Ctrl Pts',(0.0979391709064228,0.109071797518936,
0.19061203494672));
#16621=CARTESIAN_POINT('Ctrl Pts',(0.0618781726147763,0.141452159370678,
0.19325942432098));
#16622=CARTESIAN_POINT('Ctrl Pts',(0.00816883537729064,0.154178117058104,
0.195906813695239));
#16623=CARTESIAN_POINT('Ctrl Pts',(-0.0385872054932313,0.1414205281901,
0.198554203069499));
#16624=CARTESIAN_POINT('Ctrl Pts',(-0.0853432463637543,0.128662939322095,
0.201201592443759));
#16625=CARTESIAN_POINT('Ctrl Pts',(-0.125145990867313,0.0904218038986596,
0.20384898181802));
#16626=CARTESIAN_POINT('Ctrl Pts',(-0.139763737461459,0.0442135263146365,
0.20649637119228));
#16627=CARTESIAN_POINT('Ctrl Pts',(-0.144251162244238,0.030028291356252,
0.207309079266757));
#16628=CARTESIAN_POINT('Ctrl Pts',(-0.146365162502875,0.0150922359825044,
0.208121787341234));
#16629=CARTESIAN_POINT('Ctrl Pts',(-0.146245769975643,0.000123264779366826,
0.20893449541571));
#16630=CARTESIAN_POINT('Origin',(0.,0.,0.));
#16631=CARTESIAN_POINT('',(-0.146142672279203,-7.01165389862951E-5,0.266065504584291));
#16632=CARTESIAN_POINT('',(-0.146150215784492,-7.74481165901552E-5,0.258934495415711));
#16633=CARTESIAN_POINT('',(-0.14635,-1.79227059055215E-17,0.));
#16634=CARTESIAN_POINT('Ctrl Pts',(-0.146142672279203,-7.01165389862951E-5,
0.266065504584291));
#16635=CARTESIAN_POINT('Ctrl Pts',(-0.146017527260215,0.028828671850369,
0.264499287510729));
#16636=CARTESIAN_POINT('Ctrl Pts',(-0.137733916992107,0.0577936173630845,
0.262933070437168));
#16637=CARTESIAN_POINT('Ctrl Pts',(-0.121770841384076,0.0816117278206753,
0.261366853363607));
#16638=CARTESIAN_POINT('Ctrl Pts',(-0.0947991242083451,0.121855560193383,
0.258720523484505));
#16639=CARTESIAN_POINT('Ctrl Pts',(-0.0459036471244643,0.147405924851771,
0.256074193605403));
#16640=CARTESIAN_POINT('Ctrl Pts',(0.0025353607453442,0.146568017913755,
0.253427863726301));
#16641=CARTESIAN_POINT('Ctrl Pts',(0.050974368615152,0.145730110975738,
0.250781533847199));
#16642=CARTESIAN_POINT('Ctrl Pts',(0.0989569072708876,0.118503932441319,
0.248135203968097));
#16643=CARTESIAN_POINT('Ctrl Pts',(0.124520613871998,0.0773513325689396,
0.245488874088995));
#16644=CARTESIAN_POINT('Ctrl Pts',(0.150084320473109,0.0361987326965595,
0.242842544209893));
#16645=CARTESIAN_POINT('Ctrl Pts',(0.153229195019594,-0.0188802885137813,
0.240196214330791));
#16646=CARTESIAN_POINT('Ctrl Pts',(0.132515778953886,-0.0626751965094481,
0.237549884451689));
#16647=CARTESIAN_POINT('Ctrl Pts',(0.111802362888177,-0.106470104505115,
0.234903554572587));
#16648=CARTESIAN_POINT('Ctrl Pts',(0.0672306562102751,-0.138980899286108,
0.232257224693486));
#16649=CARTESIAN_POINT('Ctrl Pts',(0.0192018303028616,-0.145326878595667,
0.229610894814384));
#16650=CARTESIAN_POINT('Ctrl Pts',(-0.0288269956045516,-0.151672857905225,
0.226964564935282));
#16651=CARTESIAN_POINT('Ctrl Pts',(-0.0803129407414762,-0.131854021743351,
0.22431823505618));
#16652=CARTESIAN_POINT('Ctrl Pts',(-0.111690078002902,-0.0949417632280756,
0.221671905177078));
#16653=CARTESIAN_POINT('Ctrl Pts',(-0.133848162215005,-0.0688748557907962,
0.219803104979482));
#16654=CARTESIAN_POINT('Ctrl Pts',(-0.145978020566425,-0.0342834897603843,
0.217934304781886));
#16655=CARTESIAN_POINT('Ctrl Pts',(-0.146263250741535,0.000126870157254357,
0.21606550458429));
#16656=CARTESIAN_POINT('Ctrl Pts',(-0.146245769975643,0.000123264779366826,
0.20893449541571));
#16657=CARTESIAN_POINT('Ctrl Pts',(-0.145976242399967,-0.03366905549635,
0.210769176715493));
#16658=CARTESIAN_POINT('Ctrl Pts',(-0.134324750276972,-0.067629123606452,
0.212603858015276));
#16659=CARTESIAN_POINT('Ctrl Pts',(-0.112902327433,-0.0934976078712483,
0.214438539315059));
#16660=CARTESIAN_POINT('Ctrl Pts',(-0.0819904221256615,-0.130825044728502,
0.217085928689319));
#16661=CARTESIAN_POINT('Ctrl Pts',(-0.0307338628262512,-0.151304498698398,
0.21973331806358));
#16662=CARTESIAN_POINT('Ctrl Pts',(0.0173892134168267,-0.145555327884408,
0.22238070743784));
#16663=CARTESIAN_POINT('Ctrl Pts',(0.0655122896599044,-0.139806157070418,
0.2250280968121));
#16664=CARTESIAN_POINT('Ctrl Pts',(0.11050188284665,-0.107828361472542,
0.22767548618636));
#16665=CARTESIAN_POINT('Ctrl Pts',(0.131750448317205,-0.0642694140823833,
0.23032287556062));
#16666=CARTESIAN_POINT('Ctrl Pts',(0.15299901378776,-0.020710466692225,
0.232970264934879));
#16667=CARTESIAN_POINT('Ctrl Pts',(0.150506551542124,0.0344296324902152,
0.23561765430914));
#16668=CARTESIAN_POINT('Ctrl Pts',(0.125414737320077,0.0758938856636754,
0.2382650436834));
#16669=CARTESIAN_POINT('Ctrl Pts',(0.10032292309803,0.117358138837136,0.24091243305766));
#16670=CARTESIAN_POINT('Ctrl Pts',(0.0526317568995709,0.145146546001616,
0.24355982243192));
#16671=CARTESIAN_POINT('Ctrl Pts',(0.00418624259284972,0.146530589268381,
0.24620721180618));
#16672=CARTESIAN_POINT('Ctrl Pts',(-0.0442592717138715,0.147914632535146,
0.24885460118044));
#16673=CARTESIAN_POINT('Ctrl Pts',(-0.0934591341288551,0.122894311904195,
0.2515019905547));
#16674=CARTESIAN_POINT('Ctrl Pts',(-0.120877280418781,0.082930219442967,
0.25414937992896));
#16675=CARTESIAN_POINT('Ctrl Pts',(-0.137396572682769,0.0588520590724165,
0.255744418424543));
#16676=CARTESIAN_POINT('Ctrl Pts',(-0.146009100715185,0.0293493086505574,
0.257339456920127));
#16677=CARTESIAN_POINT('Ctrl Pts',(-0.146150215784492,-7.74481165901552E-5,
0.258934495415711));
#16678=CARTESIAN_POINT('Origin',(0.,0.,0.));
#16679=CARTESIAN_POINT('',(-0.146519404976022,-8.97763884284003E-5,0.316065504584291));
#16680=CARTESIAN_POINT('',(-0.146528765763263,-8.45393868379275E-5,0.30893449541571));
#16681=CARTESIAN_POINT('',(-0.14635,-1.79227059055215E-17,0.));
#16682=CARTESIAN_POINT('Ctrl Pts',(-0.146519404976022,-8.97763884284003E-5,
0.316065504584291));
#16683=CARTESIAN_POINT('Ctrl Pts',(-0.146208092107557,0.043076445171776,
0.313710600118674));
#16684=CARTESIAN_POINT('Ctrl Pts',(-0.125958424314353,0.0864965766126209,
0.311355695653057));
#16685=CARTESIAN_POINT('Ctrl Pts',(-0.0925183485457987,0.1137056160074,
0.309000791187441));
#16686=CARTESIAN_POINT('Ctrl Pts',(-0.0549399784004991,0.144281843189175,
0.306354461308339));
#16687=CARTESIAN_POINT('Ctrl Pts',(-0.00070450021881692,0.154386382754941,
0.303708131429237));
#16688=CARTESIAN_POINT('Ctrl Pts',(0.0453636543616171,0.139394227973128,
0.301061801550135));
#16689=CARTESIAN_POINT('Ctrl Pts',(0.0914318089420511,0.124402073191315,
0.298415471671033));
#16690=CARTESIAN_POINT('Ctrl Pts',(0.129332639921237,0.0843132240619223,
0.295769141791931));
#16691=CARTESIAN_POINT('Ctrl Pts',(0.141718340675246,0.0374769775398043,
0.293122811912829));
#16692=CARTESIAN_POINT('Ctrl Pts',(0.154104041429255,-0.00935926898231351,
0.290476482033727));
#16693=CARTESIAN_POINT('Ctrl Pts',(0.140974611958088,-0.0629429128971569,
0.287830152154626));
#16694=CARTESIAN_POINT('Ctrl Pts',(0.108339598692885,-0.0987478773661917,
0.285183822275524));
#16695=CARTESIAN_POINT('Ctrl Pts',(0.0757045854276824,-0.134552841835227,
0.282537492396422));
#16696=CARTESIAN_POINT('Ctrl Pts',(0.0235639883684441,-0.152579126858453,
0.27989116251732));
#16697=CARTESIAN_POINT('Ctrl Pts',(-0.0242166208952047,-0.144575818177467,
0.277244832638218));
#16698=CARTESIAN_POINT('Ctrl Pts',(-0.0719972301588528,-0.136572509496481,
0.274598502759116));
#16699=CARTESIAN_POINT('Ctrl Pts',(-0.115417851626912,-0.102539607111283,
0.271952172880014));
#16700=CARTESIAN_POINT('Ctrl Pts',(-0.13460418372715,-0.0580545058751705,
0.269305843000912));
#16701=CARTESIAN_POINT('Ctrl Pts',(-0.142435181350113,-0.0398976888130428,
0.268225730195372));
#16702=CARTESIAN_POINT('Ctrl Pts',(-0.146228976240411,-0.0199996345674016,
0.267145617389831));
#16703=CARTESIAN_POINT('Ctrl Pts',(-0.146142672279203,-7.01165389862951E-5,
0.266065504584291));
#16704=CARTESIAN_POINT('Ctrl Pts',(-0.146150215784492,-7.74481165901552E-5,
0.258934495415711));
#16705=CARTESIAN_POINT('Ctrl Pts',(-0.146243318595233,-0.0194921979337541,
0.259986846294387));
#16706=CARTESIAN_POINT('Ctrl Pts',(-0.142648899141753,-0.0388738684647463,
0.261039197173063));
#16707=CARTESIAN_POINT('Ctrl Pts',(-0.135204796371803,-0.0566427511368837,
0.26209154805174));
#16708=CARTESIAN_POINT('Ctrl Pts',(-0.116477735870028,-0.101343764964001,
0.264738937426));
#16709=CARTESIAN_POINT('Ctrl Pts',(-0.0733871847016099,-0.135837928326728,
0.26738632680026));
#16710=CARTESIAN_POINT('Ctrl Pts',(-0.0256708287318585,-0.144325142544676,
0.27003371617452));
#16711=CARTESIAN_POINT('Ctrl Pts',(0.0220455272378925,-0.152812356762624,
0.27268110554878));
#16712=CARTESIAN_POINT('Ctrl Pts',(0.0743876880089763,-0.135292621835792,
0.27532849492304));
#16713=CARTESIAN_POINT('Ctrl Pts',(0.10738025529095,-0.0997908762961729,
0.2779758842973));
#16714=CARTESIAN_POINT('Ctrl Pts',(0.140372822572925,-0.0642891307565533,
0.280623273671559));
#16715=CARTESIAN_POINT('Ctrl Pts',(0.154015796365789,-0.010805374604146,
0.283270663045819));
#16716=CARTESIAN_POINT('Ctrl Pts',(0.142059993874458,0.0361620845457957,
0.285918052420079));
#16717=CARTESIAN_POINT('Ctrl Pts',(0.130104191383128,0.0831295436957373,
0.288565441794339));
#16718=CARTESIAN_POINT('Ctrl Pts',(0.0925496126076039,0.123580705843213,
0.291212831168599));
#16719=CARTESIAN_POINT('Ctrl Pts',(0.0465981836912963,0.138986860871753,
0.29386022054286));
#16720=CARTESIAN_POINT('Ctrl Pts',(0.000646754774988913,0.154393015900293,
0.296507609917119));
#16721=CARTESIAN_POINT('Ctrl Pts',(-0.0537015242821025,0.144754163809898,
0.29915499929138));
#16722=CARTESIAN_POINT('Ctrl Pts',(-0.0915523499663989,0.114485393976436,
0.30180238866564));
#16723=CARTESIAN_POINT('Ctrl Pts',(-0.125542580994678,0.0873038870745135,
0.30417975758233));
#16724=CARTESIAN_POINT('Ctrl Pts',(-0.146229051243382,0.0434861464246214,
0.30655712649902));
#16725=CARTESIAN_POINT('Ctrl Pts',(-0.146528765763263,-8.45393868379275E-5,
0.30893449541571));
#16726=CARTESIAN_POINT('Origin',(0.,0.,0.));
#16727=CARTESIAN_POINT('',(-0.146416087288192,0.000126442170093593,0.366065504584291));
#16728=CARTESIAN_POINT('',(-0.146408012399712,0.000128195943346294,0.358934495415711));
#16729=CARTESIAN_POINT('',(-0.14635,-1.79227059055215E-17,0.));
#16730=CARTESIAN_POINT('Ctrl Pts',(-0.146416087288192,0.000126442170093593,
0.366065504584291));
#16731=CARTESIAN_POINT('Ctrl Pts',(-0.146499294961499,0.00925816812376314,
0.365568242605721));
#16732=CARTESIAN_POINT('Ctrl Pts',(-0.145718277739785,0.0183757049974218,
0.365070980627151));
#16733=CARTESIAN_POINT('Ctrl Pts',(-0.144021710151773,0.0273195705351122,
0.364573718648581));
#16734=CARTESIAN_POINT('Ctrl Pts',(-0.134992913071845,0.0749170536065741,
0.361927388769479));
#16735=CARTESIAN_POINT('Ctrl Pts',(-0.100034284522917,0.117595890322328,
0.359281058890377));
#16736=CARTESIAN_POINT('Ctrl Pts',(-0.0551469387876206,0.135821305661589,
0.356634729011275));
#16737=CARTESIAN_POINT('Ctrl Pts',(-0.0102595930523245,0.15404672100085,
0.353988399132173));
#16738=CARTESIAN_POINT('Ctrl Pts',(0.0445564698693406,0.147818714963618,
0.351342069253072));
#16739=CARTESIAN_POINT('Ctrl Pts',(0.0842110755700531,0.119987943896873,
0.34869573937397));
#16740=CARTESIAN_POINT('Ctrl Pts',(0.123865681270766,0.0921571728301272,
0.346049409494868));
#16741=CARTESIAN_POINT('Ctrl Pts',(0.148358829750526,0.0427236367338667,
0.343403079615766));
#16742=CARTESIAN_POINT('Ctrl Pts',(0.146479621605269,-0.00568615719458776,
0.340756749736664));
#16743=CARTESIAN_POINT('Ctrl Pts',(0.144600413460012,-0.0540959511230416,
0.338110419857562));
#16744=CARTESIAN_POINT('Ctrl Pts',(0.116348848689739,-0.101482002883689,
0.33546408997846));
#16745=CARTESIAN_POINT('Ctrl Pts',(0.0746561129649502,-0.126154971072205,
0.332817760099358));
#16746=CARTESIAN_POINT('Ctrl Pts',(0.0329633772401616,-0.150827939260721,
0.330171430220256));
#16747=CARTESIAN_POINT('Ctrl Pts',(-0.0221705294391424,-0.152787823877104,
0.327525100341154));
#16748=CARTESIAN_POINT('Ctrl Pts',(-0.0655099505772086,-0.131137554898038,
0.324878770462052));
#16749=CARTESIAN_POINT('Ctrl Pts',(-0.108849371715275,-0.109487285918972,
0.322232440582951));
#16750=CARTESIAN_POINT('Ctrl Pts',(-0.140394307312104,-0.0642268633444555,
0.319586110703849));
#16751=CARTESIAN_POINT('Ctrl Pts',(-0.14570614405606,-0.0160726946583056,
0.316939780824747));
#16752=CARTESIAN_POINT('Ctrl Pts',(-0.146291106736525,-0.0107697471190636,
0.316648355411261));
#16753=CARTESIAN_POINT('Ctrl Pts',(-0.146557930734812,-0.0054317060295066,
0.316356929997776));
#16754=CARTESIAN_POINT('Ctrl Pts',(-0.146519404976022,-8.97763884284003E-5,
0.316065504584291));
#16755=CARTESIAN_POINT('Ctrl Pts',(-0.146528765763263,-8.45393868379275E-5,
0.30893449541571));
#16756=CARTESIAN_POINT('Ctrl Pts',(-0.146562807199252,-0.00503327764821679,
0.30920451587328));
#16757=CARTESIAN_POINT('Ctrl Pts',(-0.14633385314783,-0.00997882882536714,
0.30947453633085));
#16758=CARTESIAN_POINT('Ctrl Pts',(-0.145831525524598,-0.0148964553326841,
0.309744556788419));
#16759=CARTESIAN_POINT('Ctrl Pts',(-0.140906503086998,-0.0631108472318147,
0.312391946162679));
#16760=CARTESIAN_POINT('Ctrl Pts',(-0.109703085900295,-0.108640943453547,
0.31503933553694));
#16761=CARTESIAN_POINT('Ctrl Pts',(-0.0665140418604196,-0.13063162118607,
0.3176867249112));
#16762=CARTESIAN_POINT('Ctrl Pts',(-0.0233249978205455,-0.152622298918592,
0.32033411428546));
#16763=CARTESIAN_POINT('Ctrl Pts',(0.0318496730725009,-0.151073558161906,
0.322981503659719));
#16764=CARTESIAN_POINT('Ctrl Pts',(0.0737371373950496,-0.126694801736668,
0.325628893033979));
#16765=CARTESIAN_POINT('Ctrl Pts',(0.115624601717599,-0.10231604531143,
0.328276282408239));
#16766=CARTESIAN_POINT('Ctrl Pts',(0.144224859469651,-0.0551072732176397,
0.3309236717825));
#16767=CARTESIAN_POINT('Ctrl Pts',(0.146437523492708,-0.0066925280449658,
0.33357106115676));
#16768=CARTESIAN_POINT('Ctrl Pts',(0.148650187515766,0.0417222171277085,
0.33621845053102));
#16769=CARTESIAN_POINT('Ctrl Pts',(0.124475257809829,0.0913429353792657,
0.33886583990528));
#16770=CARTESIAN_POINT('Ctrl Pts',(0.0849860939726622,0.119440788885456,
0.34151322927954));
#16771=CARTESIAN_POINT('Ctrl Pts',(0.0454969301354961,0.147538642391646,
0.344160618653799));
#16772=CARTESIAN_POINT('Ctrl Pts',(-0.00930646783289898,0.154113631152469,
0.346808008028059));
#16773=CARTESIAN_POINT('Ctrl Pts',(-0.0543213285795041,0.136154072578339,
0.349455397402319));
#16774=CARTESIAN_POINT('Ctrl Pts',(-0.0993361893261098,0.11819451400421,
0.352102786776579));
#16775=CARTESIAN_POINT('Ctrl Pts',(-0.134562512850926,0.0757004080951257,
0.35475017615084));
#16776=CARTESIAN_POINT('Ctrl Pts',(-0.143864833510727,0.0281362381501331,
0.3573975655251));
#16777=CARTESIAN_POINT('Ctrl Pts',(-0.145664973529558,0.0189318504589563,
0.357909875488637));
#16778=CARTESIAN_POINT('Ctrl Pts',(-0.146494308508217,0.00953759842677947,
0.358422185452174));
#16779=CARTESIAN_POINT('Ctrl Pts',(-0.146408012399712,0.000128195943346294,
0.358934495415711));
#16780=CARTESIAN_POINT('Origin',(0.,0.,0.));
#16781=CARTESIAN_POINT('',(-0.146110491840834,1.12683595067248E-5,0.416065504584291));
#16782=CARTESIAN_POINT('',(-0.146109756335714,8.81622270207575E-6,0.40893449541571));
#16783=CARTESIAN_POINT('',(-0.14635,-1.79227059055215E-17,0.));
#16784=CARTESIAN_POINT('Ctrl Pts',(-0.146110491840834,1.12683595067248E-5,
0.416065504584291));
#16785=CARTESIAN_POINT('Ctrl Pts',(-0.146126798292857,0.0237518011834032,
0.414779555213666));
#16786=CARTESIAN_POINT('Ctrl Pts',(-0.140669750958991,0.0474852665485293,
0.413493605843041));
#16787=CARTESIAN_POINT('Ctrl Pts',(-0.129698698951591,0.0683144158983218,
0.412207656472415));
#16788=CARTESIAN_POINT('Ctrl Pts',(-0.107121587134001,0.111178312051432,
0.409561326593314));
#16789=CARTESIAN_POINT('Ctrl Pts',(-0.0611933749717542,0.141742803557285,
0.406914996714211));
#16790=CARTESIAN_POINT('Ctrl Pts',(-0.0129361277491455,0.146018041789781,
0.40426866683511));
#16791=CARTESIAN_POINT('Ctrl Pts',(0.0353211194734639,0.150293280022276,
0.401622336956008));
#16792=CARTESIAN_POINT('Ctrl Pts',(0.0859074017564354,0.128279264981412,
0.398976007076906));
#16793=CARTESIAN_POINT('Ctrl Pts',(0.115668581836909,0.0900521576926538,
0.396329677197804));
#16794=CARTESIAN_POINT('Ctrl Pts',(0.145429761917382,0.0518250504038959,
0.393683347318702));
#16795=CARTESIAN_POINT('Ctrl Pts',(0.154365839795359,-0.0026151491327561,
0.3910370174396));
#16796=CARTESIAN_POINT('Ctrl Pts',(0.138386632036901,-0.0483503050946702,
0.388390687560498));
#16797=CARTESIAN_POINT('Ctrl Pts',(0.122407424278443,-0.094085461056585,
0.385744357681396));
#16798=CARTESIAN_POINT('Ctrl Pts',(0.0815129308835505,-0.131115573443762,
0.383098027802294));
#16799=CARTESIAN_POINT('Ctrl Pts',(0.0344212048624006,-0.142491377230642,
0.380451697923192));
#16800=CARTESIAN_POINT('Ctrl Pts',(-0.0126705211587486,-0.153867181017521,
0.37780536804409));
#16801=CARTESIAN_POINT('Ctrl Pts',(-0.0659594798061549,-0.139588676204105,
0.375159038164988));
#16802=CARTESIAN_POINT('Ctrl Pts',(-0.101054476324393,-0.106191359083811,
0.372512708285887));
#16803=CARTESIAN_POINT('Ctrl Pts',(-0.129554902927378,-0.0790696072742943,
0.370363640385355));
#16804=CARTESIAN_POINT('Ctrl Pts',(-0.146056480184715,-0.0393390709180539,
0.368214572484823));
#16805=CARTESIAN_POINT('Ctrl Pts',(-0.146416087288192,0.000126442170093593,
0.366065504584291));
#16806=CARTESIAN_POINT('Ctrl Pts',(-0.146408012399712,0.000128195943346294,
0.358934495415711));
#16807=CARTESIAN_POINT('Ctrl Pts',(-0.146048368712081,-0.0390859965171687,
0.361069574826434));
#16808=CARTESIAN_POINT('Ctrl Pts',(-0.1297855810823,-0.0785633296797545,
0.363204654237157));
#16809=CARTESIAN_POINT('Ctrl Pts',(-0.101613371150224,-0.105657280969165,
0.36533973364788));
#16810=CARTESIAN_POINT('Ctrl Pts',(-0.066681270335132,-0.139252396162569,
0.36798712302214));
#16811=CARTESIAN_POINT('Ctrl Pts',(-0.0134387509101597,-0.153808392568477,
0.370634512396399));
#16812=CARTESIAN_POINT('Ctrl Pts',(0.0337263783221333,-0.142657876135818,
0.373281901770659));
#16813=CARTESIAN_POINT('Ctrl Pts',(0.0808915075544263,-0.13150735970316,
0.375929291144919));
#16814=CARTESIAN_POINT('Ctrl Pts',(0.12197924659404,-0.0946503304319347,
0.378576680519179));
#16815=CARTESIAN_POINT('Ctrl Pts',(0.138169300408926,-0.0489692009616054,
0.38122406989344));
#16816=CARTESIAN_POINT('Ctrl Pts',(0.154359354223812,-0.00328807149127619,
0.3838714592677));
#16817=CARTESIAN_POINT('Ctrl Pts',(0.14565172281397,0.0512171581781573,
0.38651884864196));
#16818=CARTESIAN_POINT('Ctrl Pts',(0.11603494864959,0.0895802930905963,
0.38916623801622));
#16819=CARTESIAN_POINT('Ctrl Pts',(0.0864181744852101,0.127943428003035,
0.39181362739048));
#16820=CARTESIAN_POINT('Ctrl Pts',(0.0358922575662923,0.15016446815848,
0.394461016764739));
#16821=CARTESIAN_POINT('Ctrl Pts',(-0.0123993367959677,0.146065035738641,
0.397108406138999));
#16822=CARTESIAN_POINT('Ctrl Pts',(-0.0606909311582276,0.141965603318802,
0.399755795513259));
#16823=CARTESIAN_POINT('Ctrl Pts',(-0.106748202963829,0.111545698323679,
0.40240318488752));
#16824=CARTESIAN_POINT('Ctrl Pts',(-0.129474555904152,0.0687391998188283,
0.40505057426178));
#16825=CARTESIAN_POINT('Ctrl Pts',(-0.140588317483115,0.0478057390183907,
0.406345214646423));
#16826=CARTESIAN_POINT('Ctrl Pts',(-0.146122589096428,0.0239100770892618,
0.407639855031067));
#16827=CARTESIAN_POINT('Ctrl Pts',(-0.146109756335714,8.81622270207575E-6,
0.40893449541571));
#16828=CARTESIAN_POINT('Origin',(0.,0.,0.));
#16829=CARTESIAN_POINT('',(-0.146374718215768,-0.000132229735885947,0.466065504584291));
#16830=CARTESIAN_POINT('',(-0.146375609273197,-0.000132432188538665,0.458934495415711));
#16831=CARTESIAN_POINT('',(-0.14635,-1.79227059055215E-17,0.));
#16832=CARTESIAN_POINT('Ctrl Pts',(-0.146374718215768,-0.000132229735885947,
0.466065504584291));
#16833=CARTESIAN_POINT('Ctrl Pts',(-0.146022504084922,0.0379941335185874,
0.46399086782161));
#16834=CARTESIAN_POINT('Ctrl Pts',(-0.130761950520226,0.0763703265456945,
0.46191623105893));
#16835=CARTESIAN_POINT('Ctrl Pts',(-0.103994021541854,0.103314352404769,
0.45984159429625));
#16836=CARTESIAN_POINT('Ctrl Pts',(-0.0698498419286355,0.137683154682254,
0.457195264417148));
#16837=CARTESIAN_POINT('Ctrl Pts',(-0.0169824611430249,0.153451124186949,
0.454548934538046));
#16838=CARTESIAN_POINT('Ctrl Pts',(0.030409888879481,0.143401013202843,
0.451902604658944));
#16839=CARTESIAN_POINT('Ctrl Pts',(0.0778022389019875,0.133350902218736,
0.449256274779842));
#16840=CARTESIAN_POINT('Ctrl Pts',(0.119719558161389,0.0974827107458278,
0.44660994490074));
#16841=CARTESIAN_POINT('Ctrl Pts',(0.136975630157447,0.0522138743269898,
0.443963615021638));
#16842=CARTESIAN_POINT('Ctrl Pts',(0.154231702153504,0.00694503790815254,
0.441317285142536));
#16843=CARTESIAN_POINT('Ctrl Pts',(0.146826526886218,-0.0477244434566137,
0.438670955263434));
#16844=CARTESIAN_POINT('Ctrl Pts',(0.118149569579287,-0.0867714880447125,
0.436024625384332));
#16845=CARTESIAN_POINT('Ctrl Pts',(0.0894726122723542,-0.125818532632812,
0.43337829550523));
#16846=CARTESIAN_POINT('Ctrl Pts',(0.0395238729257754,-0.149243140444243,
0.430731965626129));
#16847=CARTESIAN_POINT('Ctrl Pts',(-0.00883432462988853,-0.146323499949933,
0.428085635747027));
#16848=CARTESIAN_POINT('Ctrl Pts',(-0.0571925221855517,-0.143403859455623,
0.425439305867925));
#16849=CARTESIAN_POINT('Ctrl Pts',(-0.1039601779503,-0.114139970655572,
0.422792975988823));
#16850=CARTESIAN_POINT('Ctrl Pts',(-0.127731000096207,-0.0719263758553634,
0.420146646109721));
#16851=CARTESIAN_POINT('Ctrl Pts',(-0.139950702323481,-0.0502259249733931,
0.418786265601244));
#16852=CARTESIAN_POINT('Ctrl Pts',(-0.146093241566443,-0.0251033736724598,
0.417425885092767));
#16853=CARTESIAN_POINT('Ctrl Pts',(-0.146110491840834,1.12683595067248E-5,
0.416065504584291));
#16854=CARTESIAN_POINT('Ctrl Pts',(-0.146109756335714,8.81622270207575E-6,
0.40893449541571));
#16855=CARTESIAN_POINT('Ctrl Pts',(-0.146096347589706,-0.0249652282079418,
0.410287244405327));
#16856=CARTESIAN_POINT('Ctrl Pts',(-0.140026707259891,-0.049945385460595,
0.411639993394943));
#16857=CARTESIAN_POINT('Ctrl Pts',(-0.127937780377622,-0.0715588049813403,
0.412992742384559));
#16858=CARTESIAN_POINT('Ctrl Pts',(-0.104279217835726,-0.113857219262079,
0.415640131758819));
#16859=CARTESIAN_POINT('Ctrl Pts',(-0.0575666586768896,-0.14326095580898,
0.41828752113308));
#16860=CARTESIAN_POINT('Ctrl Pts',(-0.00919685447762893,-0.146301592903247,
0.42093491050734));
#16861=CARTESIAN_POINT('Ctrl Pts',(0.039172949721632,-0.149342229997515,
0.4235822998816));
#16862=CARTESIAN_POINT('Ctrl Pts',(0.089199998961318,-0.126019767639148,
0.426229689255859));
#16863=CARTESIAN_POINT('Ctrl Pts',(0.117969334952632,-0.0870170915920772,
0.428877078630119));
#16864=CARTESIAN_POINT('Ctrl Pts',(0.146738670943946,-0.0480144155450057,
0.431524468004379));
#16865=CARTESIAN_POINT('Ctrl Pts',(0.154250293686888,0.00666847419077017,
0.43417185737864));
#16866=CARTESIAN_POINT('Ctrl Pts',(0.137063494116028,0.051984005222912,
0.4368192467529));
#16867=CARTESIAN_POINT('Ctrl Pts',(0.119876694545168,0.0972995362550541,
0.43946663612716));
#16868=CARTESIAN_POINT('Ctrl Pts',(0.0779914726605056,0.133247708583562,
0.442114025501419));
#16869=CARTESIAN_POINT('Ctrl Pts',(0.0305934116013849,0.143362412733947,
0.444761414875679));
#16870=CARTESIAN_POINT('Ctrl Pts',(-0.0168046494577345,0.153477116884331,
0.447408804249939));
#16871=CARTESIAN_POINT('Ctrl Pts',(-0.0697155496913122,0.137758352856595,
0.4500561936242));
#16872=CARTESIAN_POINT('Ctrl Pts',(-0.103903378920715,0.103406122000434,
0.45270358299846));
#16873=CARTESIAN_POINT('Ctrl Pts',(-0.130724942802416,0.0764555792150183,
0.45478055380421));
#16874=CARTESIAN_POINT('Ctrl Pts',(-0.146022533856355,0.0380362146017157,
0.45685752460996));
#16875=CARTESIAN_POINT('Ctrl Pts',(-0.146375609273197,-0.000132432188538665,
0.458934495415711));
#16876=CARTESIAN_POINT('Origin',(0.,0.,0.));
#16877=CARTESIAN_POINT('',(-0.146548608312775,6.99729089778146E-5,0.516065504584291));
#16878=CARTESIAN_POINT('',(-0.146550766805835,6.86360251013434E-5,0.508934495415711));
#16879=CARTESIAN_POINT('',(-0.14635,-1.79227059055215E-17,0.));
#16880=CARTESIAN_POINT('Ctrl Pts',(-0.146548608312775,6.99729089778146E-5,
0.516065504584291));
#16881=CARTESIAN_POINT('Ctrl Pts',(-0.146572081366671,0.00404546554386884,
0.515848510308657));
#16882=CARTESIAN_POINT('Ctrl Pts',(-0.146424333269732,0.00801918670503405,
0.515631516033023));
#16883=CARTESIAN_POINT('Ctrl Pts',(-0.146099725131082,0.0119784074854107,
0.51541452175739));
#16884=CARTESIAN_POINT('Ctrl Pts',(-0.142141002193345,0.06026265009261,
0.512768191878288));
#16885=CARTESIAN_POINT('Ctrl Pts',(-0.111878319621163,0.106390286678145,
0.510121861999186));
#16886=CARTESIAN_POINT('Ctrl Pts',(-0.069163383343408,0.129247972261684,
0.507475532120084));
#16887=CARTESIAN_POINT('Ctrl Pts',(-0.0264484470656534,0.152105657845224,
0.504829202240982));
#16888=CARTESIAN_POINT('Ctrl Pts',(0.0287187429176733,0.151693392426768,
0.50218287236188));
#16889=CARTESIAN_POINT('Ctrl Pts',(0.07108729581893,0.128199876374419,0.499536542482778));
#16890=CARTESIAN_POINT('Ctrl Pts',(0.113455848720186,0.10470636032207,0.496890212603677));
#16891=CARTESIAN_POINT('Ctrl Pts',(0.143025764539373,0.0581315936358261,
0.494243882724575));
#16892=CARTESIAN_POINT('Ctrl Pts',(0.146262427589597,0.00979357977770552,
0.491597552845473));
#16893=CARTESIAN_POINT('Ctrl Pts',(0.149499090639821,-0.0385444340804161,
0.488951222966371));
#16894=CARTESIAN_POINT('Ctrl Pts',(0.126402500921083,-0.0886456951104151,
0.486304893087269));
#16895=CARTESIAN_POINT('Ctrl Pts',(0.087544330920799,-0.117578067907642,
0.483658563208167));
#16896=CARTESIAN_POINT('Ctrl Pts',(0.0486861609205161,-0.146510440704867,
0.481012233329065));
#16897=CARTESIAN_POINT('Ctrl Pts',(-0.00593358936131212,-0.154273925269321,
0.478365903449963));
#16898=CARTESIAN_POINT('Ctrl Pts',(-0.0513146009011563,-0.137315052574797,
0.475719573570861));
#16899=CARTESIAN_POINT('Ctrl Pts',(-0.0966956124410008,-0.120356179880273,
0.473073243691759));
#16900=CARTESIAN_POINT('Ctrl Pts',(-0.132837885238862,-0.078674949926771,
0.470426913812657));
#16901=CARTESIAN_POINT('Ctrl Pts',(-0.14319853241738,-0.0313495174248821,
0.467780583933555));
#16902=CARTESIAN_POINT('Ctrl Pts',(-0.145436768368387,-0.0211256884885646,
0.467208890817134));
#16903=CARTESIAN_POINT('Ctrl Pts',(-0.146471775395962,-0.0106384445195334,
0.466637197700712));
#16904=CARTESIAN_POINT('Ctrl Pts',(-0.146374718215768,-0.000132229735885947,
0.466065504584291));
#16905=CARTESIAN_POINT('Ctrl Pts',(-0.146375609273197,-0.000132432188538665,
0.458934495415711));
#16906=CARTESIAN_POINT('Ctrl Pts',(-0.146472577787773,-0.0106150565970108,
0.45950491398422));
#16907=CARTESIAN_POINT('Ctrl Pts',(-0.145442327125792,-0.021078770125739,
0.46007533255273));
#16908=CARTESIAN_POINT('Ctrl Pts',(-0.143213999951756,-0.0312807998000163,
0.460645751121239));
#16909=CARTESIAN_POINT('Ctrl Pts',(-0.132872033528166,-0.0786297930597184,
0.463293140495499));
#16910=CARTESIAN_POINT('Ctrl Pts',(-0.0967233424557573,-0.120342081894533,
0.465940529869759));
#16911=CARTESIAN_POINT('Ctrl Pts',(-0.0513258840937604,-0.13731129538499,
0.46858791924402));
#16912=CARTESIAN_POINT('Ctrl Pts',(-0.00592842573176499,-0.154280508875447,
0.47123530861828));
#16913=CARTESIAN_POINT('Ctrl Pts',(0.0487177999198187,-0.146506647021548,
0.47388269799254));
#16914=CARTESIAN_POINT('Ctrl Pts',(0.0875820145025328,-0.117550537871965,
0.476530087366799));
#16915=CARTESIAN_POINT('Ctrl Pts',(0.126446229085248,-0.0885944287223814,
0.47917747674106));
#16916=CARTESIAN_POINT('Ctrl Pts',(0.149528432599094,-0.0384560722771122,
0.481824866115319));
#16917=CARTESIAN_POINT('Ctrl Pts',(0.146255790172295,0.0098985887573764,
0.484472255489579));
#16918=CARTESIAN_POINT('Ctrl Pts',(0.142983147745498,0.0582532497918637,
0.487119644863839));
#16919=CARTESIAN_POINT('Ctrl Pts',(0.113355659378058,0.10482421541557,0.4897670342381));
#16920=CARTESIAN_POINT('Ctrl Pts',(0.0709442366160257,0.128279591164298,
0.49241442361236));
#16921=CARTESIAN_POINT('Ctrl Pts',(0.0285328138539934,0.151734966913027,
0.49506181298662));
#16922=CARTESIAN_POINT('Ctrl Pts',(-0.0266625433026316,0.152074752786777,
0.497709202360879));
#16923=CARTESIAN_POINT('Ctrl Pts',(-0.0693595260588707,0.129143309401606,
0.500356591735139));
#16924=CARTESIAN_POINT('Ctrl Pts',(-0.11205650881511,0.106211866016435,
0.503003981109399));
#16925=CARTESIAN_POINT('Ctrl Pts',(-0.142255117170964,0.060009193372344,
0.505651370483659));
#16926=CARTESIAN_POINT('Ctrl Pts',(-0.146122837288996,0.0116984888307781,
0.50829875985792));
#16927=CARTESIAN_POINT('Ctrl Pts',(-0.146432431239741,0.00783142983325791,
0.508510671710517));
#16928=CARTESIAN_POINT('Ctrl Pts',(-0.14657331536999,0.00395086404934249,
0.508722583563114));
#16929=CARTESIAN_POINT('Ctrl Pts',(-0.146550766805835,6.86360251013434E-5,
0.508934495415711));
#16930=CARTESIAN_POINT('Origin',(0.,0.,0.));
#16931=CARTESIAN_POINT('',(-0.146165204287215,8.83645032875094E-5,0.566065504584291));
#16932=CARTESIAN_POINT('',(-0.146168951232552,9.12430751481418E-5,0.558934495415711));
#16933=CARTESIAN_POINT('',(-0.14635,-1.79227059055215E-17,0.));
#16934=CARTESIAN_POINT('Ctrl Pts',(-0.146165204287215,8.83645032875094E-5,
0.566065504584291));
#16935=CARTESIAN_POINT('Ctrl Pts',(-0.146267412293664,0.0186373661349918,
0.565059822916602));
#16936=CARTESIAN_POINT('Ctrl Pts',(-0.142994166834961,0.0371516370495788,
0.564054141248913));
#16937=CARTESIAN_POINT('Ctrl Pts',(-0.136179985035193,0.0542551712289143,
0.563048459581224));
#16938=CARTESIAN_POINT('Ctrl Pts',(-0.118249288396568,0.0992610562830057,
0.560402129702122));
#16939=CARTESIAN_POINT('Ctrl Pts',(-0.0758005933416487,0.134498778989873,
0.55775579982302));
#16940=CARTESIAN_POINT('Ctrl Pts',(-0.0282633354322908,0.143839479279877,
0.555109469943918));
#16941=CARTESIAN_POINT('Ctrl Pts',(0.0192739224770691,0.153180179569881,
0.552463140064816));
#16942=CARTESIAN_POINT('Ctrl Pts',(0.0718997432408687,0.136623857443018,
0.549816810185715));
#16943=CARTESIAN_POINT('Ctrl Pts',(0.105526460745998,0.101748602013432,
0.547170480306613));
#16944=CARTESIAN_POINT('Ctrl Pts',(0.139153178251127,0.0668733465838454,
0.544524150427511));
#16945=CARTESIAN_POINT('Ctrl Pts',(0.153780792497586,0.0136791578515372,
0.541877820548409));
#16946=CARTESIAN_POINT('Ctrl Pts',(0.142714014311998,-0.0334861471092027,
0.539231490669307));
#16947=CARTESIAN_POINT('Ctrl Pts',(0.13164723612641,-0.0806514520699426,
0.536585160790205));
#16948=CARTESIAN_POINT('Ctrl Pts',(0.0948860655087725,-0.121787873259113,
0.533938830911103));
#16949=CARTESIAN_POINT('Ctrl Pts',(0.0492566686055307,-0.138066623508903,
0.531292501032001));
#16950=CARTESIAN_POINT('Ctrl Pts',(0.00362727170228945,-0.154345373758693,
0.528646171152899));
#16951=CARTESIAN_POINT('Ctrl Pts',(-0.050870351486557,-0.145766453069103,
0.525999841273797));
#16952=CARTESIAN_POINT('Ctrl Pts',(-0.089291781429334,-0.116256568409877,
0.523353511394695));
#16953=CARTESIAN_POINT('Ctrl Pts',(-0.124562723435938,-0.0891664410515947,
0.520924175791227));
#16954=CARTESIAN_POINT('Ctrl Pts',(-0.146285818313441,-0.0444372186796531,
0.518494840187759));
#16955=CARTESIAN_POINT('Ctrl Pts',(-0.146548608312775,6.99729089778146E-5,
0.516065504584291));
#16956=CARTESIAN_POINT('Ctrl Pts',(-0.146550766805835,6.86360251013434E-5,
0.508934495415711));
#16957=CARTESIAN_POINT('Ctrl Pts',(-0.146291618860727,-0.0445493453248537,
0.511369972937373));
#16958=CARTESIAN_POINT('Ctrl Pts',(-0.124445252016267,-0.0893868858389474,
0.513805450459036));
#16959=CARTESIAN_POINT('Ctrl Pts',(-0.0890226177929609,-0.116463349340462,
0.516240927980699));
#16960=CARTESIAN_POINT('Ctrl Pts',(-0.0505178462986829,-0.145895746531099,
0.518888317354959));
#16961=CARTESIAN_POINT('Ctrl Pts',(0.00402852857008221,-0.154341804473332,
0.52153570672922));
#16962=CARTESIAN_POINT('Ctrl Pts',(0.0496314652424392,-0.137932794781367,
0.52418309610348));
#16963=CARTESIAN_POINT('Ctrl Pts',(0.0952344019147948,-0.121523785089403,
0.52683048547774));
#16964=CARTESIAN_POINT('Ctrl Pts',(0.131893900390741,-0.0802597077632436,
0.529477874851999));
#16965=CARTESIAN_POINT('Ctrl Pts',(0.14281802728161,-0.0330416298281342,
0.532125264226259));
#16966=CARTESIAN_POINT('Ctrl Pts',(0.153742154172479,0.0141764481069759,
0.53477265360052));
#16967=CARTESIAN_POINT('Ctrl Pts',(0.138930909478268,0.0673485266510362,
0.53742004297478));
#16968=CARTESIAN_POINT('Ctrl Pts',(0.105168604077417,0.102119062543277,
0.54006743234904));
#16969=CARTESIAN_POINT('Ctrl Pts',(0.0714062986765666,0.136889598435517,
0.5427148217233));
#16970=CARTESIAN_POINT('Ctrl Pts',(0.018692932569077,0.153258591675938,
0.545362211097559));
#16971=CARTESIAN_POINT('Ctrl Pts',(-0.0288260648428939,0.143728202535144,
0.548009600471819));
#16972=CARTESIAN_POINT('Ctrl Pts',(-0.0763450622548654,0.13419781339435,
0.550656989846079));
#16973=CARTESIAN_POINT('Ctrl Pts',(-0.118669690971318,0.0987680418723385,
0.55330437922034));
#16974=CARTESIAN_POINT('Ctrl Pts',(-0.136413096952957,0.0536675432455532,
0.5559517685946));
#16975=CARTESIAN_POINT('Ctrl Pts',(-0.143076734904351,0.036729792140314,
0.556946010868304));
#16976=CARTESIAN_POINT('Ctrl Pts',(-0.146273385252938,0.0184280612467595,
0.557940253142007));
#16977=CARTESIAN_POINT('Ctrl Pts',(-0.146168951232552,9.12430751481418E-5,
0.558934495415711));
#16978=CARTESIAN_POINT('Origin',(0.,0.,0.));
#16979=CARTESIAN_POINT('',(-0.146227179098081,-0.000117664897458569,0.616065504584291));
#16980=CARTESIAN_POINT('',(-0.146218520919543,-0.000115076211918358,0.608934495415711));
#16981=CARTESIAN_POINT('',(-0.14635,-1.79227059055215E-17,0.));
#16982=CARTESIAN_POINT('Ctrl Pts',(-0.146227179098081,-0.000117664897458569,
0.616065504584291));
#16983=CARTESIAN_POINT('Ctrl Pts',(-0.145977603365176,0.0329427899635141,
0.614271135524546));
#16984=CARTESIAN_POINT('Ctrl Pts',(-0.134874795495675,0.0661550248562671,
0.612476766464802));
#16985=CARTESIAN_POINT('Ctrl Pts',(-0.114309815624116,0.091770790457776,
0.610682397405058));
#16986=CARTESIAN_POINT('Ctrl Pts',(-0.0839806476072558,0.129548841477563,
0.608036067525956));
#16987=CARTESIAN_POINT('Ctrl Pts',(-0.0330710111925292,0.150804375664025,
0.605389737646855));
#16988=CARTESIAN_POINT('Ctrl Pts',(0.0151169520838501,0.145808400611758,
0.602743407767753));
#16989=CARTESIAN_POINT('Ctrl Pts',(0.0633049153602295,0.140812425559491,
0.600097077888651));
#16990=CARTESIAN_POINT('Ctrl Pts',(0.108771205498262,0.109564941268491,
0.597450748009549));
#16991=CARTESIAN_POINT('Ctrl Pts',(0.130705186191441,0.0663684129079872,
0.594804418130447));
#16992=CARTESIAN_POINT('Ctrl Pts',(0.152639166884621,0.023171884547483,
0.592158088251345));
#16993=CARTESIAN_POINT('Ctrl Pts',(0.151040838132949,-0.0319736878825246,
0.589511758372243));
#16994=CARTESIAN_POINT('Ctrl Pts',(0.126641780152193,-0.0738273082886534,
0.586865428493141));
#16995=CARTESIAN_POINT('Ctrl Pts',(0.102242722171437,-0.115680928694782,
0.584219098614039));
#16996=CARTESIAN_POINT('Ctrl Pts',(0.0550429349615966,-0.14424259707703,
0.581572768734937));
#16997=CARTESIAN_POINT('Ctrl Pts',(0.00664650371163741,-0.14643918846291,
0.578926438855836));
#16998=CARTESIAN_POINT('Ctrl Pts',(-0.0417499275383225,-0.148635779848789,
0.576280108976733));
#16999=CARTESIAN_POINT('Ctrl Pts',(-0.0913430028284016,-0.1244672942383,
0.573633779097631));
#17000=CARTESIAN_POINT('Ctrl Pts',(-0.119433191362276,-0.0849960277323969,
0.570987449218529));
#17001=CARTESIAN_POINT('Ctrl Pts',(-0.136848298201485,-0.0605249807527623,
0.569346801007117));
#17002=CARTESIAN_POINT('Ctrl Pts',(-0.145998464265635,-0.0301720919893573,
0.567706152795704));
#17003=CARTESIAN_POINT('Ctrl Pts',(-0.146165204287215,8.83645032875094E-5,
0.566065504584291));
#17004=CARTESIAN_POINT('Ctrl Pts',(-0.146168951232552,9.12430751481418E-5,
0.558934495415711));
#17005=CARTESIAN_POINT('Ctrl Pts',(-0.145995306636495,-0.0303977620653178,
0.560587642516267));
#17006=CARTESIAN_POINT('Ctrl Pts',(-0.136695352934655,-0.0609837708898569,
0.562240789616823));
#17007=CARTESIAN_POINT('Ctrl Pts',(-0.119031718004195,-0.0855580991331628,
0.563893936717379));
#17008=CARTESIAN_POINT('Ctrl Pts',(-0.090744749826965,-0.124912017153538,
0.566541326091639));
#17009=CARTESIAN_POINT('Ctrl Pts',(-0.0410086302256792,-0.148848627462727,
0.5691887154659));
#17010=CARTESIAN_POINT('Ctrl Pts',(0.00739494322942312,-0.146403732988417,
0.57183610484016));
#17011=CARTESIAN_POINT('Ctrl Pts',(0.0557985166845234,-0.143958838514108,
0.57448349421442));
#17012=CARTESIAN_POINT('Ctrl Pts',(0.10286954399344,-0.1151324392563,0.57713088358868));
#17013=CARTESIAN_POINT('Ctrl Pts',(0.127047076753504,-0.0731285067993286,
0.579778272962939));
#17014=CARTESIAN_POINT('Ctrl Pts',(0.151224609513568,-0.031124574342357,
0.5824256623372));
#17015=CARTESIAN_POINT('Ctrl Pts',(0.15250864772478,0.0240568913137802,
0.58507305171146));
#17016=CARTESIAN_POINT('Ctrl Pts',(0.130311035929276,0.0671399443948921,
0.58772044108572));
#17017=CARTESIAN_POINT('Ctrl Pts',(0.108113424133771,0.110222997476006,
0.59036783045998));
#17018=CARTESIAN_POINT('Ctrl Pts',(0.0624341623315493,0.141207637982093,
0.593015219834239));
#17019=CARTESIAN_POINT('Ctrl Pts',(0.0141966988324609,0.145901308974836,
0.595662609208499));
#17020=CARTESIAN_POINT('Ctrl Pts',(-0.0340407646666261,0.150594979967579,
0.598309998582759));
#17021=CARTESIAN_POINT('Ctrl Pts',(-0.0848364298625779,0.128997681446978,
0.60095738795702));
#17022=CARTESIAN_POINT('Ctrl Pts',(-0.114923272877171,0.091002085522857,
0.60360477733128));
#17023=CARTESIAN_POINT('Ctrl Pts',(-0.135113526827902,0.0655045372973676,
0.60538135002609));
#17024=CARTESIAN_POINT('Ctrl Pts',(-0.14597798884013,0.0326223532682757,
0.6071579227209));
#17025=CARTESIAN_POINT('Ctrl Pts',(-0.146218520919543,-0.000115076211918358,
0.608934495415711));
#17026=CARTESIAN_POINT('Origin',(0.,0.,0.));
#17027=CARTESIAN_POINT('',(-0.146586033401767,-2.15382961294558E-5,0.66606550458429));
#17028=CARTESIAN_POINT('',(-0.146582846697157,-3.00215943766004E-5,0.65893449541571));
#17029=CARTESIAN_POINT('',(-0.14635,-1.79227059055215E-17,0.));
#17030=CARTESIAN_POINT('Ctrl Pts',(-0.146586033401767,-2.15382961294558E-5,
0.66606550458429));
#17031=CARTESIAN_POINT('Ctrl Pts',(-0.146488810225965,0.0472697707580183,
0.663482448132491));
#17032=CARTESIAN_POINT('Ctrl Pts',(-0.121516563758978,0.0946492637554097,
0.660899391680692));
#17033=CARTESIAN_POINT('Ctrl Pts',(-0.0824084263440199,0.121233094478226,
0.658316335228893));
#17034=CARTESIAN_POINT('Ctrl Pts',(-0.0423423130056393,0.148468111155377,
0.655670005349791));
#17035=CARTESIAN_POINT('Ctrl Pts',(0.0125607065496858,0.153876184485078,
0.653023675470689));
#17036=CARTESIAN_POINT('Ctrl Pts',(0.0571706564953393,0.134981954220393,
0.650377345591587));
#17037=CARTESIAN_POINT('Ctrl Pts',(0.101780606440992,0.116087723955709,
0.647731015712485));
#17038=CARTESIAN_POINT('Ctrl Pts',(0.136097486776972,0.0728911900966409,
0.645084685833384));
#17039=CARTESIAN_POINT('Ctrl Pts',(0.144413921474191,0.0251640857912735,
0.642438355954282));
#17040=CARTESIAN_POINT('Ctrl Pts',(0.152730356171409,-0.0225630185140953,
0.63979202607518));
#17041=CARTESIAN_POINT('Ctrl Pts',(0.135046345229863,-0.0748206932657649,
0.637145696196077));
#17042=CARTESIAN_POINT('Ctrl Pts',(0.0994561386758346,-0.10768977857233,
0.634499366316975));
#17043=CARTESIAN_POINT('Ctrl Pts',(0.0638659321218069,-0.140558863878895,
0.631853036437873));
#17044=CARTESIAN_POINT('Ctrl Pts',(0.0103695299552984,-0.154039359740357,
0.629206706558772));
#17045=CARTESIAN_POINT('Ctrl Pts',(-0.0365469229059137,-0.141961031115491,
0.62656037667967));
#17046=CARTESIAN_POINT('Ctrl Pts',(-0.0834633757671259,-0.129882702490626,
0.623914046800568));
#17047=CARTESIAN_POINT('Ctrl Pts',(-0.123799879323041,-0.0922455493794331,
0.621267716921466));
#17048=CARTESIAN_POINT('Ctrl Pts',(-0.139093781291504,-0.0462766888972804,
0.618621387042364));
#17049=CARTESIAN_POINT('Ctrl Pts',(-0.14401750805555,-0.0314774500153124,
0.617769426223006));
#17050=CARTESIAN_POINT('Ctrl Pts',(-0.14634567687575,-0.0158146654998378,
0.616917465403648));
#17051=CARTESIAN_POINT('Ctrl Pts',(-0.146227179098081,-0.000117664897458569,
0.616065504584291));
#17052=CARTESIAN_POINT('Ctrl Pts',(-0.146218520919543,-0.000115076211918358,
0.608934495415711));
#17053=CARTESIAN_POINT('Ctrl Pts',(-0.1463364217222,-0.0161618722236638,
0.60980531209516));
#17054=CARTESIAN_POINT('Ctrl Pts',(-0.143901781624712,-0.032173889023867,
0.61067612877461));
#17055=CARTESIAN_POINT('Ctrl Pts',(-0.138761720114909,-0.0472643972675185,
0.611546945454059));
#17056=CARTESIAN_POINT('Ctrl Pts',(-0.123135303504819,-0.0931413908061287,
0.614194334828319));
#17057=CARTESIAN_POINT('Ctrl Pts',(-0.0825044494514074,-0.130501484555709,
0.616841724202579));
#17058=CARTESIAN_POINT('Ctrl Pts',(-0.0354801761942514,-0.142231836504824,
0.619489113576839));
#17059=CARTESIAN_POINT('Ctrl Pts',(0.0115440970629072,-0.15396218845394,
0.6221365029511));
#17060=CARTESIAN_POINT('Ctrl Pts',(0.0649617895238099,-0.140062798602586,
0.624783892325359));
#17061=CARTESIAN_POINT('Ctrl Pts',(0.100304854137336,-0.106900301471969,
0.627431281699619));
#17062=CARTESIAN_POINT('Ctrl Pts',(0.135647918750861,-0.0737378043413545,
0.630078671073879));
#17063=CARTESIAN_POINT('Ctrl Pts',(0.15291635551701,-0.0213121999314781,
0.63272606044814));
#17064=CARTESIAN_POINT('Ctrl Pts',(0.144200333369931,0.026362891994447,
0.6353734498224));
#17065=CARTESIAN_POINT('Ctrl Pts',(0.135484311222852,0.0740379839203748,
0.63802083919666));
#17066=CARTESIAN_POINT('Ctrl Pts',(0.100783830162543,0.11696256336235,0.640668228570919));
#17067=CARTESIAN_POINT('Ctrl Pts',(0.055993492972559,0.135474968031154,
0.643315617945179));
#17068=CARTESIAN_POINT('Ctrl Pts',(0.0112031557825773,0.153987372699956,
0.64596300731944));
#17069=CARTESIAN_POINT('Ctrl Pts',(-0.04367703753708,0.148087602595587,
0.6486103966937));
#17070=CARTESIAN_POINT('Ctrl Pts',(-0.0835091394177698,0.120478055479053,
0.65125778606796));
#17071=CARTESIAN_POINT('Ctrl Pts',(-0.122009894390588,0.0937913289882395,
0.653816689183877));
#17072=CARTESIAN_POINT('Ctrl Pts',(-0.146451680634158,0.0468218259492564,
0.656375592299793));
#17073=CARTESIAN_POINT('Ctrl Pts',(-0.146582846697157,-3.00215943766004E-5,
0.65893449541571));
#17074=CARTESIAN_POINT('Origin',(0.,0.,0.));
#17075=CARTESIAN_POINT('',(-0.146290249280603,0.000131112932912382,0.716065504584291));
#17076=CARTESIAN_POINT('',(-0.146307221518699,0.000133045872591754,0.708934495415711));
#17077=CARTESIAN_POINT('',(-0.14635,-1.79227059055215E-17,0.));
#17078=CARTESIAN_POINT('Ctrl Pts',(-0.146290249280603,0.000131112932912382,
0.716065504584291));
#17079=CARTESIAN_POINT('Ctrl Pts',(-0.146406294125046,0.0134819654399978,
0.715340090619538));
#17080=CARTESIAN_POINT('Ctrl Pts',(-0.144729088574721,0.0268041890186768,
0.714614676654786));
#17081=CARTESIAN_POINT('Ctrl Pts',(-0.141142411757643,0.0395908011096033,
0.713889262690033));
#17082=CARTESIAN_POINT('Ctrl Pts',(-0.128058117149462,0.0862367098911347,
0.711242932810931));
#17083=CARTESIAN_POINT('Ctrl Pts',(-0.0895623832093418,0.125754646095387,
0.708596602931829));
#17084=CARTESIAN_POINT('Ctrl Pts',(-0.0432753130058998,0.140056628595385,
0.705950273052727));
#17085=CARTESIAN_POINT('Ctrl Pts',(0.00301175719754219,0.154358611095384,
0.703303943173625));
#17086=CARTESIAN_POINT('Ctrl Pts',(0.0570901636643063,0.143444639891129,
0.700657613294523));
#17087=CARTESIAN_POINT('Ctrl Pts',(0.0942073689518517,0.11231021130972,
0.698011283415421));
#17088=CARTESIAN_POINT('Ctrl Pts',(0.131324574239397,0.0811757827283121,
0.695364953536319));
#17089=CARTESIAN_POINT('Ctrl Pts',(0.151480578347723,0.0298208967697505,
0.692718623657217));
#17090=CARTESIAN_POINT('Ctrl Pts',(0.145449661086834,-0.0182485073085286,
0.690072293778115));
#17091=CARTESIAN_POINT('Ctrl Pts',(0.139418743825945,-0.0663179113868083,
0.687425963899014));
#17092=CARTESIAN_POINT('Ctrl Pts',(0.107200905195838,-0.111101833584806,
0.684779634019911));
#17093=CARTESIAN_POINT('Ctrl Pts',(0.0635427568131047,-0.132101968137704,
0.68213330414081));
#17094=CARTESIAN_POINT('Ctrl Pts',(0.0198846084303716,-0.153102102690602,
0.679486974261708));
#17095=CARTESIAN_POINT('Ctrl Pts',(-0.0352138497049885,-0.150318449598402,
0.676840644382606));
#17096=CARTESIAN_POINT('Ctrl Pts',(-0.0765331864534889,-0.125025130675956,
0.674194314503504));
#17097=CARTESIAN_POINT('Ctrl Pts',(-0.117852523201989,-0.0997318117535095,
0.671547984624402));
#17098=CARTESIAN_POINT('Ctrl Pts',(-0.14539273856363,-0.0519288270008166,
0.6689016547453));
#17099=CARTESIAN_POINT('Ctrl Pts',(-0.146548242683733,-0.00349635461217019,
0.666255324866198));
#17100=CARTESIAN_POINT('Ctrl Pts',(-0.146575870647472,-0.00233834005587287,
0.666192051438896));
#17101=CARTESIAN_POINT('Ctrl Pts',(-0.146588414938392,-0.00117996563262623,
0.666128778011593));
#17102=CARTESIAN_POINT('Ctrl Pts',(-0.146586033401767,-2.15382961294558E-5,
0.66606550458429));
#17103=CARTESIAN_POINT('Ctrl Pts',(-0.146582846697157,-3.00215943766004E-5,
0.65893449541571));
#17104=CARTESIAN_POINT('Ctrl Pts',(-0.146587382388275,-0.00165014728799839,
0.659022981674053));
#17105=CARTESIAN_POINT('Ctrl Pts',(-0.146562848415234,-0.00327013229389975,
0.659111467932396));
#17106=CARTESIAN_POINT('Ctrl Pts',(-0.146508820881567,-0.00488913307276392,
0.659199954190739));
#17107=CARTESIAN_POINT('Ctrl Pts',(-0.144892390022949,-0.0533274503793473,
0.661847343564999));
#17108=CARTESIAN_POINT('Ctrl Pts',(-0.116875517863988,-0.100884760863813,
0.66449473293926));
#17109=CARTESIAN_POINT('Ctrl Pts',(-0.0752913709948059,-0.125777373450206,
0.66714212231352));
#17110=CARTESIAN_POINT('Ctrl Pts',(-0.0337072241256252,-0.150669986036599,
0.66978951168778));
#17111=CARTESIAN_POINT('Ctrl Pts',(0.021444197453776,-0.15289790072492,
0.672436901062039));
#17112=CARTESIAN_POINT('Ctrl Pts',(0.0649007096996251,-0.131440618146733,
0.675084290436299));
#17113=CARTESIAN_POINT('Ctrl Pts',(0.108357221945475,-0.109983335568545,
0.677731679810559));
#17114=CARTESIAN_POINT('Ctrl Pts',(0.140118824857774,-0.0648408557238465,
0.68037906918482));
#17115=CARTESIAN_POINT('Ctrl Pts',(0.145637072805965,-0.0166907532130915,
0.68302645855908));
#17116=CARTESIAN_POINT('Ctrl Pts',(0.151155320754156,0.031459349297663,
0.68567384793334));
#17117=CARTESIAN_POINT('Ctrl Pts',(0.130430213738242,0.0826170744744734,
0.688321237307599));
#17118=CARTESIAN_POINT('Ctrl Pts',(0.0929549153570804,0.113349556369966,
0.690968626681859));
#17119=CARTESIAN_POINT('Ctrl Pts',(0.0554796169759186,0.14408203826546,
0.693616016056119));
#17120=CARTESIAN_POINT('Ctrl Pts',(0.00125412722950909,0.154389276879634,
0.69626340543038));
#17121=CARTESIAN_POINT('Ctrl Pts',(-0.0448834941801804,0.139550027475769,
0.69891079480464));
#17122=CARTESIAN_POINT('Ctrl Pts',(-0.0910211155898686,0.124710778071904,
0.7015581841789));
#17123=CARTESIAN_POINT('Ctrl Pts',(-0.129070868662838,0.0847250406500019,
0.704205573553159));
#17124=CARTESIAN_POINT('Ctrl Pts',(-0.141604011991841,0.0379083368947344,
0.706852962927419));
#17125=CARTESIAN_POINT('Ctrl Pts',(-0.144888775625201,0.0256383259412015,
0.707546807090183));
#17126=CARTESIAN_POINT('Ctrl Pts',(-0.146420824649375,0.0128991016161637,
0.708240651252947));
#17127=CARTESIAN_POINT('Ctrl Pts',(-0.146307221518699,0.000133045872591754,
0.708934495415711));
#17128=CARTESIAN_POINT('Origin',(0.,0.,0.));
#17129=CARTESIAN_POINT('',(-0.1461301977291,-5.61458017395017E-5,0.766065504584291));
#17130=CARTESIAN_POINT('',(-0.14612241379348,-4.54149644099216E-5,0.758934495415711));
#17131=CARTESIAN_POINT('',(-0.14635,-1.79227059055215E-17,0.));
#17132=CARTESIAN_POINT('Ctrl Pts',(-0.1461301977291,-5.61458017395017E-5,
0.766065504584291));
#17133=CARTESIAN_POINT('Ctrl Pts',(-0.14603380141711,0.0278870014676159,
0.764551403227483));
#17134=CARTESIAN_POINT('Ctrl Pts',(-0.138327245009168,0.0558793842949389,
0.763037301870675));
#17135=CARTESIAN_POINT('Ctrl Pts',(-0.123350675409043,0.079203679241543,
0.761523200513867));
#17136=CARTESIAN_POINT('Ctrl Pts',(-0.0971747899961838,0.119969628197767,
0.758876870634766));
#17137=CARTESIAN_POINT('Ctrl Pts',(-0.048790709571801,0.146475657227381,
0.756230540755664));
#17138=CARTESIAN_POINT('Ctrl Pts',(-0.000344588961360588,0.146589539830481,
0.753584210876561));
#17139=CARTESIAN_POINT('Ctrl Pts',(0.0481015316490792,0.14670342243358,
0.750937880997459));
#17140=CARTESIAN_POINT('Ctrl Pts',(0.0966096924455767,0.120425158610167,
0.748291551118357));
#17141=CARTESIAN_POINT('Ctrl Pts',(0.122976945064223,0.0797827231418903,
0.745645221239255));
#17142=CARTESIAN_POINT('Ctrl Pts',(0.149344197682869,0.0391402876736125,
0.742998891360154));
#17143=CARTESIAN_POINT('Ctrl Pts',(0.153570542123663,-0.01586631943953,
0.740352561481052));
#17144=CARTESIAN_POINT('Ctrl Pts',(0.133721514043982,-0.0600597087159893,
0.73770623160195));
#17145=CARTESIAN_POINT('Ctrl Pts',(0.113872485964301,-0.104253097992448,
0.735059901722848));
#17146=CARTESIAN_POINT('Ctrl Pts',(0.0699480853641458,-0.137633269432224,
0.732413571843746));
#17147=CARTESIAN_POINT('Ctrl Pts',(0.0220532014503509,-0.144921593405036,
0.729767241964644));
#17148=CARTESIAN_POINT('Ctrl Pts',(-0.0258416824634434,-0.152209917377848,
0.727120912085542));
#17149=CARTESIAN_POINT('Ctrl Pts',(-0.0777070496908773,-0.133406393883698,
0.724474582206441));
#17150=CARTESIAN_POINT('Ctrl Pts',(-0.109803305666473,-0.0971176914572187,
0.721828252327339));
#17151=CARTESIAN_POINT('Ctrl Pts',(-0.133101311474982,-0.0707764758164216,
0.71990733641299));
#17152=CARTESIAN_POINT('Ctrl Pts',(-0.14598295937539,-0.0352223077304616,
0.71798642049864));
#17153=CARTESIAN_POINT('Ctrl Pts',(-0.146290249280603,0.000131112932912382,
0.716065504584291));
#17154=CARTESIAN_POINT('Ctrl Pts',(-0.146307221518699,0.000133045872591754,
0.708934495415711));
#17155=CARTESIAN_POINT('Ctrl Pts',(-0.145987367488279,-0.0358102803178394,
0.710888040627207));
#17156=CARTESIAN_POINT('Ctrl Pts',(-0.132622002370819,-0.0719663061161047,
0.712841585838703));
#17157=CARTESIAN_POINT('Ctrl Pts',(-0.1086007072861,-0.0984612847532928,
0.7147951310502));
#17158=CARTESIAN_POINT('Ctrl Pts',(-0.0760477256663158,-0.134366532557423,
0.71744252042446));
#17159=CARTESIAN_POINT('Ctrl Pts',(-0.0239252288417074,-0.152529358077047,
0.720089909798719));
#17160=CARTESIAN_POINT('Ctrl Pts',(0.0238920022682765,-0.144630254255197,
0.722737299172979));
#17161=CARTESIAN_POINT('Ctrl Pts',(0.071709233378259,-0.136731150433346,
0.725384688547239));
#17162=CARTESIAN_POINT('Ctrl Pts',(0.115221198773618,-0.102770117270024,
0.7280320779215));
#17163=CARTESIAN_POINT('Ctrl Pts',(0.134497183226257,-0.058303052428779,
0.730679467295759));
#17164=CARTESIAN_POINT('Ctrl Pts',(0.153773167678896,-0.0138359875875333,
0.733326856670019));
#17165=CARTESIAN_POINT('Ctrl Pts',(0.148813171188813,0.0411371089316358,
0.735974246044279));
#17166=CARTESIAN_POINT('Ctrl Pts',(0.121889126928366,0.0814357351225549,
0.738621635418539));
#17167=CARTESIAN_POINT('Ctrl Pts',(0.0949650826679194,0.121734361313473,
0.741269024792799));
#17168=CARTESIAN_POINT('Ctrl Pts',(0.0460769906371109,0.147358517176143,
0.74391641416706));
#17169=CARTESIAN_POINT('Ctrl Pts',(-0.00238189178169058,0.146571023090686,
0.74656380354132));
#17170=CARTESIAN_POINT('Ctrl Pts',(-0.0508407742004934,0.14578352900523,
0.74921119291558));
#17171=CARTESIAN_POINT('Ctrl Pts',(-0.0988704470072894,0.118584384971644,
0.751858582289839));
#17172=CARTESIAN_POINT('Ctrl Pts',(-0.124470852918682,0.0774321960944291,
0.754505971664099));
#17173=CARTESIAN_POINT('Ctrl Pts',(-0.138745545153454,0.0544858868428234,
0.75598214624797));
#17174=CARTESIAN_POINT('Ctrl Pts',(-0.146046671909043,0.027201385339783,
0.757458320831841));
#17175=CARTESIAN_POINT('Ctrl Pts',(-0.14612241379348,-4.54149644099216E-5,
0.758934495415711));
#17176=CARTESIAN_POINT('Origin',(0.,0.,0.));
#17177=CARTESIAN_POINT('',(-0.146495788566881,-0.000101744904923998,0.816065504584291));
#17178=CARTESIAN_POINT('',(-0.146473871348434,-0.000110945968026819,0.808934495415711));
#17179=CARTESIAN_POINT('',(-0.14635,-1.79227059055215E-17,0.));
#17180=CARTESIAN_POINT('Ctrl Pts',(-0.146495788566881,-0.000101744904923998,
0.816065504584291));
#17181=CARTESIAN_POINT('Ctrl Pts',(-0.14616118452328,0.0421270051992108,
0.813762715835428));
#17182=CARTESIAN_POINT('Ctrl Pts',(-0.126905337350145,0.0846218946815527,
0.811459927086565));
#17183=CARTESIAN_POINT('Ctrl Pts',(-0.0947343415465314,0.111866064832055,
0.809157138337701));
#17184=CARTESIAN_POINT('Ctrl Pts',(-0.0577639214515077,0.143174651664521,
0.806510808458599));
#17185=CARTESIAN_POINT('Ctrl Pts',(-0.00373742343573488,0.154342745753647,
0.803864478579497));
#17186=CARTESIAN_POINT('Ctrl Pts',(0.0426163743729279,0.140258534729872,
0.801218148700395));
#17187=CARTESIAN_POINT('Ctrl Pts',(0.0889701721815907,0.126174323706097,
0.798571818821294));
#17188=CARTESIAN_POINT('Ctrl Pts',(0.127651269783143,0.0868378075694234,
0.795925488942192));
#17189=CARTESIAN_POINT('Ctrl Pts',(0.140954720244851,0.040253928627653,
0.79327915906309));
#17190=CARTESIAN_POINT('Ctrl Pts',(0.154258170706558,-0.00632995031411615,
0.790632829183988));
#17191=CARTESIAN_POINT('Ctrl Pts',(0.14218397402842,-0.060161192060982,
0.787986499304886));
#17192=CARTESIAN_POINT('Ctrl Pts',(0.110258679990485,-0.0966003903512828,
0.785340169425784));
#17193=CARTESIAN_POINT('Ctrl Pts',(0.0783333859525485,-0.133039588641585,
0.782693839546682));
#17194=CARTESIAN_POINT('Ctrl Pts',(0.0265569945548152,-0.152086743475322,
0.780047509667581));
#17195=CARTESIAN_POINT('Ctrl Pts',(-0.021371625274328,-0.14502367242074,
0.777401179788479));
#17196=CARTESIAN_POINT('Ctrl Pts',(-0.0693002451034712,-0.137960601366157,
0.774754849909377));
#17197=CARTESIAN_POINT('Ctrl Pts',(-0.113381093364023,-0.104787304423254,
0.772108520030274));
#17198=CARTESIAN_POINT('Ctrl Pts',(-0.133437672293631,-0.0606877215103841,
0.769462190151172));
#17199=CARTESIAN_POINT('Ctrl Pts',(-0.1420188514214,-0.0418197768941368,
0.768329961628878));
#17200=CARTESIAN_POINT('Ctrl Pts',(-0.146202281842484,-0.0209517273285418,
0.767197733106584));
#17201=CARTESIAN_POINT('Ctrl Pts',(-0.1461301977291,-5.61458017395017E-5,
0.766065504584291));
#17202=CARTESIAN_POINT('Ctrl Pts',(-0.14612241379348,-4.54149644099216E-5,
0.758934495415711));
#17203=CARTESIAN_POINT('Ctrl Pts',(-0.146182508321779,-0.0216633562673834,
0.760105710206101));
#17204=CARTESIAN_POINT('Ctrl Pts',(-0.141694203021096,-0.0432575645610501,
0.76127692499649));
#17205=CARTESIAN_POINT('Ctrl Pts',(-0.132531725405586,-0.0626424774360703,
0.76244813978688));
#17206=CARTESIAN_POINT('Ctrl Pts',(-0.111821052965107,-0.106459728368519,
0.76509552916114));
#17207=CARTESIAN_POINT('Ctrl Pts',(-0.067228569068158,-0.138988996512573,
0.767742918535399));
#17208=CARTESIAN_POINT('Ctrl Pts',(-0.0191799219195066,-0.145330206128911,
0.770390307909659));
#17209=CARTESIAN_POINT('Ctrl Pts',(0.0288687252291434,-0.151671415745249,
0.773037697283919));
#17210=CARTESIAN_POINT('Ctrl Pts',(0.080373535629496,-0.131824566833873,
0.77568508665818));
#17211=CARTESIAN_POINT('Ctrl Pts',(0.111742660473083,-0.0948805356683208,
0.77833247603244));
#17212=CARTESIAN_POINT('Ctrl Pts',(0.14311178531667,-0.0579365045027684,
0.7809798654067));
#17213=CARTESIAN_POINT('Ctrl Pts',(0.154345224603492,-0.00389529108304171,
0.783627254780959));
#17214=CARTESIAN_POINT('Ctrl Pts',(0.140297486112651,0.0424894529122293,
0.786274644155219));
#17215=CARTESIAN_POINT('Ctrl Pts',(0.126249747621811,0.0888741969075009,
0.788922033529479));
#17216=CARTESIAN_POINT('Ctrl Pts',(0.0869208313533056,0.127602471478316,
0.79156942290374));
#17217=CARTESIAN_POINT('Ctrl Pts',(0.0403254011646538,0.140934737517831,
0.794216812278));
#17218=CARTESIAN_POINT('Ctrl Pts',(-0.00627002902399674,0.154267003557346,
0.79686420165226));
#17219=CARTESIAN_POINT('Ctrl Pts',(-0.0601319731327944,0.142203261065564,
0.799511591026519));
#17220=CARTESIAN_POINT('Ctrl Pts',(-0.0965888940360299,0.110269323781398,
0.802158980400779));
#17221=CARTESIAN_POINT('Ctrl Pts',(-0.127690529151203,0.0830262752573849,
0.804417485405756));
#17222=CARTESIAN_POINT('Ctrl Pts',(-0.146124951115714,0.0413218847513699,
0.806675990410734));
#17223=CARTESIAN_POINT('Ctrl Pts',(-0.146473871348434,-0.000110945968026819,
0.808934495415711));
#17224=CARTESIAN_POINT('Origin',(0.,0.,0.));
#17225=CARTESIAN_POINT('',(-0.146444331750498,0.000119944961782359,0.866065504584291));
#17226=CARTESIAN_POINT('',(-0.146471560192382,0.00011177640072981,0.858934495415711));
#17227=CARTESIAN_POINT('',(-0.14635,-1.79227059055215E-17,0.));
#17228=CARTESIAN_POINT('Ctrl Pts',(-0.146444331750498,0.000119944961782359,
0.866065504584291));
#17229=CARTESIAN_POINT('Ctrl Pts',(-0.146516681599632,0.00829054204730037,
0.865620358322474));
#17230=CARTESIAN_POINT('Ctrl Pts',(-0.145891801779796,0.0164500693154795,
0.865175212060658));
#17231=CARTESIAN_POINT('Ctrl Pts',(-0.14453063157077,0.0244848619971339,
0.864730065798841));
#17232=CARTESIAN_POINT('Ctrl Pts',(-0.136438672357208,0.0722505376181754,
0.862083735919739));
#17233=CARTESIAN_POINT('Ctrl Pts',(-0.102325254887189,0.115607931012472,
0.859437406040638));
#17234=CARTESIAN_POINT('Ctrl Pts',(-0.0578046270350215,0.134711681091902,
0.856791076161536));
#17235=CARTESIAN_POINT('Ctrl Pts',(-0.0132839991828526,0.153815431171333,
0.854144746282434));
#17236=CARTESIAN_POINT('Ctrl Pts',(0.0416438390514653,0.148665537935894,
0.851498416403331));
#17237=CARTESIAN_POINT('Ctrl Pts',(0.081837551941475,0.121619188541491,
0.848852086524229));
#17238=CARTESIAN_POINT('Ctrl Pts',(0.122031264831484,0.0945728391470885,
0.846205756645128));
#17239=CARTESIAN_POINT('Ctrl Pts',(0.147490852377186,0.0456300335937214,
0.843559426766026));
#17240=CARTESIAN_POINT('Ctrl Pts',(0.146563060809277,-0.0028073360113171,
0.840913096886925));
#17241=CARTESIAN_POINT('Ctrl Pts',(0.145635269241369,-0.0512447056163556,
0.838266767007823));
#17242=CARTESIAN_POINT('Ctrl Pts',(0.118320098559852,-0.0991766392730661,
0.835620437128721));
#17243=CARTESIAN_POINT('Ctrl Pts',(0.0771201321287374,-0.124663936845065,
0.832974107249619));
#17244=CARTESIAN_POINT('Ctrl Pts',(0.035920165697623,-0.150151234417064,
0.830327777370517));
#17245=CARTESIAN_POINT('Ctrl Pts',(-0.0191645964830881,-0.153193895904352,
0.827681447491415));
#17246=CARTESIAN_POINT('Ctrl Pts',(-0.0629209921278279,-0.132399247274726,
0.825035117612313));
#17247=CARTESIAN_POINT('Ctrl Pts',(-0.106677387772568,-0.111604598645101,
0.822388787733211));
#17248=CARTESIAN_POINT('Ctrl Pts',(-0.139105416881337,-0.0669726398985626,
0.819742457854109));
#17249=CARTESIAN_POINT('Ctrl Pts',(-0.145362260348583,-0.0189321207373897,
0.817096127975007));
#17250=CARTESIAN_POINT('Ctrl Pts',(-0.146174510965348,-0.0126955988357878,
0.816752586844768));
#17251=CARTESIAN_POINT('Ctrl Pts',(-0.146545706411658,-0.00640163348415362,
0.81640904571453));
#17252=CARTESIAN_POINT('Ctrl Pts',(-0.146495788566881,-0.000101744904923998,
0.816065504584291));
#17253=CARTESIAN_POINT('Ctrl Pts',(-0.146473871348434,-0.000110945968026819,
0.808934495415711));
#17254=CARTESIAN_POINT('Ctrl Pts',(-0.146533950748007,-0.00724512552769256,
0.809323379784994));
#17255=CARTESIAN_POINT('Ctrl Pts',(-0.146057826922151,-0.0143712538186879,
0.809712264154277));
#17256=CARTESIAN_POINT('Ctrl Pts',(-0.145017839345608,-0.0214141189368497,
0.81010114852356));
#17257=CARTESIAN_POINT('Ctrl Pts',(-0.137937966054276,-0.0693594922943736,
0.81274853789782));
#17258=CARTESIAN_POINT('Ctrl Pts',(-0.104726321773939,-0.113446106932874,
0.81539592727208));
#17259=CARTESIAN_POINT('Ctrl Pts',(-0.0605955455659204,-0.133480028752914,
0.818043316646339));
#17260=CARTESIAN_POINT('Ctrl Pts',(-0.0164647693578984,-0.153513950572954,
0.820690706020599));
#17261=CARTESIAN_POINT('Ctrl Pts',(0.0385851387778066,-0.149495179574532,
0.823338095394859));
#17262=CARTESIAN_POINT('Ctrl Pts',(0.0793384931690736,-0.12326451930694,
0.825985484769119));
#17263=CARTESIAN_POINT('Ctrl Pts',(0.120091847560339,-0.0970338590393495,
0.828632874143379));
#17264=CARTESIAN_POINT('Ctrl Pts',(0.146548648207165,-0.0485913095025905,
0.83128026351764));
#17265=CARTESIAN_POINT('Ctrl Pts',(0.146590321408106,-0.000126046730599388,
0.833927652891899));
#17266=CARTESIAN_POINT('Ctrl Pts',(0.146631994609047,0.0483392160413931,
0.836575042266159));
#17267=CARTESIAN_POINT('Ctrl Pts',(0.120258540364101,0.0968271920486179,
0.839222431640419));
#17268=CARTESIAN_POINT('Ctrl Pts',(0.0795503554414038,0.123127897600245,
0.841869821014679));
#17269=CARTESIAN_POINT('Ctrl Pts',(0.0388421705187073,0.149428603151872,
0.844517210388939));
#17270=CARTESIAN_POINT('Ctrl Pts',(-0.0162007450817403,0.153542038247903,
0.8471645997632));
#17271=CARTESIAN_POINT('Ctrl Pts',(-0.0603659086281491,0.133584038319734,
0.84981198913746));
#17272=CARTESIAN_POINT('Ctrl Pts',(-0.104531072174558,0.113626038391565,
0.85245937851172));
#17273=CARTESIAN_POINT('Ctrl Pts',(-0.137818483666928,0.0695966034391962,
0.855106767885979));
#17274=CARTESIAN_POINT('Ctrl Pts',(-0.144980798768897,0.0216634763286692,
0.857754157260239));
#17275=CARTESIAN_POINT('Ctrl Pts',(-0.146045237806912,0.0145398171508471,
0.858147603312063));
#17276=CARTESIAN_POINT('Ctrl Pts',(-0.146532654486068,0.00732993751956911,
0.858541049363887));
#17277=CARTESIAN_POINT('Ctrl Pts',(-0.146471560192382,0.00011177640072981,
0.858934495415711));
#17278=CARTESIAN_POINT('Origin',(0.,0.,0.));
#17279=CARTESIAN_POINT('',(-0.146114231148477,2.69008449349656E-5,0.916065504584291));
#17280=CARTESIAN_POINT('',(-0.146121644853617,4.41067432152685E-5,0.908934495415711));
#17281=CARTESIAN_POINT('',(-0.14635,-1.79227059055215E-17,0.));
#17282=CARTESIAN_POINT('Ctrl Pts',(-0.146114231148477,2.69008449349656E-5,
0.916065504584291));
#17283=CARTESIAN_POINT('Ctrl Pts',(-0.146151635159142,0.0228038459942234,
0.914831670930419));
#17284=CARTESIAN_POINT('Ctrl Pts',(-0.141147538069067,0.0455652341090756,
0.913597837276548));
#17285=CARTESIAN_POINT('Ctrl Pts',(-0.131015765267123,0.0657531838068269,
0.912364003622676));
#17286=CARTESIAN_POINT('Ctrl Pts',(-0.109285110563454,0.109052354902802,
0.909717673743574));
#17287=CARTESIAN_POINT('Ctrl Pts',(-0.0639662294071284,0.140513248471977,
0.907071343864472));
#17288=CARTESIAN_POINT('Ctrl Pts',(-0.015802286694576,0.145735718560985,
0.90442501398537));
#17289=CARTESIAN_POINT('Ctrl Pts',(0.0323616560179757,0.150958188649994,
0.901778684106268));
#17290=CARTESIAN_POINT('Ctrl Pts',(0.0833706602867547,0.129942235258839,
0.899132354227166));
#17291=CARTESIAN_POINT('Ctrl Pts',(0.113877102345416,0.0923071908936453,
0.896486024348064));
#17292=CARTESIAN_POINT('Ctrl Pts',(0.144383544404078,0.0546721465284523,
0.893839694468962));
#17293=CARTESIAN_POINT('Ctrl Pts',(0.15438742425262,0.000418011189221586,
0.891193364589861));
#17294=CARTESIAN_POINT('Ctrl Pts',(0.139309808695705,-0.0456222438118789,
0.888547034710759));
#17295=CARTESIAN_POINT('Ctrl Pts',(0.124232193138789,-0.0916624988129813,
0.885900704831657));
#17296=CARTESIAN_POINT('Ctrl Pts',(0.0840730821764119,-0.129488873475953,
0.883254374952555));
#17297=CARTESIAN_POINT('Ctrl Pts',(0.0372139327097935,-0.141787641004198,
0.880608045073453));
#17298=CARTESIAN_POINT('Ctrl Pts',(-0.00964521675682358,-0.154086408532443,
0.877961715194351));
#17299=CARTESIAN_POINT('Ctrl Pts',(-0.0632044047276821,-0.140857568925962,
0.875315385315249));
#17300=CARTESIAN_POINT('Ctrl Pts',(-0.0989487482345592,-0.108156170198829,
0.872669055436147));
#17301=CARTESIAN_POINT('Ctrl Pts',(-0.128680439645858,-0.0809555616469925,
0.870467871818862));
#17302=CARTESIAN_POINT('Ctrl Pts',(-0.146086572253705,-0.0402824710322022,
0.868266688201576));
#17303=CARTESIAN_POINT('Ctrl Pts',(-0.146444331750498,0.000119944961782359,
0.866065504584291));
#17304=CARTESIAN_POINT('Ctrl Pts',(-0.146471560192382,0.00011177640072981,
0.858934495415711));
#17305=CARTESIAN_POINT('Ctrl Pts',(-0.146121567926216,-0.0412390669452651,
0.861188438738147));
#17306=CARTESIAN_POINT('Ctrl Pts',(-0.127770397964496,-0.0828616943330661,
0.863442382060584));
#17307=CARTESIAN_POINT('Ctrl Pts',(-0.096778382793969,-0.110103055552942,
0.86569632538302));
#17308=CARTESIAN_POINT('Ctrl Pts',(-0.0603764330055066,-0.142099641055337,
0.86834371475728));
#17309=CARTESIAN_POINT('Ctrl Pts',(-0.00653531471701479,-0.154255992791443,
0.870991104131539));
#17310=CARTESIAN_POINT('Ctrl Pts',(0.040082974241256,-0.14100387723139,
0.873638493505799));
#17311=CARTESIAN_POINT('Ctrl Pts',(0.0867012631995282,-0.127751761671338,
0.876285882880059));
#17312=CARTESIAN_POINT('Ctrl Pts',(0.12609672282758,-0.0890911788151255,
0.878933272254319));
#17313=CARTESIAN_POINT('Ctrl Pts',(0.140224208991091,-0.042730661487191,
0.88158066162858));
#17314=CARTESIAN_POINT('Ctrl Pts',(0.154351695154603,0.00362985584074295,
0.88422805100284));
#17315=CARTESIAN_POINT('Ctrl Pts',(0.143211207853577,0.057690307640398,
0.886875440377099));
#17316=CARTESIAN_POINT('Ctrl Pts',(0.111905662524754,0.09468823006692,0.889522829751359));
#17317=CARTESIAN_POINT('Ctrl Pts',(0.0806001171959318,0.131686152493442,
0.892170219125619));
#17318=CARTESIAN_POINT('Ctrl Pts',(0.0291295138393125,0.15162154554683,
0.894817608499879));
#17319=CARTESIAN_POINT('Ctrl Pts',(-0.0189299673197759,0.145362975188259,
0.897464997874139));
#17320=CARTESIAN_POINT('Ctrl Pts',(-0.0669894484788628,0.139104404829688,
0.9001123872484));
#17321=CARTESIAN_POINT('Ctrl Pts',(-0.11163780744042,0.10665187105916,0.902759776622659));
#17322=CARTESIAN_POINT('Ctrl Pts',(-0.132423802349956,0.0628703013313112,
0.905407165996919));
#17323=CARTESIAN_POINT('Ctrl Pts',(-0.141655418982822,0.043425734493323,
0.90658294246985));
#17324=CARTESIAN_POINT('Ctrl Pts',(-0.146180218154578,0.0217465313827003,
0.907758718942781));
#17325=CARTESIAN_POINT('Ctrl Pts',(-0.146121644853617,4.41067432152685E-5,
0.908934495415711));
#17326=CARTESIAN_POINT('Origin',(0.,0.,0.));
#17327=CARTESIAN_POINT('',(-0.146345621585321,-0.000133809880645736,0.966065504584291));
#17328=CARTESIAN_POINT('',(-0.146309694201085,-0.000133223314395004,0.958934495415711));
#17329=CARTESIAN_POINT('',(-0.14635,-1.79227059055215E-17,0.));
#17330=CARTESIAN_POINT('Ctrl Pts',(-0.146345621585321,-0.000133809880645736,
0.966065504584291));
#17331=CARTESIAN_POINT('Ctrl Pts',(-0.146004672532387,0.0370537288701324,
0.964042983538364));
#17332=CARTESIAN_POINT('Ctrl Pts',(-0.131578083002406,0.0744765756810296,
0.962020462492437));
#17333=CARTESIAN_POINT('Ctrl Pts',(-0.106003654037246,0.101251356830495,
0.959997941446511));
#17334=CARTESIAN_POINT('Ctrl Pts',(-0.0725412702228666,0.136284319036219,
0.957351611567409));
#17335=CARTESIAN_POINT('Ctrl Pts',(-0.0199938687303381,0.153087872523943,
0.954705281688306));
#17336=CARTESIAN_POINT('Ctrl Pts',(0.0275867780614433,0.143970766496025,
0.952058951809204));
#17337=CARTESIAN_POINT('Ctrl Pts',(0.0751674248532248,0.134853660468108,
0.949412621930102));
#17338=CARTESIAN_POINT('Ctrl Pts',(0.11778131694426,0.0998158949245492,
0.946766292051));
#17339=CARTESIAN_POINT('Ctrl Pts',(0.135923405490256,0.0548948063954655,
0.944119962171899));
#17340=CARTESIAN_POINT('Ctrl Pts',(0.154065494036253,0.0099737178663825,
0.941473632292797));
#17341=CARTESIAN_POINT('Ctrl Pts',(0.147735779037212,-0.0448306936482241,
0.938827302413695));
#17342=CARTESIAN_POINT('Ctrl Pts',(0.119831470632095,-0.0844335867733556,
0.936180972534593));
#17343=CARTESIAN_POINT('Ctrl Pts',(0.0919271622269763,-0.124036479898489,
0.933534642655491));
#17344=CARTESIAN_POINT('Ctrl Pts',(0.0424482604157787,-0.148437854634144,
0.93088831277639));
#17345=CARTESIAN_POINT('Ctrl Pts',(-0.00595796300272124,-0.146468817862788,
0.928241982897288));
#17346=CARTESIAN_POINT('Ctrl Pts',(-0.0543641864212212,-0.144499781091432,
0.925595653018186));
#17347=CARTESIAN_POINT('Ctrl Pts',(-0.101697731447024,-0.116160332813065,
0.922949323139084));
#17348=CARTESIAN_POINT('Ctrl Pts',(-0.126293289834417,-0.0744218843624929,
0.920302993259982));
#17349=CARTESIAN_POINT('Ctrl Pts',(-0.139421333187579,-0.052143709087005,
0.918890497034752));
#17350=CARTESIAN_POINT('Ctrl Pts',(-0.146071410932229,-0.0260482098028304,
0.917478000809521));
#17351=CARTESIAN_POINT('Ctrl Pts',(-0.146114231148477,2.69008449349656E-5,
0.916065504584291));
#17352=CARTESIAN_POINT('Ctrl Pts',(-0.146121644853617,4.41067432152685E-5,
0.908934495415711));
#17353=CARTESIAN_POINT('Ctrl Pts',(-0.146048333958771,-0.027118852224649,
0.910406108317041));
#17354=CARTESIAN_POINT('Ctrl Pts',(-0.138795050353101,-0.0543181883240968,
0.91187772121837));
#17355=CARTESIAN_POINT('Ctrl Pts',(-0.124603830013468,-0.0772180274565794,
0.9133493341197));
#17356=CARTESIAN_POINT('Ctrl Pts',(-0.0990742319099257,-0.118414180831446,
0.91599672349396));
#17357=CARTESIAN_POINT('Ctrl Pts',(-0.0510914048453256,-0.145695881896007,
0.91864411286822));
#17358=CARTESIAN_POINT('Ctrl Pts',(-0.00263394834681351,-0.146566710184873,
0.92129150224248));
#17359=CARTESIAN_POINT('Ctrl Pts',(0.0458235081516972,-0.147437538473739,
0.92393889161674));
#17360=CARTESIAN_POINT('Ctrl Pts',(0.0947555940841207,-0.121897493986912,
0.926586280990999));
#17361=CARTESIAN_POINT('Ctrl Pts',(0.121748900601314,-0.0816452290135895,
0.929233670365259));
#17362=CARTESIAN_POINT('Ctrl Pts',(0.148742207118509,-0.0413929640402651,
0.931881059739519));
#17363=CARTESIAN_POINT('Ctrl Pts',(0.153796734220472,0.0135715214195569,
0.93452844911378));
#17364=CARTESIAN_POINT('Ctrl Pts',(0.134597248858856,0.0580716696672091,
0.93717583848804));
#17365=CARTESIAN_POINT('Ctrl Pts',(0.115397763497239,0.102571817914861,
0.9398232278623));
#17366=CARTESIAN_POINT('Ctrl Pts',(0.0719442656720451,0.136607628950342,
0.942470617236559));
#17367=CARTESIAN_POINT('Ctrl Pts',(0.0241406894609324,0.144588953003544,
0.945118006610819));
#17368=CARTESIAN_POINT('Ctrl Pts',(-0.023662886750181,0.152570277056746,
0.947765395985079));
#17369=CARTESIAN_POINT('Ctrl Pts',(-0.0758165413472122,0.134497114127667,
0.950412785359339));
#17370=CARTESIAN_POINT('Ctrl Pts',(-0.108431221550465,0.0986479012011113,
0.953060174733599));
#17371=CARTESIAN_POINT('Ctrl Pts',(-0.132554242808212,0.0721325001574252,
0.955018281627637));
#17372=CARTESIAN_POINT('Ctrl Pts',(-0.145988218858404,0.0358924841874147,
0.956976388521674));
#17373=CARTESIAN_POINT('Ctrl Pts',(-0.146309694201085,-0.000133223314395004,
0.958934495415711));
#17374=CARTESIAN_POINT('Origin',(0.,0.,0.));
#17375=CARTESIAN_POINT('',(-0.146565171121453,5.44893591410845E-5,1.01606550458429));
#17376=CARTESIAN_POINT('',(-0.146582076026177,3.15354312248815E-5,1.00893449541571));
#17377=CARTESIAN_POINT('',(-0.14635,-1.79227059055215E-17,0.));
#17378=CARTESIAN_POINT('Ctrl Pts',(-0.146565171121453,5.44893591410845E-5,
1.01606550458429));
#17379=CARTESIAN_POINT('Ctrl Pts',(-0.146579596851449,0.00307427920823236,
1.01590062602541));
#17380=CARTESIAN_POINT('Ctrl Pts',(-0.146494352296349,0.00609323927190738,
1.01573574746653));
#17381=CARTESIAN_POINT('Ctrl Pts',(-0.146306854564556,0.00910583530985269,
1.01557086890765));
#17382=CARTESIAN_POINT('Ctrl Pts',(-0.143297482980539,0.0574585317612167,
1.01292453902855));
#17383=CARTESIAN_POINT('Ctrl Pts',(-0.11394685994478,0.104171803331984,
1.01027820914945));
#17384=CARTESIAN_POINT('Ctrl Pts',(-0.0716892273871119,0.127864250695428,
1.00763187927034));
#17385=CARTESIAN_POINT('Ctrl Pts',(-0.0294315948294418,0.151556698058874,
1.00498554939124));
#17386=CARTESIAN_POINT('Ctrl Pts',(0.0257330472501378,0.152228321214993,
1.00233921951214));
#17387=CARTESIAN_POINT('Ctrl Pts',(0.0685549742796134,0.129571707678744,
0.999692889633039));
#17388=CARTESIAN_POINT('Ctrl Pts',(0.111376901309088,0.106915094142495,
0.997046559753937));
#17389=CARTESIAN_POINT('Ctrl Pts',(0.141856113288459,0.0609302439138786,
0.994400229874835));
#17390=CARTESIAN_POINT('Ctrl Pts',(0.146041795372579,0.0126651464112397,
0.991753899995733));
#17391=CARTESIAN_POINT('Ctrl Pts',(0.150227477456699,-0.0355999510913994,
0.989107570116631));
#17392=CARTESIAN_POINT('Ctrl Pts',(0.128119629645567,-0.0861452958680607,
0.986461240237529));
#17393=CARTESIAN_POINT('Ctrl Pts',(0.0898373616998479,-0.115835488396583,
0.983814910358427));
#17394=CARTESIAN_POINT('Ctrl Pts',(0.051555093754129,-0.145525680925106,
0.981168580479325));
#17395=CARTESIAN_POINT('Ctrl Pts',(-0.00290159432617693,-0.154360721205491,
0.978522250600224));
#17396=CARTESIAN_POINT('Ctrl Pts',(-0.0486070196525971,-0.138296672301818,
0.975875920721122));
#17397=CARTESIAN_POINT('Ctrl Pts',(-0.0943124449790173,-0.122232623398145,
0.97322959084202));
#17398=CARTESIAN_POINT('Ctrl Pts',(-0.131266607551552,-0.081269485310415,
0.970583260962917));
#17399=CARTESIAN_POINT('Ctrl Pts',(-0.142555005769704,-0.0341567308046872,
0.967936931083816));
#17400=CARTESIAN_POINT('Ctrl Pts',(-0.145215975052668,-0.0230510282813687,
0.967313122250641));
#17401=CARTESIAN_POINT('Ctrl Pts',(-0.146450780951306,-0.0116036114945705,
0.966689313417466));
#17402=CARTESIAN_POINT('Ctrl Pts',(-0.146345621585321,-0.000133809880645736,
0.966065504584291));
#17403=CARTESIAN_POINT('Ctrl Pts',(-0.146309694201085,-0.000133223314395004,
0.958934495415711));
#17404=CARTESIAN_POINT('Ctrl Pts',(-0.146422858258782,-0.0128148032088542,
0.959623777895933));
#17405=CARTESIAN_POINT('Ctrl Pts',(-0.14491119500038,-0.0254698272036438,
0.960313060376156));
#17406=CARTESIAN_POINT('Ctrl Pts',(-0.141668994059001,-0.037664762585484,
0.961002342856379));
#17407=CARTESIAN_POINT('Ctrl Pts',(-0.129216380554811,-0.0845029505214961,
0.963649732230639));
#17408=CARTESIAN_POINT('Ctrl Pts',(-0.0912354477369537,-0.12455406346949,
0.966297121604899));
#17409=CARTESIAN_POINT('Ctrl Pts',(-0.0451234138007503,-0.1394726343957,
0.968944510979159));
#17410=CARTESIAN_POINT('Ctrl Pts',(0.00098862013545236,-0.154391205321909,
0.97159190035342));
#17411=CARTESIAN_POINT('Ctrl Pts',(0.055231755190001,-0.144177234226336,
0.974239289727679));
#17412=CARTESIAN_POINT('Ctrl Pts',(0.0927598492034174,-0.113509244531313,
0.976886679101939));
#17413=CARTESIAN_POINT('Ctrl Pts',(0.130287943216833,-0.0828412548362905,
0.979534068476199));
#17414=CARTESIAN_POINT('Ctrl Pts',(0.151100996189117,-0.0317192465418168,
0.982181457850459));
#17415=CARTESIAN_POINT('Ctrl Pts',(0.145665560755875,0.0164402745715088,
0.984828847224719));
#17416=CARTESIAN_POINT('Ctrl Pts',(0.140230125322634,0.0645997956848379,
0.987476236598979));
#17417=CARTESIAN_POINT('Ctrl Pts',(0.108546201483865,0.109796829617019,
0.990123625973239));
#17418=CARTESIAN_POINT('Ctrl Pts',(0.0651266538643092,0.131328813193254,
0.992771015347499));
#17419=CARTESIAN_POINT('Ctrl Pts',(0.0217071062447581,0.152860796769488,
0.995418404721759));
#17420=CARTESIAN_POINT('Ctrl Pts',(-0.0334480651555777,0.15072772998978,
0.998065794096019));
#17421=CARTESIAN_POINT('Ctrl Pts',(-0.0750749586823209,0.125906667008376,
1.00071318347028));
#17422=CARTESIAN_POINT('Ctrl Pts',(-0.116701852209067,0.101085604026969,
1.00336057284454));
#17423=CARTESIAN_POINT('Ctrl Pts',(-0.144800467862219,0.053576544843864,
1.0060079622188));
#17424=CARTESIAN_POINT('Ctrl Pts',(-0.146500196332402,0.00514107896046776,
1.00865535159306));
#17425=CARTESIAN_POINT('Ctrl Pts',(-0.146559936783033,0.00343871495990628,
1.00874839953394));
#17426=CARTESIAN_POINT('Ctrl Pts',(-0.146587066279139,0.00173520655478852,
1.00884144747483));
#17427=CARTESIAN_POINT('Ctrl Pts',(-0.146582076026177,3.15354312248815E-5,
1.00893449541571));
#17428=CARTESIAN_POINT('Origin',(0.,0.,0.));
#17429=CARTESIAN_POINT('',(-0.146184049129756,9.96948043307314E-5,1.06606550458429));
#17430=CARTESIAN_POINT('',(-0.146216477546812,0.000114345603752017,1.05893449541571));
#17431=CARTESIAN_POINT('',(-0.14635,-1.79227059055215E-17,0.));
#17432=CARTESIAN_POINT('Ctrl Pts',(-0.146184049129756,9.96948043307314E-5,
1.06606550458429));
#17433=CARTESIAN_POINT('Ctrl Pts',(-0.146294264763128,0.0176817746259609,
1.06511193863336));
#17434=CARTESIAN_POINT('Ctrl Pts',(-0.143360807533043,0.0352283113603788,
1.06415837268242));
#17435=CARTESIAN_POINT('Ctrl Pts',(-0.13721959397524,0.0515693218739058,
1.06320480673148));
#17436=CARTESIAN_POINT('Ctrl Pts',(-0.120176538991979,0.0969187854681546,
1.06055847685238));
#17437=CARTESIAN_POINT('Ctrl Pts',(-0.0784283132238915,0.132983650068601,
1.05791214697328));
#17438=CARTESIAN_POINT('Ctrl Pts',(-0.0310837364199337,0.143256459747686,
1.05526581709418));
#17439=CARTESIAN_POINT('Ctrl Pts',(0.0162608403840241,0.153529269426771,
1.05261948721508));
#17440=CARTESIAN_POINT('Ctrl Pts',(0.0692017682238519,0.138010024184496,
1.04997315733597));
#17441=CARTESIAN_POINT('Ctrl Pts',(0.103507151520239,0.103802126728842,
1.04732682745687));
#17442=CARTESIAN_POINT('Ctrl Pts',(0.137812534816628,0.0695942292731864,
1.04468049757777));
#17443=CARTESIAN_POINT('Ctrl Pts',(0.153482373569574,0.01669767960415,1.04203416769867));
#17444=CARTESIAN_POINT('Ctrl Pts',(0.143344336052008,-0.0306759392859165,
1.03938783781957));
#17445=CARTESIAN_POINT('Ctrl Pts',(0.133206298534443,-0.0780495581759789,
1.03674150794047));
#17446=CARTESIAN_POINT('Ctrl Pts',(0.0972603847463712,-0.119900246287072,
1.03409517806136));
#17447=CARTESIAN_POINT('Ctrl Pts',(0.0519596049571008,-0.137072285243832,
1.03144884818226));
#17448=CARTESIAN_POINT('Ctrl Pts',(0.00665882516783032,-0.154244324200591,
1.02880251830316));
#17449=CARTESIAN_POINT('Ctrl Pts',(-0.0479968206226384,-0.146737714003016,
1.02615618842406));
#17450=CARTESIAN_POINT('Ctrl Pts',(-0.0869905834517384,-0.11798834823825,
1.02350985854496));
#17451=CARTESIAN_POINT('Ctrl Pts',(-0.123554854979944,-0.0910302005802824,
1.02102840722473));
#17452=CARTESIAN_POINT('Ctrl Pts',(-0.146348061346918,-0.0453938791777224,
1.01854695590451));
#17453=CARTESIAN_POINT('Ctrl Pts',(-0.146565171121453,5.44893591410845E-5,
1.01606550458429));
#17454=CARTESIAN_POINT('Ctrl Pts',(-0.146582076026177,3.15354312248815E-5,
1.00893449541571));
#17455=CARTESIAN_POINT('Ctrl Pts',(-0.146445084172466,-0.0467374494427972,
1.01148883684909));
#17456=CARTESIAN_POINT('Ctrl Pts',(-0.122102455869861,-0.0936290599181376,
1.01404317828246));
#17457=CARTESIAN_POINT('Ctrl Pts',(-0.0837162036049941,-0.120334265578335,
1.01659751971584));
#17458=CARTESIAN_POINT('Ctrl Pts',(-0.0439316411201867,-0.14801227165006,
1.0192449090901));
#17459=CARTESIAN_POINT('Ctrl Pts',(0.0109383251366414,-0.154006411209824,
1.02189229846436));
#17460=CARTESIAN_POINT('Ctrl Pts',(0.0557604321169594,-0.135571060438576,
1.02453968783862));
#17461=CARTESIAN_POINT('Ctrl Pts',(0.100582539097277,-0.11713570966733,
1.02718707721288));
#17462=CARTESIAN_POINT('Ctrl Pts',(0.135356786801084,-0.0742708685650716,
1.02983446658714));
#17463=CARTESIAN_POINT('Ctrl Pts',(0.144154783532934,-0.0266108361928598,
1.0324818559614));
#17464=CARTESIAN_POINT('Ctrl Pts',(0.152952780264784,0.0210491961793507,
1.03512924533566));
#17465=CARTESIAN_POINT('Ctrl Pts',(0.135774526024679,0.0735044198215165,
1.03777663470992));
#17466=CARTESIAN_POINT('Ctrl Pts',(0.100488543649143,0.106727647840587,
1.04042402408418));
#17467=CARTESIAN_POINT('Ctrl Pts',(0.0652025612736062,0.139950875859659,
1.04307141345844));
#17468=CARTESIAN_POINT('Ctrl Pts',(0.0118088507626404,0.153942108255635,
1.0457188028327));
#17469=CARTESIAN_POINT('Ctrl Pts',(-0.0352355257975899,0.142292641904202,
1.04836619220696));
#17470=CARTESIAN_POINT('Ctrl Pts',(-0.0822799023578202,0.130643175552769,
1.05101358158122));
#17471=CARTESIAN_POINT('Ctrl Pts',(-0.122974944967313,0.0933530104539243,
1.05366097095548));
#17472=CARTESIAN_POINT('Ctrl Pts',(-0.138680233730631,0.0475029577050484,
1.05630836032974));
#17473=CARTESIAN_POINT('Ctrl Pts',(-0.143873300563147,0.0323423075707214,
1.05718373869173));
#17474=CARTESIAN_POINT('Ctrl Pts',(-0.146334133026589,0.0162457690968458,
1.05805911705372));
#17475=CARTESIAN_POINT('Ctrl Pts',(-0.146216477546812,0.000114345603752017,
1.05893449541571));
#17476=CARTESIAN_POINT('Origin',(0.,0.,0.));
#17477=CARTESIAN_POINT('',(-0.146204073634541,-0.000109175101205505,1.11606550458429));
#17478=CARTESIAN_POINT('',(-0.146170555016798,-9.22629125885076E-5,1.10893449541571));
#17479=CARTESIAN_POINT('',(-0.14635,-1.79227059055215E-17,0.));
#17480=CARTESIAN_POINT('Ctrl Pts',(-0.146204073634541,-0.000109175101205505,
1.11606550458429));
#17481=CARTESIAN_POINT('Ctrl Pts',(-0.145981599624502,0.032003853555373,
1.1143232512413));
#17482=CARTESIAN_POINT('Ctrl Pts',(-0.135565881201595,0.0642480963468658,
1.11258099789831));
#17483=CARTESIAN_POINT('Ctrl Pts',(-0.11609067353381,0.0895073597405865,
1.11083874455532));
#17484=CARTESIAN_POINT('Ctrl Pts',(-0.0865095427755784,0.127873963375947,
1.10819241467622));
#17485=CARTESIAN_POINT('Ctrl Pts',(-0.0360273159486943,0.150125560802435,
1.10554608479712));
#17486=CARTESIAN_POINT('Ctrl Pts',(0.0122494975033169,0.14607724579886,
1.10289975491801));
#17487=CARTESIAN_POINT('Ctrl Pts',(0.0605263109553308,0.142028930795284,
1.10025342503891));
#17488=CARTESIAN_POINT('Ctrl Pts',(0.10659771103247,0.111680703361642,1.09760709515981));
#17489=CARTESIAN_POINT('Ctrl Pts',(0.129376093089052,0.0689234246557527,
1.09496076528071));
#17490=CARTESIAN_POINT('Ctrl Pts',(0.152154475145634,0.0261661459498645,
1.09231443540161));
#17491=CARTESIAN_POINT('Ctrl Pts',(0.151639839181659,-0.0290001840282729,
1.0896681055225));
#17492=CARTESIAN_POINT('Ctrl Pts',(0.128067742174483,-0.0713250681289163,
1.0870217756434));
#17493=CARTESIAN_POINT('Ctrl Pts',(0.104495645167307,-0.11364995222956,
1.0843754457643));
#17494=CARTESIAN_POINT('Ctrl Pts',(0.0578660871169326,-0.143133390452712,
1.0817291158852));
#17495=CARTESIAN_POINT('Ctrl Pts',(0.00952215035475689,-0.146280349267719,
1.0790827860061));
#17496=CARTESIAN_POINT('Ctrl Pts',(-0.0388217864074202,-0.149427308082725,
1.07643645612699));
#17497=CARTESIAN_POINT('Ctrl Pts',(-0.0888801018813974,-0.126237787489585,
1.07379012624789));
#17498=CARTESIAN_POINT('Ctrl Pts',(-0.117740317519168,-0.0873259958989869,
1.07114379636879));
#17499=CARTESIAN_POINT('Ctrl Pts',(-0.136201180005177,-0.0624354946409797,
1.06945103244062));
#17500=CARTESIAN_POINT('Ctrl Pts',(-0.145988395071105,-0.0311118962502767,
1.06775826851246));
#17501=CARTESIAN_POINT('Ctrl Pts',(-0.146184049129756,9.96948043307314E-5,
1.06606550458429));
#17502=CARTESIAN_POINT('Ctrl Pts',(-0.146216477546812,0.000114345603752017,
1.05893449541571));
#17503=CARTESIAN_POINT('Ctrl Pts',(-0.145978309898544,-0.0325401742182177,
1.06070650642798));
#17504=CARTESIAN_POINT('Ctrl Pts',(-0.135174246449945,-0.06533764273189,
1.06247851744025));
#17505=CARTESIAN_POINT('Ctrl Pts',(-0.115079600404687,-0.0908043159161929,
1.06425052845252));
#17506=CARTESIAN_POINT('Ctrl Pts',(-0.0850581433982766,-0.128851596389654,
1.06689791782678));
#17507=CARTESIAN_POINT('Ctrl Pts',(-0.0342996944683099,-0.150536216937668,
1.06954530720104));
#17508=CARTESIAN_POINT('Ctrl Pts',(0.0139457694684962,-0.145925507476389,
1.0721926965753));
#17509=CARTESIAN_POINT('Ctrl Pts',(0.0621912334052997,-0.14131479801511,
1.07484008594956));
#17510=CARTESIAN_POINT('Ctrl Pts',(0.107923712348941,-0.110408758544542,
1.07748747532382));
#17511=CARTESIAN_POINT('Ctrl Pts',(0.1301953818052,-0.0673639426912374,
1.08013486469808));
#17512=CARTESIAN_POINT('Ctrl Pts',(0.15246705126146,-0.024319126837932,
1.08278225407234));
#17513=CARTESIAN_POINT('Ctrl Pts',(0.151277911230334,0.0308644653981125,
1.0854296434466));
#17514=CARTESIAN_POINT('Ctrl Pts',(0.127172648928576,0.0729099141598672,
1.08807703282086));
#17515=CARTESIAN_POINT('Ctrl Pts',(0.103067386626818,0.114955362921624,
1.09072442219512));
#17516=CARTESIAN_POINT('Ctrl Pts',(0.0560460020544268,0.143862668209093,
1.09337181156938));
#17517=CARTESIAN_POINT('Ctrl Pts',(0.00764670469074742,0.146390799320458,
1.09601920094364));
#17518=CARTESIAN_POINT('Ctrl Pts',(-0.0407525926729279,0.148918930431823,
1.0986665903179));
#17519=CARTESIAN_POINT('Ctrl Pts',(-0.0905298028278899,0.125067887367091,
1.10131397969216));
#17520=CARTESIAN_POINT('Ctrl Pts',(-0.11888440661962,0.0857626730052823,
1.10396136906642));
#17521=CARTESIAN_POINT('Ctrl Pts',(-0.136639133674055,0.0611510311732957,
1.10561907784952));
#17522=CARTESIAN_POINT('Ctrl Pts',(-0.145994366384503,0.0304800321277272,
1.10727678663261));
#17523=CARTESIAN_POINT('Ctrl Pts',(-0.146170555016798,-9.22629125885076E-5,
1.10893449541571));
#17524=CARTESIAN_POINT('Origin',(0.,0.,0.));
#17525=CARTESIAN_POINT('',(-0.146577386142569,-3.88073511912723E-5,1.16606550458429));
#17526=CARTESIAN_POINT('',(-0.146552328192774,-6.73160170860698E-5,1.15893449541571));
#17527=CARTESIAN_POINT('',(-0.14635,-1.79227059055215E-17,0.));
#17528=CARTESIAN_POINT('Ctrl Pts',(-0.146577386142569,-3.88073511912723E-5,
1.16606550458429));
#17529=CARTESIAN_POINT('Ctrl Pts',(-0.146413350709018,0.0463056768050285,
1.16353456384924));
#17530=CARTESIAN_POINT('Ctrl Pts',(-0.122574225104448,0.0927954474992645,
1.1610036231142));
#17531=CARTESIAN_POINT('Ctrl Pts',(-0.0847742546295189,0.119590709008994,
1.15847268237915));
#17532=CARTESIAN_POINT('Ctrl Pts',(-0.0452509303920754,0.147607604138013,
1.15582635250005));
#17533=CARTESIAN_POINT('Ctrl Pts',(0.00953524646069181,0.154093252855687,
1.15318002262095));
#17534=CARTESIAN_POINT('Ctrl Pts',(0.0545077808453859,0.136079071706768,
1.15053369274185));
#17535=CARTESIAN_POINT('Ctrl Pts',(0.0994803152300801,0.118064890557849,
1.14788736286275));
#17536=CARTESIAN_POINT('Ctrl Pts',(0.134639207146701,0.0755508795423365,
1.14524103298364));
#17537=CARTESIAN_POINT('Ctrl Pts',(0.14389167861853,0.027996370364851,1.14259470310454));
#17538=CARTESIAN_POINT('Ctrl Pts',(0.15314415009036,-0.0195581388126345,
1.13994837322544));
#17539=CARTESIAN_POINT('Ctrl Pts',(0.136490201117397,-0.0721531461520931,
1.13730204334634));
#17540=CARTESIAN_POINT('Ctrl Pts',(0.101552606157185,-0.105715089329518,
1.13465571346724));
#17541=CARTESIAN_POINT('Ctrl Pts',(0.0666150111969725,-0.139277032506943,
1.13200938358813));
#17542=CARTESIAN_POINT('Ctrl Pts',(0.0133937702495101,-0.153805911522335,
1.12936305370903));
#17543=CARTESIAN_POINT('Ctrl Pts',(-0.033750917386428,-0.142651629870951,
1.12671672382993));
#17544=CARTESIAN_POINT('Ctrl Pts',(-0.0808956050223675,-0.131497348219567,
1.12407039395083));
#17545=CARTESIAN_POINT('Ctrl Pts',(-0.121963739346782,-0.094659905901407,
1.12142406407173));
#17546=CARTESIAN_POINT('Ctrl Pts',(-0.1381577891642,-0.0490003798202082,
1.11877773419262));
#17547=CARTESIAN_POINT('Ctrl Pts',(-0.143690228857438,-0.0334015285560649,
1.11787365765651));
#17548=CARTESIAN_POINT('Ctrl Pts',(-0.146319518115206,-0.0167730178360648,
1.1169695811204));
#17549=CARTESIAN_POINT('Ctrl Pts',(-0.146204073634541,-0.000109175101205505,
1.11606550458429));
#17550=CARTESIAN_POINT('Ctrl Pts',(-0.146170555016798,-9.22629125885076E-5,
1.10893449541571));
#17551=CARTESIAN_POINT('Ctrl Pts',(-0.146275742653821,-0.0183444476975235,
1.10992417600687));
#17552=CARTESIAN_POINT('Ctrl Pts',(-0.143109248288425,-0.0365614514641733,
1.11091385659804));
#17553=CARTESIAN_POINT('Ctrl Pts',(-0.136505188007283,-0.0534328725168923,
1.1119035371892));
#17554=CARTESIAN_POINT('Ctrl Pts',(-0.118839368174718,-0.0985638180183679,
1.11455092656346));
#17555=CARTESIAN_POINT('Ctrl Pts',(-0.0765757310810901,-0.134066323362434,
1.11719831593772));
#17556=CARTESIAN_POINT('Ctrl Pts',(-0.0290731934694857,-0.143678417446031,
1.11984570531198));
#17557=CARTESIAN_POINT('Ctrl Pts',(0.01842934414212,-0.153290511529629,
1.12249309468624));
#17558=CARTESIAN_POINT('Ctrl Pts',(0.071170782271703,-0.137012194352758,
1.1251404840605));
#17559=CARTESIAN_POINT('Ctrl Pts',(0.10499283308901,-0.102299771349957,
1.12778787343476));
#17560=CARTESIAN_POINT('Ctrl Pts',(0.138814883906317,-0.0675873483471558,
1.13043526280902));
#17561=CARTESIAN_POINT('Ctrl Pts',(0.153717547411349,-0.0144408195184256,
1.13308265218328));
#17562=CARTESIAN_POINT('Ctrl Pts',(0.142874638214406,0.0327959749574983,
1.13573004155754));
#17563=CARTESIAN_POINT('Ctrl Pts',(0.132031729017462,0.0800327694334235,
1.1383774309318));
#17564=CARTESIAN_POINT('Ctrl Pts',(0.0954432471185425,0.121359829556542,
1.14102482030606));
#17565=CARTESIAN_POINT('Ctrl Pts',(0.0498685966661331,0.137847238945365,
1.14367220968032));
#17566=CARTESIAN_POINT('Ctrl Pts',(0.00429394621372511,0.154334648334189,
1.14631959905458));
#17567=CARTESIAN_POINT('Ctrl Pts',(-0.0502668727921719,0.145982406988718,
1.14896698842884));
#17568=CARTESIAN_POINT('Ctrl Pts',(-0.0888222026239048,0.116616270474356,
1.1516143778031));
#17569=CARTESIAN_POINT('Ctrl Pts',(-0.124357782404925,0.0895501633622979,
1.1540544170073));
#17570=CARTESIAN_POINT('Ctrl Pts',(-0.146296868742479,0.0446329749882746,
1.15649445621151));
#17571=CARTESIAN_POINT('Ctrl Pts',(-0.146552328192774,-6.73160170860698E-5,
1.15893449541571));
#17572=CARTESIAN_POINT('Origin',(0.,0.,0.));
#17573=CARTESIAN_POINT('',(-0.146318311025392,0.000133437649768732,1.21606550458429));
#17574=CARTESIAN_POINT('',(-0.146373054956946,0.000132657382717961,1.20893449541571));
#17575=CARTESIAN_POINT('',(-0.14635,-1.79227059055215E-17,0.));
#17576=CARTESIAN_POINT('Ctrl Pts',(-0.146318311025392,0.000133437649768732,
1.21606550458429));
#17577=CARTESIAN_POINT('Ctrl Pts',(-0.146429658069886,0.0125190846592594,
1.21539220633629));
#17578=CARTESIAN_POINT('Ctrl Pts',(-0.144988168643405,0.0248791929292086,
1.21471890808829));
#17579=CARTESIAN_POINT('Ctrl Pts',(-0.141892968227885,0.0368102906365087,
1.21404560984029));
#17580=CARTESIAN_POINT('Ctrl Pts',(-0.129727599662405,0.083704249513052,
1.21139927996119));
#17581=CARTESIAN_POINT('Ctrl Pts',(-0.0920156607298113,0.123970842060419,
1.20875295008209));
#17582=CARTESIAN_POINT('Ctrl Pts',(-0.0460184991925076,0.139179415364965,
1.20610662020299));
#17583=CARTESIAN_POINT('Ctrl Pts',(-2.13376552038805E-5,0.15438798866951,
1.20346029032389));
#17584=CARTESIAN_POINT('Ctrl Pts',(0.0542610464868107,0.144538542731236,
1.20081396044478));
#17585=CARTESIAN_POINT('Ctrl Pts',(0.091982751999895,0.114139323915075,
1.19816763056568));
#17586=CARTESIAN_POINT('Ctrl Pts',(0.129704457512977,0.0837401050989159,
1.19552130068658));
#17587=CARTESIAN_POINT('Ctrl Pts',(0.150865484397133,0.0327911134048729,
1.19287497080748));
#17588=CARTESIAN_POINT('Ctrl Pts',(0.145780097726084,-0.0153874961003253,
1.19022864092838));
#17589=CARTESIAN_POINT('Ctrl Pts',(0.140694711055036,-0.063566105605525,
1.18758231104927));
#17590=CARTESIAN_POINT('Ctrl Pts',(0.109362910828785,-0.108974332921877,
1.18493598117017));
#17591=CARTESIAN_POINT('Ctrl Pts',(0.0661257549466402,-0.130828118009858,
1.18228965129107));
#17592=CARTESIAN_POINT('Ctrl Pts',(0.0228885990644955,-0.152681903097838,
1.17964332141197));
#17593=CARTESIAN_POINT('Ctrl Pts',(-0.0322539124735426,-0.150981245957443,
1.17699699153287));
#17594=CARTESIAN_POINT('Ctrl Pts',(-0.0740621845924981,-0.126504564117865,
1.17435066165376));
#17595=CARTESIAN_POINT('Ctrl Pts',(-0.115870456711455,-0.102027882278287,
1.17170433177466));
#17596=CARTESIAN_POINT('Ctrl Pts',(-0.144344489411329,-0.0547751757395235,
1.16905800189556));
#17597=CARTESIAN_POINT('Ctrl Pts',(-0.146451269950206,-0.00637475169995868,
1.16641167201646));
#17598=CARTESIAN_POINT('Ctrl Pts',(-0.146543132875163,-0.00426432565444621,
1.1662962828724));
#17599=CARTESIAN_POINT('Ctrl Pts',(-0.146584864748453,-0.00215171749738942,
1.16618089372835));
#17600=CARTESIAN_POINT('Ctrl Pts',(-0.146577386142569,-3.88073511912723E-5,
1.16606550458429));
#17601=CARTESIAN_POINT('Ctrl Pts',(-0.146552328192774,-6.73160170860698E-5,
1.15893449541571));
#17602=CARTESIAN_POINT('Ctrl Pts',(-0.146574036680232,-0.00386586684592084,
1.15914184558577));
#17603=CARTESIAN_POINT('Ctrl Pts',(-0.1464391612665,-0.00766285139452399,
1.15934919575582));
#17604=CARTESIAN_POINT('Ctrl Pts',(-0.146142739258869,-0.0114471821958193,
1.15955654592588));
#17605=CARTESIAN_POINT('Ctrl Pts',(-0.142358105404532,-0.0597644666683822,
1.16220393530014));
#17606=CARTESIAN_POINT('Ctrl Pts',(-0.112238997038288,-0.106019003930254,
1.1648513246744));
#17607=CARTESIAN_POINT('Ctrl Pts',(-0.0695815129186611,-0.129023839960917,
1.16749871404866));
#17608=CARTESIAN_POINT('Ctrl Pts',(-0.026924028799035,-0.15202867599158,
1.17014610342292));
#17609=CARTESIAN_POINT('Ctrl Pts',(0.0282718310739737,-0.151783810791035,
1.17279349279718));
#17610=CARTESIAN_POINT('Ctrl Pts',(0.0707235276354612,-0.128401405199111,
1.17544088217144));
#17611=CARTESIAN_POINT('Ctrl Pts',(0.11317522419695,-0.105018999607187,
1.1780882715457));
#17612=CARTESIAN_POINT('Ctrl Pts',(0.142882757446916,-0.0584990536238821,
1.18073566091996));
#17613=CARTESIAN_POINT('Ctrl Pts',(0.146238551171451,-0.0101500920973681,
1.18338305029422));
#17614=CARTESIAN_POINT('Ctrl Pts',(0.149594344895986,0.0381988694291446,
1.18603043966848));
#17615=CARTESIAN_POINT('Ctrl Pts',(0.12659839909509,0.0883768464988665,
1.18867782904274));
#17616=CARTESIAN_POINT('Ctrl Pts',(0.0877840381772113,0.117399748124142,
1.191325218417));
#17617=CARTESIAN_POINT('Ctrl Pts',(0.0489696772593311,0.146422649749419,
1.19397260779126));
#17618=CARTESIAN_POINT('Ctrl Pts',(-0.00566309877553352,0.154290475930249,
1.19661999716552));
#17619=CARTESIAN_POINT('Ctrl Pts',(-0.0510896721842483,0.137399358129564,
1.19926738653978));
#17620=CARTESIAN_POINT('Ctrl Pts',(-0.0965162455929618,0.12050824032888,
1.20191477591404));
#17621=CARTESIAN_POINT('Ctrl Pts',(-0.132736616375526,0.0788581785466829,
1.2045621652883));
#17622=CARTESIAN_POINT('Ctrl Pts',(-0.143159994183491,0.0315270405159292,
1.20720955466256));
#17623=CARTESIAN_POINT('Ctrl Pts',(-0.145423823013163,0.021247302336111,
1.20778453491361));
#17624=CARTESIAN_POINT('Ctrl Pts',(-0.146470795531708,0.0106995851133921,
1.20835951516466));
#17625=CARTESIAN_POINT('Ctrl Pts',(-0.146373054956946,0.000132657382717961,
1.20893449541571));
#17626=CARTESIAN_POINT('Origin',(0.,0.,0.));
#17627=CARTESIAN_POINT('',(-0.146120596765396,-4.14129048147555E-5,1.26606550458429));
#17628=CARTESIAN_POINT('',(-0.146109918970638,-1.0198006988139E-5,1.25893449541571));
#17629=CARTESIAN_POINT('',(-0.14635,-1.79227059055215E-17,0.));
#17630=CARTESIAN_POINT('Ctrl Pts',(-0.146120596765396,-4.14129048147555E-5,
1.26606550458429));
#17631=CARTESIAN_POINT('Ctrl Pts',(-0.14605219935785,0.0269443530192317,
1.26460351894424));
#17632=CARTESIAN_POINT('Ctrl Pts',(-0.138898723445843,0.053963836666407,
1.26314153330418));
#17633=CARTESIAN_POINT('Ctrl Pts',(-0.124882896249422,0.0767650581554474,
1.26167954766413));
#17634=CARTESIAN_POINT('Ctrl Pts',(-0.0995129464537159,0.118037388097231,
1.25903321778503));
#17635=CARTESIAN_POINT('Ctrl Pts',(-0.051658938874944,0.145488850208621,
1.25638688790592));
#17636=CARTESIAN_POINT('Ctrl Pts',(-0.00322440565727106,0.146554478394238,
1.25374055802682));
#17637=CARTESIAN_POINT('Ctrl Pts',(0.0452101275604033,0.147620106579856,
1.25109422814772));
#17638=CARTESIAN_POINT('Ctrl Pts',(0.0942251864169787,0.122299900839699,
1.24844789826862));
#17639=CARTESIAN_POINT('Ctrl Pts',(0.121385807331354,0.0821833176976391,
1.24580156838952));
#17640=CARTESIAN_POINT('Ctrl Pts',(0.148546428245729,0.0420667345555804,
1.24315523851041));
#17641=CARTESIAN_POINT('Ctrl Pts',(0.153852611217905,-0.0128462259883804,
1.24050890863131));
#17642=CARTESIAN_POINT('Ctrl Pts',(0.134875632820701,-0.0574210379606392,
1.23786257875221));
#17643=CARTESIAN_POINT('Ctrl Pts',(0.115898654423498,-0.101995849932898,
1.23521624887311));
#17644=CARTESIAN_POINT('Ctrl Pts',(0.0726385146569148,-0.136232513333455,
1.23256991899401));
#17645=CARTESIAN_POINT('Ctrl Pts',(0.0248960600935515,-0.144460368686643,
1.2299235891149));
#17646=CARTESIAN_POINT('Ctrl Pts',(-0.0228463944698117,-0.152688224039831,
1.2272772592358));
#17647=CARTESIAN_POINT('Ctrl Pts',(-0.0750711638299551,-0.134907271345651,
1.2246309293567));
#17648=CARTESIAN_POINT('Ctrl Pts',(-0.107874149410843,-0.0992561323957017,
1.2219845994776));
#17649=CARTESIAN_POINT('Ctrl Pts',(-0.132331163880887,-0.072675612185966,
1.2200115678465));
#17650=CARTESIAN_POINT('Ctrl Pts',(-0.145992019903337,-0.0361614337449312,
1.21803853621539));
#17651=CARTESIAN_POINT('Ctrl Pts',(-0.146318311025392,0.000133437649768732,
1.21606550458429));
#17652=CARTESIAN_POINT('Ctrl Pts',(-0.146373054956946,0.000132657382717961,
1.20893449541571));
#17653=CARTESIAN_POINT('Ctrl Pts',(-0.146020767276673,-0.0379538636644633,
1.21100690453892));
#17654=CARTESIAN_POINT('Ctrl Pts',(-0.130797424420382,-0.0762899498869128,
1.21307931366213));
#17655=CARTESIAN_POINT('Ctrl Pts',(-0.104081054125652,-0.103227285106232,
1.21515172278534));
#17656=CARTESIAN_POINT('Ctrl Pts',(-0.0699523514264828,-0.137638258418326,
1.2177991121596));
#17657=CARTESIAN_POINT('Ctrl Pts',(-0.0170685611947798,-0.153447990763203,
1.22044650153386));
#17658=CARTESIAN_POINT('Ctrl Pts',(0.0303468241642401,-0.143414812629152,
1.22309389090812));
#17659=CARTESIAN_POINT('Ctrl Pts',(0.0777622095232573,-0.133381634495101,
1.22574128028238));
#17660=CARTESIAN_POINT('Ctrl Pts',(0.119709190009594,-0.0975055458821257,
1.22838866965664));
#17661=CARTESIAN_POINT('Ctrl Pts',(0.136973893871985,-0.052219638220276,
1.2310360590309));
#17662=CARTESIAN_POINT('Ctrl Pts',(0.154238597734379,-0.00693373055842239,
1.23368344840516));
#17663=CARTESIAN_POINT('Ctrl Pts',(0.146821024972825,0.0477619961523044,
1.23633083777942));
#17664=CARTESIAN_POINT('Ctrl Pts',(0.118118804930222,0.0868140895256425,
1.23897822715368));
#17665=CARTESIAN_POINT('Ctrl Pts',(0.0894165848876198,0.125866182898978,
1.24162561652794));
#17666=CARTESIAN_POINT('Ctrl Pts',(0.0394297175639698,0.149274642934924,
1.2442730059022));
#17667=CARTESIAN_POINT('Ctrl Pts',(-0.00894524413350711,0.146317192515786,
1.24692039527646));
#17668=CARTESIAN_POINT('Ctrl Pts',(-0.0573202058309854,0.143359742096648,
1.24956778465072));
#17669=CARTESIAN_POINT('Ctrl Pts',(-0.104083261902292,0.114036381222425,
1.25221517402498));
#17670=CARTESIAN_POINT('Ctrl Pts',(-0.127814530591109,0.0717787154251623,
1.25486256339924));
#17671=CARTESIAN_POINT('Ctrl Pts',(-0.139981499518435,0.0501133037087236,
1.2562198740714));
#17672=CARTESIAN_POINT('Ctrl Pts',(-0.146094355379323,0.0250479932723348,
1.25757718474355));
#17673=CARTESIAN_POINT('Ctrl Pts',(-0.146109918970638,-1.0198006988139E-5,
1.25893449541571));
#17674=CARTESIAN_POINT('Origin',(0.,0.,0.));
#17675=CARTESIAN_POINT('',(-0.146470135615938,-0.000111966546850736,1.31606550458429));
#17676=CARTESIAN_POINT('',(-0.146410535958061,-0.000127756381200432,1.30893449541571));
#17677=CARTESIAN_POINT('',(-0.14635,-1.79227059055215E-17,0.));
#17678=CARTESIAN_POINT('Ctrl Pts',(-0.146470135615938,-0.000111966546850736,
1.31606550458429));
#17679=CARTESIAN_POINT('Ctrl Pts',(-0.146120207411574,0.0411799307449602,
1.31381483155218));
#17680=CARTESIAN_POINT('Ctrl Pts',(-0.127827491572984,0.0827431563937987,
1.31156415852007));
#17681=CARTESIAN_POINT('Ctrl Pts',(-0.0969137672218927,0.10998333351997,
1.30931348548796));
#17682=CARTESIAN_POINT('Ctrl Pts',(-0.0605655677022408,0.142012194937238,
1.30666715560886));
#17683=CARTESIAN_POINT('Ctrl Pts',(-0.00676890401288169,0.154239532672684,
1.30402082572976));
#17684=CARTESIAN_POINT('Ctrl Pts',(0.0398526445220406,0.14106870189023,
1.30137449585066));
#17685=CARTESIAN_POINT('Ctrl Pts',(0.0864741930569617,0.127897871107775,
1.29872816597155));
#17686=CARTESIAN_POINT('Ctrl Pts',(0.125920626437448,0.0893288718074177,
1.29608183609245));
#17687=CARTESIAN_POINT('Ctrl Pts',(0.14013669149516,0.0430153417578024,
1.29343550621335));
#17688=CARTESIAN_POINT('Ctrl Pts',(0.154352756552873,-0.00329818829181684,
1.29078917633425));
#17689=CARTESIAN_POINT('Ctrl Pts',(0.143338453287813,-0.0573562490906975,
1.28814284645515));
#17690=CARTESIAN_POINT('Ctrl Pts',(0.112135201594409,-0.0944156157243562,
1.28549651657604));
#17691=CARTESIAN_POINT('Ctrl Pts',(0.0809319499010078,-0.131474982358013,
1.28285018669694));
#17692=CARTESIAN_POINT('Ctrl Pts',(0.0295397497792676,-0.151535654826449,
1.28020385681784));
#17693=CARTESIAN_POINT('Ctrl Pts',(-0.0185183802362589,-0.1454155477333,
1.27755752693874));
#17694=CARTESIAN_POINT('Ctrl Pts',(-0.066576510251784,-0.139295440640151,
1.27491119705964));
#17695=CARTESIAN_POINT('Ctrl Pts',(-0.111300570161094,-0.106994553985419,
1.27226486718053));
#17696=CARTESIAN_POINT('Ctrl Pts',(-0.13221965410943,-0.0632975117719662,
1.26961853730143));
#17697=CARTESIAN_POINT('Ctrl Pts',(-0.141581826511298,-0.0437412423069929,
1.26843419306239));
#17698=CARTESIAN_POINT('Ctrl Pts',(-0.146176005022067,-0.0219023912433209,
1.26724984882334));
#17699=CARTESIAN_POINT('Ctrl Pts',(-0.146120596765396,-4.14129048147555E-5,
1.26606550458429));
#17700=CARTESIAN_POINT('Ctrl Pts',(-0.146109918970638,-1.0198006988139E-5,
1.25893449541571));
#17701=CARTESIAN_POINT('Ctrl Pts',(-0.146124711647138,-0.0238271763493914,
1.26022457411781));
#17702=CARTESIAN_POINT('Ctrl Pts',(-0.140631289159497,-0.0476377233371588,
1.26151465281992));
#17703=CARTESIAN_POINT('Ctrl Pts',(-0.129592576141605,-0.0685164391025303,
1.26280473152202));
#17704=CARTESIAN_POINT('Ctrl Pts',(-0.106939871696956,-0.111361957112663,
1.26545212089628));
#17705=CARTESIAN_POINT('Ctrl Pts',(-0.0609349815013302,-0.141861022412626,
1.26809951027054));
#17706=CARTESIAN_POINT('Ctrl Pts',(-0.0126505083952331,-0.146043496451057,
1.2707468996448));
#17707=CARTESIAN_POINT('Ctrl Pts',(0.0356339647108625,-0.150225970489488,
1.27339428901906));
#17708=CARTESIAN_POINT('Ctrl Pts',(0.0861980207274291,-0.128091853266388,
1.27604167839332));
#17709=CARTESIAN_POINT('Ctrl Pts',(0.11588072467734,-0.0897797074320025,
1.27868906776758));
#17710=CARTESIAN_POINT('Ctrl Pts',(0.145563428627253,-0.0514675615976161,
1.28133645714184));
#17711=CARTESIAN_POINT('Ctrl Pts',(0.154364780510509,0.00302261284805656,
1.2839838465161));
#17712=CARTESIAN_POINT('Ctrl Pts',(0.138253309066183,0.0487315170146188,
1.28663123589036));
#17713=CARTESIAN_POINT('Ctrl Pts',(0.122141837621857,0.0944404211811797,
1.28927862526462));
#17714=CARTESIAN_POINT('Ctrl Pts',(0.0811175428499519,0.131368055068631,
1.29192601463888));
#17715=CARTESIAN_POINT('Ctrl Pts',(0.0339716590485425,0.142599665496764,
1.29457340401314));
#17716=CARTESIAN_POINT('Ctrl Pts',(-0.013174224752867,0.153831275924897,
1.2972207933874));
#17717=CARTESIAN_POINT('Ctrl Pts',(-0.0664416975837803,0.139366862893713,
1.29986818276166));
#17718=CARTESIAN_POINT('Ctrl Pts',(-0.101431520699135,0.105831870563862,
1.30251557213592));
#17719=CARTESIAN_POINT('Ctrl Pts',(-0.129710573305276,0.0787286237393239,
1.30465521322918));
#17720=CARTESIAN_POINT('Ctrl Pts',(-0.146050663974784,0.0391684733249047,
1.30679485432245));
#17721=CARTESIAN_POINT('Ctrl Pts',(-0.146410535958061,-0.000127756381200432,
1.30893449541571));
#17722=CARTESIAN_POINT('Origin',(0.,0.,0.));
#17723=CARTESIAN_POINT('',(-0.146471469669193,0.000111495080380188,1.36606550458429));
#17724=CARTESIAN_POINT('',(-0.146526884620975,8.5711493927648E-5,1.35893449541571));
#17725=CARTESIAN_POINT('',(-0.14635,-1.79227059055215E-17,0.));
#17726=CARTESIAN_POINT('Ctrl Pts',(-0.146471469669193,0.000111495080380188,
1.36606550458429));
#17727=CARTESIAN_POINT('Ctrl Pts',(-0.146532402405025,0.0073220458586883,
1.36567247403923));
#17728=CARTESIAN_POINT('Ctrl Pts',(-0.146045973070864,0.0145243451116175,
1.36527944349416));
#17729=CARTESIAN_POINT('Ctrl Pts',(-0.144983764805735,0.0216407019395156,
1.3648864129491));
#17730=CARTESIAN_POINT('Ctrl Pts',(-0.137831767320671,0.0695561322809842,
1.36224008307));
#17731=CARTESIAN_POINT('Ctrl Pts',(-0.104576727819841,0.113575347233418,
1.3595937531909));
#17732=CARTESIAN_POINT('Ctrl Pts',(-0.060440002550743,0.133550058215342,
1.3569474233118));
#17733=CARTESIAN_POINT('Ctrl Pts',(-0.0163032772816473,0.153524769197265,
1.35430109343269));
#17734=CARTESIAN_POINT('Ctrl Pts',(0.0387151337557165,0.149454976208681,
1.35165476355359));
#17735=CARTESIAN_POINT('Ctrl Pts',(0.0794324390145508,0.123203488242689,
1.34900843367449));
#17736=CARTESIAN_POINT('Ctrl Pts',(0.120149744273387,0.0969520002766962,
1.34636210379539));
#17737=CARTESIAN_POINT('Ctrl Pts',(0.146565943753694,0.048518817333291,
1.34371577391629));
#17738=CARTESIAN_POINT('Ctrl Pts',(0.14658992694451,7.25688577880009E-5,
1.34106944403718));
#17739=CARTESIAN_POINT('Ctrl Pts',(0.146613910135327,-0.0483736796177136,
1.33842311415808));
#17740=CARTESIAN_POINT('Ctrl Pts',(0.120245677036657,-0.0968329936253116,
1.33577678427898));
#17741=CARTESIAN_POINT('Ctrl Pts',(0.0795543829983497,-0.123124782547022,
1.33313045439988));
#17742=CARTESIAN_POINT('Ctrl Pts',(0.0388630889600415,-0.149416571468734,
1.33048412452078));
#17743=CARTESIAN_POINT('Ctrl Pts',(-0.0161512660179049,-0.153540835304554,
1.32783779464168));
#17744=CARTESIAN_POINT('Ctrl Pts',(-0.0603077462478081,-0.133609833714981,
1.32519146476257));
#17745=CARTESIAN_POINT('Ctrl Pts',(-0.10446422647771,-0.113678832125408,
1.32254513488347));
#17746=CARTESIAN_POINT('Ctrl Pts',(-0.137762831959571,-0.0696925651104417,
1.31989880500437));
#17747=CARTESIAN_POINT('Ctrl Pts',(-0.144962267025529,-0.0217842390534145,
1.31725247512527));
#17748=CARTESIAN_POINT('Ctrl Pts',(-0.146038665626028,-0.0146213916011371,
1.31685681827827));
#17749=CARTESIAN_POINT('Ctrl Pts',(-0.146531651210624,-0.00737087161912708,
1.31646116143128));
#17750=CARTESIAN_POINT('Ctrl Pts',(-0.146470135615938,-0.000111966546850736,
1.31606550458429));
#17751=CARTESIAN_POINT('Ctrl Pts',(-0.146410535958061,-0.000127756381200432,
1.30893449541571));
#17752=CARTESIAN_POINT('Ctrl Pts',(-0.146495935505426,-0.00945296197092968,
1.30944224369671));
#17753=CARTESIAN_POINT('Ctrl Pts',(-0.145681427739287,-0.018763305174839,
1.3099499919777));
#17754=CARTESIAN_POINT('Ctrl Pts',(-0.143913007029536,-0.0278887903271487,
1.3104577402587));
#17755=CARTESIAN_POINT('Ctrl Pts',(-0.134692496844786,-0.0754688872597875,
1.31310512963296));
#17756=CARTESIAN_POINT('Ctrl Pts',(-0.0995393030754929,-0.118023509496548,
1.31575251900722));
#17757=CARTESIAN_POINT('Ctrl Pts',(-0.0545553941775042,-0.136060454153345,
1.31839990838148));
#17758=CARTESIAN_POINT('Ctrl Pts',(-0.00957148527951295,-0.154097398810142,
1.32104729775574));
#17759=CARTESIAN_POINT('Ctrl Pts',(0.0452431387471776,-0.14761666588697,
1.32369468713));
#17760=CARTESIAN_POINT('Ctrl Pts',(0.0847805644327026,-0.119586763955155,
1.32634207650426));
#17761=CARTESIAN_POINT('Ctrl Pts',(0.124317990118227,-0.09155686202334,
1.32898946587852));
#17762=CARTESIAN_POINT('Ctrl Pts',(0.148578217462589,-0.041977791082884,
1.33163685525278));
#17763=CARTESIAN_POINT('Ctrl Pts',(0.146448816178573,0.00644068764408242,
1.33428424462704));
#17764=CARTESIAN_POINT('Ctrl Pts',(0.144319414894557,0.0548591663710502,
1.3369316340013));
#17765=CARTESIAN_POINT('Ctrl Pts',(0.115800384982161,0.102117052884526,
1.33957902337556));
#17766=CARTESIAN_POINT('Ctrl Pts',(0.0739549070570988,0.126567807678519,
1.34222641274982));
#17767=CARTESIAN_POINT('Ctrl Pts',(0.0321094291320376,0.151018562472512,
1.34487380212408));
#17768=CARTESIAN_POINT('Ctrl Pts',(-0.0230624968056921,0.152662185547021,
1.34752119149834));
#17769=CARTESIAN_POINT('Ctrl Pts',(-0.0662892946253695,0.1307458130856,
1.3501685808726));
#17770=CARTESIAN_POINT('Ctrl Pts',(-0.109516092445046,0.10882944062418,
1.35281597024686));
#17771=CARTESIAN_POINT('Ctrl Pts',(-0.140797762146673,0.0633530726268328,
1.35546335962112));
#17772=CARTESIAN_POINT('Ctrl Pts',(-0.145805692234247,0.0151472216574969,
1.35811074899538));
#17773=CARTESIAN_POINT('Ctrl Pts',(-0.146325105122407,0.0101474034011793,
1.35838533113549));
#17774=CARTESIAN_POINT('Ctrl Pts',(-0.146561879835735,0.00511822289583405,
1.3586599132756));
#17775=CARTESIAN_POINT('Ctrl Pts',(-0.146526884620975,8.5711493927648E-5,
1.35893449541571));
#17776=CARTESIAN_POINT('Origin',(0.,0.,0.));
#17777=CARTESIAN_POINT('',(-0.146120987371435,4.2191387702159E-5,1.41606550458429));
#17778=CARTESIAN_POINT('',(-0.146148882937928,7.6306569664006E-5,1.40893449541571));
#17779=CARTESIAN_POINT('',(-0.14635,-1.79227059055215E-17,0.));
#17780=CARTESIAN_POINT('Ctrl Pts',(-0.146120987371435,4.2191387702159E-5,
1.41606550458429));
#17781=CARTESIAN_POINT('Ctrl Pts',(-0.146177309023295,0.021854523983563,
1.41488378664717));
#17782=CARTESIAN_POINT('Ctrl Pts',(-0.141604359564088,0.0436444172696427,
1.41370206871005));
#17783=CARTESIAN_POINT('Ctrl Pts',(-0.132282279973341,0.0631665524487371,
1.41252035077294));
#17784=CARTESIAN_POINT('Ctrl Pts',(-0.1114064880593,0.106884268839086,1.40987402089383));
#17785=CARTESIAN_POINT('Ctrl Pts',(-0.0667143915920224,0.139229456738304,
1.40722769101473));
#17786=CARTESIAN_POINT('Ctrl Pts',(-0.0186623352932378,0.145397151366753,
1.40458136113563));
#17787=CARTESIAN_POINT('Ctrl Pts',(0.0293897210055454,0.151564845995202,
1.40193503125653));
#17788=CARTESIAN_POINT('Ctrl Pts',(0.0808017371358351,0.131555047352884,
1.39928870137743));
#17789=CARTESIAN_POINT('Ctrl Pts',(0.112041660826149,0.0945265884816804,
1.39664237149832));
#17790=CARTESIAN_POINT('Ctrl Pts',(0.143281584516463,0.0574981296104763,
1.39399604161922));
#17791=CARTESIAN_POINT('Ctrl Pts',(0.154349415766802,0.00345101051038574,
1.39134971174012));
#17792=CARTESIAN_POINT('Ctrl Pts',(0.140179214932283,-0.0428765696854336,
1.38870338186102));
#17793=CARTESIAN_POINT('Ctrl Pts',(0.126009014097764,-0.089204149881253,
1.38605705198192));
#17794=CARTESIAN_POINT('Ctrl Pts',(0.0866007811783877,-0.127812191172801,
1.38341072210282));
#17795=CARTESIAN_POINT('Ctrl Pts',(0.0399922944706322,-0.14102917638501,
1.38076439222371));
#17796=CARTESIAN_POINT('Ctrl Pts',(-0.00661619223712474,-0.15424616159722,
1.37811806234461));
#17797=CARTESIAN_POINT('Ctrl Pts',(-0.060424932733261,-0.142072090730089,
1.37547173246551));
#17798=CARTESIAN_POINT('Ctrl Pts',(-0.0968048252466797,-0.110079232431271,
1.37282540258641));
#17799=CARTESIAN_POINT('Ctrl Pts',(-0.127781608685608,-0.08283792481198,
1.37057210325237));
#17800=CARTESIAN_POINT('Ctrl Pts',(-0.146122133733866,-0.0412276055847571,
1.36831880391833));
#17801=CARTESIAN_POINT('Ctrl Pts',(-0.146471469669193,0.000111495080380188,
1.36606550458429));
#17802=CARTESIAN_POINT('Ctrl Pts',(-0.146526884620975,8.5711493927648E-5,
1.35893449541571));
#17803=CARTESIAN_POINT('Ctrl Pts',(-0.146224472749943,-0.0434028397118431,
1.36130730264986));
#17804=CARTESIAN_POINT('Ctrl Pts',(-0.125627402569456,-0.0871401285467012,
1.36368010988401));
#17805=CARTESIAN_POINT('Ctrl Pts',(-0.0917490966422633,-0.114327780902106,
1.36605291711816));
#17806=CARTESIAN_POINT('Ctrl Pts',(-0.0539503804891888,-0.144661598551044,
1.36870030649242));
#17807=CARTESIAN_POINT('Ctrl Pts',(0.00038124229047478,-0.154393899907594,
1.37134769586668));
#17808=CARTESIAN_POINT('Ctrl Pts',(0.0463590973565905,-0.139066790892088,
1.37399508524094));
#17809=CARTESIAN_POINT('Ctrl Pts',(0.0923369524227062,-0.123739681876581,
1.3766424746152));
#17810=CARTESIAN_POINT('Ctrl Pts',(0.129961039775272,-0.083353162489017,
1.37928986398946));
#17811=CARTESIAN_POINT('Ctrl Pts',(0.141997595260484,-0.0364063334065561,
1.38193725336372));
#17812=CARTESIAN_POINT('Ctrl Pts',(0.154034150745695,0.0105404956759021,
1.38458464273798));
#17813=CARTESIAN_POINT('Ctrl Pts',(0.140483174363557,0.0640476344532581,
1.38723203211224));
#17814=CARTESIAN_POINT('Ctrl Pts',(0.10755170844225,0.0996060653705087,
1.3898794214865));
#17815=CARTESIAN_POINT('Ctrl Pts',(0.0746202425209409,0.135164496287762,
1.39252681086076));
#17816=CARTESIAN_POINT('Ctrl Pts',(0.0223082870604623,0.152774219344908,
1.39517420023502));
#17817=CARTESIAN_POINT('Ctrl Pts',(-0.025422593472234,0.144369075867769,
1.39782158960928));
#17818=CARTESIAN_POINT('Ctrl Pts',(-0.073153474004929,0.135963932390631,
1.40046897898354));
#17819=CARTESIAN_POINT('Ctrl Pts',(-0.11630327960984,0.101543922379208,
1.4031163683578));
#17820=CARTESIAN_POINT('Ctrl Pts',(-0.135107186188192,0.0568751802851974,
1.40576375773206));
#17821=CARTESIAN_POINT('Ctrl Pts',(-0.142614236437708,0.0390421576584788,
1.40682067029328));
#17822=CARTESIAN_POINT('Ctrl Pts',(-0.14624095998336,0.0195756595648056,
1.40787758285449));
#17823=CARTESIAN_POINT('Ctrl Pts',(-0.146148882937928,7.6306569664006E-5,
1.40893449541571));
#17824=CARTESIAN_POINT('Origin',(0.,0.,0.));
#17825=CARTESIAN_POINT('',(-0.14631473222987,-0.000131398079681141,1.46606550458429));
#17826=CARTESIAN_POINT('',(-0.146248097568756,-0.000123763188177425,1.45893449541571));
#17827=CARTESIAN_POINT('',(-0.14635,-1.79227059055215E-17,0.));
#17828=CARTESIAN_POINT('Ctrl Pts',(-0.14631473222987,-0.000131398079681141,
1.46606550458429));
#17829=CARTESIAN_POINT('Ctrl Pts',(-0.145989697979493,0.0361157155227289,
1.46409509925512));
#17830=CARTESIAN_POINT('Ctrl Pts',(-0.132370868650209,0.0725796635271419,
1.46212469392594));
#17831=CARTESIAN_POINT('Ctrl Pts',(-0.107973319296019,0.0991484059484618,
1.46015428859677));
#17832=CARTESIAN_POINT('Ctrl Pts',(-0.0752064754000165,0.134831245351468,
1.45750795871767));
#17833=CARTESIAN_POINT('Ctrl Pts',(-0.0229974942306327,0.152665588379184,
1.45486162883857));
#17834=CARTESIAN_POINT('Ctrl Pts',(0.0247535192036911,0.144485406820094,
1.45221529895946));
#17835=CARTESIAN_POINT('Ctrl Pts',(0.0725045326380122,0.136305225261004,
1.44956896908036));
#17836=CARTESIAN_POINT('Ctrl Pts',(0.115797578337275,0.102110519115111,
1.44692263920126));
#17837=CARTESIAN_POINT('Ctrl Pts',(0.134818450998255,0.0575543070937695,
1.44427630932216));
#17838=CARTESIAN_POINT('Ctrl Pts',(0.153839323659235,0.0129980950724284,
1.44162997944306));
#17839=CARTESIAN_POINT('Ctrl Pts',(0.148588023281934,-0.0419196228243577,
1.43898364956396));
#17840=CARTESIAN_POINT('Ctrl Pts',(0.121467255745355,-0.082062966762292,
1.43633731968485));
#17841=CARTESIAN_POINT('Ctrl Pts',(0.0943464882087764,-0.122206310700226,
1.43369098980575));
#17842=CARTESIAN_POINT('Ctrl Pts',(0.0453562535129183,-0.147575280679306,
1.43104465992665));
#17843=CARTESIAN_POINT('Ctrl Pts',(-0.00307937473935208,-0.146557666176543,
1.42839833004755));
#17844=CARTESIAN_POINT('Ctrl Pts',(-0.0515150029916225,-0.14554005167378,
1.42575200016845));
#17845=CARTESIAN_POINT('Ctrl Pts',(-0.0993960248003067,-0.118135852689175,
1.42310567028934));
#17846=CARTESIAN_POINT('Ctrl Pts',(-0.124806792024246,-0.0768886307561326,
1.42045934041024));
#17847=CARTESIAN_POINT('Ctrl Pts',(-0.138870387581649,-0.0540603453281256,
1.41899472846826));
#17848=CARTESIAN_POINT('Ctrl Pts',(-0.146051182757901,-0.0269918425378075,
1.41753011652627));
#17849=CARTESIAN_POINT('Ctrl Pts',(-0.146120987371435,4.2191387702159E-5,
1.41606550458429));
#17850=CARTESIAN_POINT('Ctrl Pts',(-0.146148882937928,7.6306569664006E-5,
1.40893449541571));
#17851=CARTESIAN_POINT('Ctrl Pts',(-0.146010322369016,-0.0292669616874671,
1.41052497222875));
#17852=CARTESIAN_POINT('Ctrl Pts',(-0.137450455640384,-0.0586846305953837,
1.4121154490418));
#17853=CARTESIAN_POINT('Ctrl Pts',(-0.121019719714466,-0.0827222215753489,
1.41370592585484));
#17854=CARTESIAN_POINT('Ctrl Pts',(-0.0936703391105966,-0.122733407165291,
1.4163533152291));
#17855=CARTESIAN_POINT('Ctrl Pts',(-0.0445135703510636,-0.147838304168576,
1.41900070460336));
#17856=CARTESIAN_POINT('Ctrl Pts',(0.00393424939099551,-0.146537573651384,
1.42164809397762));
#17857=CARTESIAN_POINT('Ctrl Pts',(0.0523820691330518,-0.145236843134192,
1.42429548335188));
#17858=CARTESIAN_POINT('Ctrl Pts',(0.100120939857634,-0.117530485096527,
1.42694287272614));
#17859=CARTESIAN_POINT('Ctrl Pts',(0.125284029446909,-0.0761094471358441,
1.4295902621004));
#17860=CARTESIAN_POINT('Ctrl Pts',(0.150447119036187,-0.0346884091751576,
1.43223765147466));
#17861=CARTESIAN_POINT('Ctrl Pts',(0.153034427490153,0.020447308708549,
1.43488504084892));
#17862=CARTESIAN_POINT('Ctrl Pts',(0.13186079120536,0.0640427391611241,
1.43753243022318));
#17863=CARTESIAN_POINT('Ctrl Pts',(0.110687154920568,0.107638169613697,
1.44017981959744));
#17864=CARTESIAN_POINT('Ctrl Pts',(0.0657525738970213,0.139693312635139,
1.4428272089717));
#17865=CARTESIAN_POINT('Ctrl Pts',(0.0176394768514684,0.145525221357757,
1.44547459834596));
#17866=CARTESIAN_POINT('Ctrl Pts',(-0.0304736201940859,0.151357130080375,
1.44812198772022));
#17867=CARTESIAN_POINT('Ctrl Pts',(-0.0817652332616461,0.130965804504167,
1.45076937709448));
#17868=CARTESIAN_POINT('Ctrl Pts',(-0.112741325423428,0.0936916042199666,
1.45341676646874));
#17869=CARTESIAN_POINT('Ctrl Pts',(-0.134261605244105,0.0677957870194472,
1.45525600945106));
#17870=CARTESIAN_POINT('Ctrl Pts',(-0.145976367207401,0.0337512577971725,
1.45709525243339));
#17871=CARTESIAN_POINT('Ctrl Pts',(-0.146248097568756,-0.000123763188177425,
1.45893449541571));
#17872=CARTESIAN_POINT('Origin',(0.,0.,-0.0924367114736175));
#17873=CARTESIAN_POINT('',(-0.117746618301147,-0.000105742458702955,1.48256328852638));
#17874=CARTESIAN_POINT('',(-0.117971241274414,-5.28325160115065E-6,1.49243671147361));
#17875=CARTESIAN_POINT('',(-0.117775,2.85464118895969E-14,-0.0924367114736175));
#17876=CARTESIAN_POINT('',(-0.117668597464313,0.00500517689812599,1.532225));
#17877=CARTESIAN_POINT('Ctrl Pts',(-0.117746618301147,-0.000105742458702949,
1.48256328852638));
#17878=CARTESIAN_POINT('Ctrl Pts',(-0.117836347163251,-0.0101121102621826,
1.48323921307631));
#17879=CARTESIAN_POINT('Ctrl Pts',(-0.112089674709738,-0.0591937430214443,
1.48656146750534));
#17880=CARTESIAN_POINT('Ctrl Pts',(-0.0435804807853106,-0.132222740314769,
1.49253005181348));
#17881=CARTESIAN_POINT('Ctrl Pts',(0.0874774386997331,-0.108286040948335,
1.50046904145078));
#17882=CARTESIAN_POINT('Ctrl Pts',(0.138385550162814,0.0147146982980264,
1.50840803108809));
#17883=CARTESIAN_POINT('Ctrl Pts',(0.0627460642121078,0.124368470664037,
1.51634702072539));
#17884=CARTESIAN_POINT('Ctrl Pts',(-0.0706026869052757,0.119928391791904,
1.5242860103627));
#17885=CARTESIAN_POINT('Ctrl Pts',(-0.116004137797729,0.0441355889673283,
1.5295786701209));
#17886=CARTESIAN_POINT('Ctrl Pts',(-0.117668597464313,0.00500517689812487,
1.532225));
#17887=CARTESIAN_POINT('',(-0.0334019664627544,0.1129391839063,1.53222500000001));
#17888=CARTESIAN_POINT('Origin',(0.,0.,1.532225));
#17889=CARTESIAN_POINT('Ctrl Pts',(-0.117971276761593,-5.28420699491729E-6,
1.49243671147361));
#17890=CARTESIAN_POINT('Ctrl Pts',(-0.117971582784674,-0.000385634193345565,
1.49246252744444));
#17891=CARTESIAN_POINT('Ctrl Pts',(-0.117794795258817,-0.0397700451254522,
1.49513573278954));
#17892=CARTESIAN_POINT('Ctrl Pts',(-0.0742871760264013,-0.117748889605885,
1.50045632750888));
#17893=CARTESIAN_POINT('Ctrl Pts',(0.0586284551779338,-0.126233948370975,
1.50839849563167));
#17894=CARTESIAN_POINT('Ctrl Pts',(0.137995068118234,-0.019163470063063,
1.51634066375444));
#17895=CARTESIAN_POINT('Ctrl Pts',(0.0906261803825392,0.105639137646141,
1.52428283187723));
#17896=CARTESIAN_POINT('Ctrl Pts',(0.00417072711528833,0.124051375507138,
1.52957761062575));
#17897=CARTESIAN_POINT('Ctrl Pts',(-0.0334019664627544,0.1129391839063,
1.53222500000001));
#17898=CARTESIAN_POINT('Origin',(0.,0.,-0.0924367114736175));
#17899=CARTESIAN_POINT('',(-0.117590702341447,3.3953472435133E-5,1.43256328852638));
#17900=CARTESIAN_POINT('',(-0.117692994131604,-9.95982882293356E-5,1.44243671147361));
#17901=CARTESIAN_POINT('',(-0.117775,2.85464118895969E-14,-0.0924367114736175));
#17902=CARTESIAN_POINT('Ctrl Pts',(-0.117590702341447,3.39534724351446E-5,
1.43256328852638));
#17903=CARTESIAN_POINT('Ctrl Pts',(-0.117534527156218,-0.0217216553118358,
1.43402790046837));
#17904=CARTESIAN_POINT('Ctrl Pts',(-0.101314495966545,-0.0828641818343832,
1.43813884228945));
#17905=CARTESIAN_POINT('Ctrl Pts',(-0.00292444232197888,-0.139176693688359,
1.44489611398964));
#17906=CARTESIAN_POINT('Ctrl Pts',(0.115350068603298,-0.0779297424218237,
1.45283510362695));
#17907=CARTESIAN_POINT('Ctrl Pts',(0.128028003046829,0.0546551750765237,
1.46077409326425));
#17908=CARTESIAN_POINT('Ctrl Pts',(0.0235079116789307,0.137209630484779,
1.46871308290156));
#17909=CARTESIAN_POINT('Ctrl Pts',(-0.0918059616614023,0.0978189523496558,
1.47597614798894));
#17910=CARTESIAN_POINT('Ctrl Pts',(-0.117485047349053,0.0290640819657798,
1.48059288319721));
#17911=CARTESIAN_POINT('Ctrl Pts',(-0.117746618301147,-0.000105742458702949,
1.48256328852638));
#17912=CARTESIAN_POINT('Ctrl Pts',(-0.117692994131604,-9.9598288229346E-5,
1.44243671147361));
#17913=CARTESIAN_POINT('Ctrl Pts',(-0.117789077779518,-0.0120777797952868,
1.44324485786555));
#17914=CARTESIAN_POINT('Ctrl Pts',(-0.110597905189529,-0.0631824179582176,
1.44670039363175));
#17915=CARTESIAN_POINT('Ctrl Pts',(-0.0368790902657646,-0.134252921254984,
1.45280331877221));
#17916=CARTESIAN_POINT('Ctrl Pts',(0.0928396680879532,-0.103751556080299,
1.46074548689499));
#17917=CARTESIAN_POINT('Ctrl Pts',(0.137511141307062,0.0217950526079239,
1.46868765501776));
#17918=CARTESIAN_POINT('Ctrl Pts',(0.0562018483347667,0.127378648737854,
1.47662982314055));
#17919=CARTESIAN_POINT('Ctrl Pts',(-0.0761502833827582,0.1162998103107,
1.48454617529249));
#17920=CARTESIAN_POINT('Ctrl Pts',(-0.117940200573233,0.0386186906477724,
1.48981513807018));
#17921=CARTESIAN_POINT('Ctrl Pts',(-0.117971276761593,-5.28420699491729E-6,
1.49243671147361));
#17922=CARTESIAN_POINT('Origin',(0.,0.,-0.0924367114736175));
#17923=CARTESIAN_POINT('',(-0.117872752581409,8.97255421561373E-5,1.38256328852638));
#17924=CARTESIAN_POINT('',(-0.117613151267609,6.14076272390171E-5,1.39243671147361));
#17925=CARTESIAN_POINT('',(-0.117775,2.85464118895969E-14,-0.0924367114736175));
#17926=CARTESIAN_POINT('Ctrl Pts',(-0.117872752581409,8.97255421561322E-5,
1.38256328852638));
#17927=CARTESIAN_POINT('Ctrl Pts',(-0.117591624875346,-0.0331778698171688,
1.38481658786042));
#17928=CARTESIAN_POINT('Ctrl Pts',(-0.0854981695600773,-0.105990339321694,
1.38971621707357));
#17929=CARTESIAN_POINT('Ctrl Pts',(0.0379781508110965,-0.133926497290667,
1.39726217616581));
#17930=CARTESIAN_POINT('Ctrl Pts',(0.133119345865688,-0.0407171622080862,
1.40520116580311));
#17931=CARTESIAN_POINT('Ctrl Pts',(0.106398871137127,0.0897659150453452,
1.41314015544042));
#17932=CARTESIAN_POINT('Ctrl Pts',(-0.0177224175491345,0.138074504763813,
1.42107914507772));
#17933=CARTESIAN_POINT('Ctrl Pts',(-0.105714817800915,0.0743914165933911,
1.42755352277305));
#17934=CARTESIAN_POINT('Ctrl Pts',(-0.11763602712824,0.0175874039095825,
1.43138157058926));
#17935=CARTESIAN_POINT('Ctrl Pts',(-0.117590702341447,3.39534724351446E-5,
1.43256328852638));
#17936=CARTESIAN_POINT('Ctrl Pts',(-0.117613151267609,6.1407627239024E-5,
1.39243671147361));
#17937=CARTESIAN_POINT('Ctrl Pts',(-0.117501644803633,-0.0235525549213426,
1.39402718828666));
#17938=CARTESIAN_POINT('Ctrl Pts',(-0.0991469449676741,-0.0866320980727062,
1.39826505447396));
#17939=CARTESIAN_POINT('Ctrl Pts',(0.00373660876362508,-0.139175849115243,
1.40515031003553));
#17940=CARTESIAN_POINT('Ctrl Pts',(0.118990018389619,-0.0722858665142316,
1.41309247815831));
#17941=CARTESIAN_POINT('Ctrl Pts',(0.125236419206141,0.0608253567263532,
1.42103464628109));
#17942=CARTESIAN_POINT('Ctrl Pts',(0.0167532566496359,0.13821437898841,
1.42897681440387));
#17943=CARTESIAN_POINT('Ctrl Pts',(-0.0944771051913143,0.0939940009069027,
1.43611083613471));
#17944=CARTESIAN_POINT('Ctrl Pts',(-0.117474319425011,0.0271612872365273,
1.44059746849129));
#17945=CARTESIAN_POINT('Ctrl Pts',(-0.117692994131604,-9.9598288229346E-5,
1.44243671147361));
#17946=CARTESIAN_POINT('Origin',(0.,0.,-0.0924367114736175));
#17947=CARTESIAN_POINT('',(-0.117871679003533,-9.01049542302267E-5,1.33256328852638));
#17948=CARTESIAN_POINT('',(-0.117917347702326,6.89762296073142E-5,1.34243671147361));
#17949=CARTESIAN_POINT('',(-0.117775,2.85464118895969E-14,-0.0924367114736175));
#17950=CARTESIAN_POINT('Ctrl Pts',(-0.117871679003533,-9.01049542302501E-5,
1.33256328852638));
#17951=CARTESIAN_POINT('Ctrl Pts',(-0.117921183610054,-0.00593170075121234,
1.33295894537338));
#17952=CARTESIAN_POINT('Ctrl Pts',(-0.114870949065289,-0.0507926200311143,
1.33600093209947));
#17953=CARTESIAN_POINT('Ctrl Pts',(-0.0572704544775333,-0.126880813469472,
1.34168924870467));
#17954=CARTESIAN_POINT('Ctrl Pts',(0.0755477687720905,-0.116923823242002,
1.34962823834197));
#17955=CARTESIAN_POINT('Ctrl Pts',(0.13920718769651,6.89141801743488E-5,
1.35756722797928));
#17956=CARTESIAN_POINT('Ctrl Pts',(0.0754319660950179,0.116998564767658,
1.36550621761658));
#17957=CARTESIAN_POINT('Ctrl Pts',(-0.0573960494825499,0.126824048933643,
1.37344520725389));
#17958=CARTESIAN_POINT('Ctrl Pts',(-0.11489462347839,0.0507140179075799,
1.37913089755716));
#17959=CARTESIAN_POINT('Ctrl Pts',(-0.117921788132912,0.00589240827474643,
1.38217025798132));
#17960=CARTESIAN_POINT('Ctrl Pts',(-0.117872752581409,8.97255421561322E-5,
1.38256328852638));
#17961=CARTESIAN_POINT('Ctrl Pts',(-0.117917347702326,6.89762296073276E-5,
1.34243671147361));
#17962=CARTESIAN_POINT('Ctrl Pts',(-0.117673982084908,-0.0349283870656527,
1.34480951870776));
#17963=CARTESIAN_POINT('Ctrl Pts',(-0.0826049238592893,-0.109396528181867,
1.34982971531618));
#17964=CARTESIAN_POINT('Ctrl Pts',(0.0440301174146577,-0.132080378229483,
1.35749730129884));
#17965=CARTESIAN_POINT('Ctrl Pts',(0.13486394497766,-0.0345773583278084,
1.36543946942163));
#17966=CARTESIAN_POINT('Ctrl Pts',(0.102148545386143,0.0946020732301706,
1.3733816375444));
#17967=CARTESIAN_POINT('Ctrl Pts',(-0.0241454188302812,0.137116288461919,
1.38132380566719));
#17968=CARTESIAN_POINT('Ctrl Pts',(-0.107458038693719,0.07065895059964,
1.38767549697692));
#17969=CARTESIAN_POINT('Ctrl Pts',(-0.117687250167678,0.015753490298928,
1.3913797989124));
#17970=CARTESIAN_POINT('Ctrl Pts',(-0.117613151267609,6.1407627239024E-5,
1.39243671147361));
#17971=CARTESIAN_POINT('Origin',(0.,0.,-0.0924367114736175));
#17972=CARTESIAN_POINT('',(-0.117590388001671,-3.33269891443968E-5,1.28256328852638));
#17973=CARTESIAN_POINT('',(-0.117823716245033,-0.000102811805890834,1.29243671147362));
#17974=CARTESIAN_POINT('',(-0.117775,2.85464118895969E-14,-0.0924367114736175));
#17975=CARTESIAN_POINT('Ctrl Pts',(-0.117590388001671,-3.33269891444124E-5,
1.28256328852638));
#17976=CARTESIAN_POINT('Ctrl Pts',(-0.117634977734708,-0.017625925033684,
1.28374763276543));
#17977=CARTESIAN_POINT('Ctrl Pts',(-0.105676786131388,-0.0744702911817869,
1.28757830688358));
#17978=CARTESIAN_POINT('Ctrl Pts',(-0.0175857351491984,-0.138091953858251,
1.29405531088083));
#17979=CARTESIAN_POINT('Ctrl Pts',(0.106487712804436,-0.089660542174548,
1.30199430051814));
#17980=CARTESIAN_POINT('Ctrl Pts',(0.133078957772855,0.0408489510387311,
1.30993329015544));
#17981=CARTESIAN_POINT('Ctrl Pts',(0.0378455373822902,0.133964029124136,
1.31787227979275));
#17982=CARTESIAN_POINT('Ctrl Pts',(-0.0855601048685178,0.105915403748908,
1.32541561258306));
#17983=CARTESIAN_POINT('Ctrl Pts',(-0.117590074669608,0.0331395035428114,
1.33031261549427));
#17984=CARTESIAN_POINT('Ctrl Pts',(-0.117871679003533,-9.01049542302501E-5,
1.33256328852638));
#17985=CARTESIAN_POINT('Ctrl Pts',(-0.117823716245033,-0.000102811805890825,
1.29243671147362));
#17986=CARTESIAN_POINT('Ctrl Pts',(-0.117892441435953,-0.00760726064997237,
1.29294445975461));
#17987=CARTESIAN_POINT('Ctrl Pts',(-0.113819337750002,-0.0541654333254181,
1.29609959740987));
#17988=CARTESIAN_POINT('Ctrl Pts',(-0.0518146499729274,-0.129225073214149,
1.30190212443939));
#17989=CARTESIAN_POINT('Ctrl Pts',(0.0805213734929343,-0.11357898534207,
1.30984429256217));
#17990=CARTESIAN_POINT('Ctrl Pts',(0.1390915465469,0.0061171215252809,1.31778646068495));
#17991=CARTESIAN_POINT('Ctrl Pts',(0.0702395735793815,0.120209316621791,
1.32572862880773));
#17992=CARTESIAN_POINT('Ctrl Pts',(-0.0629590648350173,0.124177428154433,
1.33367079693051));
#17993=CARTESIAN_POINT('Ctrl Pts',(-0.115917830154768,0.0471875384414626,
1.33924015781913));
#17994=CARTESIAN_POINT('Ctrl Pts',(-0.117945510062545,0.00411888419242175,
1.3421621293335));
#17995=CARTESIAN_POINT('Ctrl Pts',(-0.117917347702326,6.89762296073276E-5,
1.34243671147361));
#17996=CARTESIAN_POINT('Origin',(0.,0.,-0.0924367114736175));
#17997=CARTESIAN_POINT('',(-0.11774949833287,0.000107383800510985,1.23256328852638));
#17998=CARTESIAN_POINT('',(-0.117581795058195,-8.20683476789735E-6,1.24243671147361));
#17999=CARTESIAN_POINT('',(-0.117775,2.85464118895969E-14,-0.0924367114736175));
#18000=CARTESIAN_POINT('Ctrl Pts',(-0.11774949833287,0.000107383800510997,
1.23256328852638));
#18001=CARTESIAN_POINT('Ctrl Pts',(-0.1174869159147,-0.0291008736543001,
1.23453632015749));
#18002=CARTESIAN_POINT('Ctrl Pts',(-0.0917482398636095,-0.0978979247776974,
1.23915568166769));
#18003=CARTESIAN_POINT('Ctrl Pts',(0.0236422145726536,-0.137184880695923,
1.246421373057));
#18004=CARTESIAN_POINT('Ctrl Pts',(0.128082862902196,-0.0545291301253663,
1.2543603626943));
#18005=CARTESIAN_POINT('Ctrl Pts',(0.115272428336817,0.0780443019497631,
1.26229935233161));
#18006=CARTESIAN_POINT('Ctrl Pts',(-0.00306201423577413,0.139173524314926,
1.27023834196891));
#18007=CARTESIAN_POINT('Ctrl Pts',(-0.101358337705897,0.08278581645186,
1.27699298736717));
#18008=CARTESIAN_POINT('Ctrl Pts',(-0.117535345263889,0.02168343817453,
1.28110130288633));
#18009=CARTESIAN_POINT('Ctrl Pts',(-0.117590388001671,-3.33269891444124E-5,
1.28256328852638));
#18010=CARTESIAN_POINT('Ctrl Pts',(-0.117581795058195,-8.20683476789562E-6,
1.24243671147361));
#18011=CARTESIAN_POINT('Ctrl Pts',(-0.117593699448189,-0.0191748937105988,
1.24372679017572));
#18012=CARTESIAN_POINT('Ctrl Pts',(-0.104100832827715,-0.0776580224685839,
1.24766425825208));
#18013=CARTESIAN_POINT('Ctrl Pts',(-0.0120149744006178,-0.138706589206355,
1.25424911570271));
#18014=CARTESIAN_POINT('Ctrl Pts',(0.110059129405696,-0.0852693704304675,
1.26219128382548));
#18015=CARTESIAN_POINT('Ctrl Pts',(0.13130776387206,0.0462833517151888,
1.27013345194827));
#18016=CARTESIAN_POINT('Ctrl Pts',(0.0322649968732001,0.135435768819968,
1.27807562007105));
#18017=CARTESIAN_POINT('Ctrl Pts',(-0.0881142830049797,0.102747609761224,
1.28551003991283));
#18018=CARTESIAN_POINT('Ctrl Pts',(-0.117534109666069,0.0315207854174475,
1.29029707038035));
#18019=CARTESIAN_POINT('Ctrl Pts',(-0.117823716245033,-0.000102811805890825,
1.29243671147362));
#18020=CARTESIAN_POINT('Origin',(0.,0.,-0.0924367114736175));
#18021=CARTESIAN_POINT('',(-0.117957988745754,-3.12301727557783E-5,1.18256328852638));
#18022=CARTESIAN_POINT('',(-0.117793553451004,0.000106755881474893,1.19243671147362));
#18023=CARTESIAN_POINT('',(-0.117775,2.85464118895969E-14,-0.0924367114736175));
#18024=CARTESIAN_POINT('Ctrl Pts',(-0.117957988745754,-3.12301727557569E-5,
1.18256328852638));
#18025=CARTESIAN_POINT('Ctrl Pts',(-0.117964007145535,-0.00173159226684161,
1.18267867767044));
#18026=CARTESIAN_POINT('Ctrl Pts',(-0.117160216762375,-0.0424221720604921,
1.1854403966936));
#18027=CARTESIAN_POINT('Ctrl Pts',(-0.0703321751825429,-0.12013338809653,
1.19084844559586));
#18028=CARTESIAN_POINT('Ctrl Pts',(0.0627954496153871,-0.124239193932754,
1.19878743523316));
#18029=CARTESIAN_POINT('Ctrl Pts',(0.138438143943654,-0.0146125323915816,
1.20672642487047));
#18030=CARTESIAN_POINT('Ctrl Pts',(0.0873502052771435,0.108390901091839,
1.21466541450777));
#18031=CARTESIAN_POINT('Ctrl Pts',(-0.043700859820065,0.132169893139269,
1.22260440414508));
#18032=CARTESIAN_POINT('Ctrl Pts',(-0.112119660921406,0.0591163174148552,
1.22857036215128));
#18033=CARTESIAN_POINT('Ctrl Pts',(-0.117839104743291,0.0100747194789664,
1.23188999027838));
#18034=CARTESIAN_POINT('Ctrl Pts',(-0.11774949833287,0.000107383800510997,
1.23256328852638));
#18035=CARTESIAN_POINT('Ctrl Pts',(-0.117793553451004,0.000106755881474891,
1.19243671147362));
#18036=CARTESIAN_POINT('Ctrl Pts',(-0.117510050331475,-0.0305433296418112,
1.19450912059683));
#18037=CARTESIAN_POINT('Ctrl Pts',(-0.0896091397727994,-0.100804620014092,
1.19922891909429));
#18038=CARTESIAN_POINT('Ctrl Pts',(0.0288222657999454,-0.136209964735594,
1.20659610696603));
#18039=CARTESIAN_POINT('Ctrl Pts',(0.130092623711363,-0.0495962373069701,
1.21453827508881));
#18040=CARTESIAN_POINT('Ctrl Pts',(0.112184773380136,0.082452738709893,
1.22248044321158));
#18041=CARTESIAN_POINT('Ctrl Pts',(-0.00849585454694533,0.138966535376798,
1.23042261133437));
#18042=CARTESIAN_POINT('Ctrl Pts',(-0.103054997843392,0.079672038485689,
1.23707470075504));
#18043=CARTESIAN_POINT('Ctrl Pts',(-0.11756927027536,0.0201573447738481,
1.24107940080146));
#18044=CARTESIAN_POINT('Ctrl Pts',(-0.117581795058195,-8.20683476789562E-6,
1.24243671147361));
#18045=CARTESIAN_POINT('Origin',(0.,0.,-0.0924367114736175));
#18046=CARTESIAN_POINT('',(-0.117657565919426,-8.78585414499747E-5,1.13256328852638));
#18047=CARTESIAN_POINT('',(-0.117937823388479,-5.4172489969917E-5,1.14243671147362));
#18048=CARTESIAN_POINT('',(-0.117775,2.85464118895969E-14,-0.0924367114736175));
#18049=CARTESIAN_POINT('Ctrl Pts',(-0.117657565919426,-8.78585414499974E-5,
1.13256328852638));
#18050=CARTESIAN_POINT('Ctrl Pts',(-0.11775046973706,-0.0134980674796043,
1.13346736506249));
#18051=CARTESIAN_POINT('Ctrl Pts',(-0.109441032251172,-0.0660497484721492,
1.13701777147771));
#18052=CARTESIAN_POINT('Ctrl Pts',(-0.0320511128216771,-0.13546723577438,
1.14321450777202));
#18053=CARTESIAN_POINT('Ctrl Pts',(0.0964380908528195,-0.100390938007982,
1.15115349740933));
#18054=CARTESIAN_POINT('Ctrl Pts',(0.136644831685568,0.0265863832644056,
1.15909248704664));
#18055=CARTESIAN_POINT('Ctrl Pts',(0.0517625939920979,0.129225692742072,
1.16703147668394));
#18056=CARTESIAN_POINT('Ctrl Pts',(-0.0785823129332351,0.113795317289389,
1.17485507717719));
#18057=CARTESIAN_POINT('Ctrl Pts',(-0.117825981412732,0.0372644419932696,
1.18003234779134));
#18058=CARTESIAN_POINT('Ctrl Pts',(-0.117957988745754,-3.12301727557569E-5,
1.18256328852638));
#18059=CARTESIAN_POINT('Ctrl Pts',(-0.117937823388479,-5.41724899699178E-5,
1.14243671147362));
#18060=CARTESIAN_POINT('Ctrl Pts',(-0.117955293269658,-0.0031110520517566,
1.14264406164367));
#18061=CARTESIAN_POINT('Ctrl Pts',(-0.116460933142332,-0.0451799670343263,
1.14549880118799));
#18062=CARTESIAN_POINT('Ctrl Pts',(-0.0660858892268601,-0.122541963197144,
1.15100093010657));
#18063=CARTESIAN_POINT('Ctrl Pts',(0.0671705316110708,-0.121950798202395,
1.15894309822935));
#18064=CARTESIAN_POINT('Ctrl Pts',(0.138891844802359,-0.00964017357273747,
1.16688526635212));
#18065=CARTESIAN_POINT('Ctrl Pts',(0.0833739592533277,0.111501840422208,
1.17482743447491));
#18066=CARTESIAN_POINT('Ctrl Pts',(-0.0485230383040216,0.130496713571114,
1.18276960259768));
#18067=CARTESIAN_POINT('Ctrl Pts',(-0.113150295826959,0.0561813708375219,
1.18863936159726));
#18068=CARTESIAN_POINT('Ctrl Pts',(-0.117872210070015,0.00861047923971886,
1.19186173122257));
#18069=CARTESIAN_POINT('Ctrl Pts',(-0.117793553451004,0.000106755881474891,
1.19243671147362));
#18070=CARTESIAN_POINT('Origin',(0.,0.,-0.0924367114736175));
#18071=CARTESIAN_POINT('',(-0.117641451221435,8.0229283111194E-5,1.08256328852638));
#18072=CARTESIAN_POINT('',(-0.117630591849015,-7.42484764288953E-5,1.09243671147362));
#18073=CARTESIAN_POINT('',(-0.117775,2.85464118895969E-14,-0.0924367114736175));
#18074=CARTESIAN_POINT('Ctrl Pts',(-0.117641451221435,8.02292831111745E-5,
1.08256328852638));
#18075=CARTESIAN_POINT('Ctrl Pts',(-0.117483998834985,-0.0250372639622414,
1.08425605245455));
#18076=CARTESIAN_POINT('Ctrl Pts',(-0.0972946570053161,-0.0896524615425008,
1.08859514626182));
#18077=CARTESIAN_POINT('Ctrl Pts',(0.00904258428980543,-0.13891320121148,
1.09558056994819));
#18078=CARTESIAN_POINT('Ctrl Pts',(0.121617839487272,-0.067732908692211,
1.1035195595855));
#18079=CARTESIAN_POINT('Ctrl Pts',(0.122860297649024,0.0654522196953821,
1.1114585492228));
#18080=CARTESIAN_POINT('Ctrl Pts',(0.0116325734791967,0.138720326685422,
1.11939753886011));
#18081=CARTESIAN_POINT('Ctrl Pts',(-0.096364912740844,0.0911171059582243,
1.1264324519613));
#18082=CARTESIAN_POINT('Ctrl Pts',(-0.117478530206868,0.0257550656131636,
1.13082103518339));
#18083=CARTESIAN_POINT('Ctrl Pts',(-0.117657565919426,-8.78585414499974E-5,
1.13256328852638));
#18084=CARTESIAN_POINT('Ctrl Pts',(-0.117630591849015,-7.42484764288814E-5,
1.09243671147362));
#18085=CARTESIAN_POINT('Ctrl Pts',(-0.117715241483118,-0.0147626739157663,
1.09342639206478));
#18086=CARTESIAN_POINT('Ctrl Pts',(-0.108350501834675,-0.0686384992808382,
1.0970634620302));
#18087=CARTESIAN_POINT('Ctrl Pts',(-0.0276126195379174,-0.136460326620484,
1.10334792136989));
#18088=CARTESIAN_POINT('Ctrl Pts',(0.0997182217817603,-0.0971604536002107,
1.11129008949267));
#18089=CARTESIAN_POINT('Ctrl Pts',(0.135696927507188,0.0311483765905046,
1.11923225761545));
#18090=CARTESIAN_POINT('Ctrl Pts',(0.0473633069609982,0.130922093830007,
1.12717442573822));
#18091=CARTESIAN_POINT('Ctrl Pts',(-0.0809210029008042,0.111284164335459,
1.13490924369095));
#18092=CARTESIAN_POINT('Ctrl Pts',(-0.117732242679493,0.0359183370635313,
1.13999667226941));
#18093=CARTESIAN_POINT('Ctrl Pts',(-0.117937823388479,-5.41724899699178E-5,
1.14243671147362));
#18094=CARTESIAN_POINT('Origin',(0.,0.,-0.0924367114736175));
#18095=CARTESIAN_POINT('',(-0.117948158721073,4.38502512853227E-5,1.03256328852638));
#18096=CARTESIAN_POINT('',(-0.117667547954054,9.20194976846214E-5,1.04243671147362));
#18097=CARTESIAN_POINT('',(-0.117775,2.85464118895969E-14,-0.0924367114736175));
#18098=CARTESIAN_POINT('Ctrl Pts',(-0.117948158721073,4.38502512853157E-5,
1.03256328852638));
#18099=CARTESIAN_POINT('Ctrl Pts',(-0.117773439871091,-0.0365306738650768,
1.03504473984661));
#18100=CARTESIAN_POINT('Ctrl Pts',(-0.0798690478914953,-0.112422454385097,
1.04017252104593));
#18101=CARTESIAN_POINT('Ctrl Pts',(0.0493427524230464,-0.130168884856471,
1.04794663212436));
#18102=CARTESIAN_POINT('Ctrl Pts',(0.136125055048066,-0.0291310004912345,
1.05588562176166));
#18103=CARTESIAN_POINT('Ctrl Pts',(0.0982941990358779,0.0985743183458784,
1.06382461139897));
#18104=CARTESIAN_POINT('Ctrl Pts',(-0.0295182596522469,0.136041604476578,
1.07176360103627));
#18105=CARTESIAN_POINT('Ctrl Pts',(-0.108818061611988,0.067537217334308,
1.07800982674541));
#18106=CARTESIAN_POINT('Ctrl Pts',(-0.11773014713001,0.0142293884972668,
1.08160972257545));
#18107=CARTESIAN_POINT('Ctrl Pts',(-0.117641451221435,8.02292831111745E-5,
1.08256328852638));
#18108=CARTESIAN_POINT('Ctrl Pts',(-0.117667547954054,9.20194976846197E-5,
1.04243671147362));
#18109=CARTESIAN_POINT('Ctrl Pts',(-0.117475882803567,-0.0261866690710452,
1.04420872248589));
#18110=CARTESIAN_POINT('Ctrl Pts',(-0.0957916308421219,-0.0920126959480487,
1.04862812287242));
#18111=CARTESIAN_POINT('Ctrl Pts',(0.0132451643780021,-0.13859452774087,
1.05569491263321));
#18112=CARTESIAN_POINT('Ctrl Pts',(0.123654649330263,-0.0639797248987874,
1.06363708075599));
#18113=CARTESIAN_POINT('Ctrl Pts',(0.120783771971213,0.0692470788374567,
1.07157924887876));
#18114=CARTESIAN_POINT('Ctrl Pts',(0.00726255089817806,0.139036444335888,
1.07952141700155));
#18115=CARTESIAN_POINT('Ctrl Pts',(-0.0979368667310299,0.0886295245336828,
1.08647390453316));
#18116=CARTESIAN_POINT('Ctrl Pts',(-0.117488804242801,0.0245287720112504,
1.09077900269052));
#18117=CARTESIAN_POINT('Ctrl Pts',(-0.117630591849015,-7.42484764288814E-5,
1.09243671147362));
#18118=CARTESIAN_POINT('Origin',(0.,0.,-0.0924367114736175));
#18119=CARTESIAN_POINT('',(-0.117771476475648,-0.000107683352847938,0.982563288526384));
#18120=CARTESIAN_POINT('',(-0.11796176292438,2.53781033017321E-5,0.992436711473616));
#18121=CARTESIAN_POINT('',(-0.117775,2.85464118895969E-14,-0.0924367114736175));
#18122=CARTESIAN_POINT('Ctrl Pts',(-0.117771476475648,-0.000107683352847945,
0.982563288526384));
#18123=CARTESIAN_POINT('Ctrl Pts',(-0.117856103358663,-0.00933799346614349,
0.983187097359559));
#18124=CARTESIAN_POINT('Ctrl Pts',(-0.112646870919438,-0.057630810124202,
0.986457236071836));
#18125=CARTESIAN_POINT('Ctrl Pts',(-0.0461590140787468,-0.131331607851033,
0.992373704663214));
#18126=CARTESIAN_POINT('Ctrl Pts',(0.0853128637208732,-0.110001641284132,
1.00031269430052));
#18127=CARTESIAN_POINT('Ctrl Pts',(0.138686661656432,0.0120272889735618,
1.00825168393783));
#18128=CARTESIAN_POINT('Ctrl Pts',(0.0651023256631918,0.123046060459907,
1.01619067357513));
#18129=CARTESIAN_POINT('Ctrl Pts',(-0.0680787277209358,0.121424596492465,
1.02412966321244));
#18130=CARTESIAN_POINT('Ctrl Pts',(-0.116790117880403,0.0438975063746073,
1.02958720152952));
#18131=CARTESIAN_POINT('Ctrl Pts',(-0.11795976781127,0.00247402277930658,
1.0323984099675));
#18132=CARTESIAN_POINT('Ctrl Pts',(-0.117948158721073,4.38502512853157E-5,
1.03256328852638));
#18133=CARTESIAN_POINT('Ctrl Pts',(-0.11796176292438,2.53781033017319E-5,
0.992436711473616));
#18134=CARTESIAN_POINT('Ctrl Pts',(-0.117851518882229,-0.0376119105440478,
0.994991052906992));
#18135=CARTESIAN_POINT('Ctrl Pts',(-0.077958511321084,-0.114458475672252,
1.00019278371463));
#18136=CARTESIAN_POINT('Ctrl Pts',(0.0529591494285269,-0.128760265574912,
1.00804190389653));
#18137=CARTESIAN_POINT('Ctrl Pts',(0.136912761112491,-0.0252739657289669,
1.0159840720193));
#18138=CARTESIAN_POINT('Ctrl Pts',(0.0954402180350474,0.101365883217864,
1.02392624014209));
#18139=CARTESIAN_POINT('Ctrl Pts',(-0.0334653697086341,0.135144169424284,
1.03186840826486));
#18140=CARTESIAN_POINT('Ctrl Pts',(-0.109792739119276,0.0652029671457737,
1.03803856537538));
#18141=CARTESIAN_POINT('Ctrl Pts',(-0.117762231070763,0.0130737646421874,
1.04156133311163));
#18142=CARTESIAN_POINT('Ctrl Pts',(-0.117667547954054,9.20194976846197E-5,
1.04243671147362));
#18143=CARTESIAN_POINT('Origin',(0.,0.,-0.0924367114736175));
#18144=CARTESIAN_POINT('',(-0.117585265278523,2.16484251076657E-5,0.932563288526384));
#18145=CARTESIAN_POINT('',(-0.117742563953077,-0.000107211314308964,0.942436711473616));
#18146=CARTESIAN_POINT('',(-0.117775,2.85464118895969E-14,-0.0924367114736175));
#18147=CARTESIAN_POINT('Ctrl Pts',(-0.117585265278523,2.16484251076635E-5,
0.932563288526384));
#18148=CARTESIAN_POINT('Ctrl Pts',(-0.117550805757046,-0.0209622679161363,
0.933975784751614));
#18149=CARTESIAN_POINT('Ctrl Pts',(-0.102172791552808,-0.0813069697478888,
0.938034610855947));
#18150=CARTESIAN_POINT('Ctrl Pts',(-0.00565790085648466,-0.139092177922979,
0.944739766839381));
#18151=CARTESIAN_POINT('Ctrl Pts',(0.113796373024222,-0.0801812402497705,
0.952678756476687));
#18152=CARTESIAN_POINT('Ctrl Pts',(0.129077866376032,0.0521301276928276,
0.960617746113992));
#18153=CARTESIAN_POINT('Ctrl Pts',(0.026197419344502,0.13671993644362,0.968556735751298));
#18154=CARTESIAN_POINT('Ctrl Pts',(-0.0906967139502387,0.0993396518733501,
0.975871916555428));
#18155=CARTESIAN_POINT('Ctrl Pts',(-0.117497098103867,0.02981894716558,
0.980540767480457));
#18156=CARTESIAN_POINT('Ctrl Pts',(-0.117771476475648,-0.000107683352847945,
0.982563288526384));
#18157=CARTESIAN_POINT('Ctrl Pts',(-0.117742563953077,-0.000107211314308957,
0.942436711473616));
#18158=CARTESIAN_POINT('Ctrl Pts',(-0.117833632602859,-0.0103126986533654,
0.943125993953839));
#18159=CARTESIAN_POINT('Ctrl Pts',(-0.111944766202914,-0.0596118697348184,
0.946462665808322));
#18160=CARTESIAN_POINT('Ctrl Pts',(-0.0428565117498991,-0.132465832952297,
0.952446727037066));
#18161=CARTESIAN_POINT('Ctrl Pts',(0.0880997963686447,-0.107806787258123,
0.960388895159846));
#18162=CARTESIAN_POINT('Ctrl Pts',(0.138347640177547,0.0156143509765511,
0.968331063282625));
#18163=CARTESIAN_POINT('Ctrl Pts',(0.061854832590724,0.124731139593481,
0.976273231405407));
#18164=CARTESIAN_POINT('Ctrl Pts',(-0.0713033562375951,0.119581390225944,
0.984215399528185));
#18165=CARTESIAN_POINT('Ctrl Pts',(-0.117322772537986,0.0417718924351975,
0.989603226217589));
#18166=CARTESIAN_POINT('Ctrl Pts',(-0.11796577882491,0.00139640554830399,
0.992343663532733));
#18167=CARTESIAN_POINT('Ctrl Pts',(-0.11796176292438,2.53781033017319E-5,
0.992436711473616));
#18168=CARTESIAN_POINT('Origin',(0.,0.,-0.0924367114736175));
#18169=CARTESIAN_POINT('',(-0.117850913371472,9.6525574830472E-5,0.882563288526384));
#18170=CARTESIAN_POINT('',(-0.117591231449503,3.54948526558943E-5,0.892436711473616));
#18171=CARTESIAN_POINT('',(-0.117775,2.85464118895969E-14,-0.0924367114736175));
#18172=CARTESIAN_POINT('Ctrl Pts',(-0.117850913371472,9.65255748304767E-5,
0.882563288526384));
#18173=CARTESIAN_POINT('Ctrl Pts',(-0.117563006813672,-0.0324172738354332,
0.884764472143669));
#18174=CARTESIAN_POINT('Ctrl Pts',(-0.0867151192651892,-0.104499852648429,
0.889611985640057));
#18175=CARTESIAN_POINT('Ctrl Pts',(0.0353397195745277,-0.134646760160997,
0.897105829015547));
#18176=CARTESIAN_POINT('Ctrl Pts',(0.132293719443212,-0.0433245611326863,
0.905044818652852));
#18177=CARTESIAN_POINT('Ctrl Pts',(0.108141885842356,0.0876583043865096,
0.912983808290157));
#18178=CARTESIAN_POINT('Ctrl Pts',(-0.0150064327997127,0.138395999855801,
0.920922797927463));
#18179=CARTESIAN_POINT('Ctrl Pts',(-0.104951114476159,0.0759553573435841,
0.927449291339539));
#18180=CARTESIAN_POINT('Ctrl Pts',(-0.117615366114572,0.01835136974357,
0.931329454872513));
#18181=CARTESIAN_POINT('Ctrl Pts',(-0.117585265278523,2.16484251076635E-5,
0.932563288526384));
#18182=CARTESIAN_POINT('Ctrl Pts',(-0.117591231449503,3.54948526559117E-5,
0.892436711473616));
#18183=CARTESIAN_POINT('Ctrl Pts',(-0.117532234588281,-0.0218238662162972,
0.893908324374946));
#18184=CARTESIAN_POINT('Ctrl Pts',(-0.101194437785642,-0.0830895288483654,
0.898027326650536));
#18185=CARTESIAN_POINT('Ctrl Pts',(-0.00250162451743248,-0.139203517821528,
0.904793718300386));
#18186=CARTESIAN_POINT('Ctrl Pts',(0.115632500949424,-0.0775435504945224,
0.912735886423165));
#18187=CARTESIAN_POINT('Ctrl Pts',(0.127835376168433,0.0551542754370876,
0.920678054545947));
#18188=CARTESIAN_POINT('Ctrl Pts',(0.0229279137899797,0.137325118854324,
0.928620222668725));
#18189=CARTESIAN_POINT('Ctrl Pts',(-0.0920562790907298,0.0974788594069619,
0.935873108311283));
#18190=CARTESIAN_POINT('Ctrl Pts',(-0.117483857027998,0.0288844367965532,
0.94047860457958));
#18191=CARTESIAN_POINT('Ctrl Pts',(-0.117742563953077,-0.000107211314308957,
0.942436711473616));
#18192=CARTESIAN_POINT('Origin',(0.,0.,-0.0924367114736175));
#18193=CARTESIAN_POINT('',(-0.11789232318732,-8.18790992476613E-5,0.832563288526384));
#18194=CARTESIAN_POINT('',(-0.117872825429845,8.99519344067963E-5,0.842436711473616));
#18195=CARTESIAN_POINT('',(-0.117775,2.85464118895969E-14,-0.0924367114736175));
#18196=CARTESIAN_POINT('Ctrl Pts',(-0.11789232318732,-8.18790992476734E-5,
0.832563288526384));
#18197=CARTESIAN_POINT('Ctrl Pts',(-0.117932494517479,-0.00515170743829337,
0.832906829656623));
#18198=CARTESIAN_POINT('Ctrl Pts',(-0.115332713682068,-0.0492334187378749,
0.835896700665964));
#18199=CARTESIAN_POINT('Ctrl Pts',(-0.059752088941783,-0.125731196083361,
0.841532901554406));
#18200=CARTESIAN_POINT('Ctrl Pts',(0.0732361146625898,-0.118385460722959,
0.849471891191712));
#18201=CARTESIAN_POINT('Ctrl Pts',(0.139181674492094,-0.00266594955618734,
0.857410880829018));
#18202=CARTESIAN_POINT('Ctrl Pts',(0.077715950067195,0.115494055719818,
0.865349870466323));
#18203=CARTESIAN_POINT('Ctrl Pts',(-0.0548934004223171,0.127927168308903,
0.87328886010363));
#18204=CARTESIAN_POINT('Ctrl Pts',(-0.114416768398411,0.0522742940766184,
0.879026666123649));
#18205=CARTESIAN_POINT('Ctrl Pts',(-0.117909136832228,0.0066718045071592,
0.882118142264567));
#18206=CARTESIAN_POINT('Ctrl Pts',(-0.117850913371472,9.65255748304767E-5,
0.882563288526384));
#18207=CARTESIAN_POINT('Ctrl Pts',(-0.117872825429845,8.99519344067998E-5,
0.842436711473616));
#18208=CARTESIAN_POINT('Ctrl Pts',(-0.117591169542271,-0.0331870933343037,
0.844690654796053));
#18209=CARTESIAN_POINT('Ctrl Pts',(-0.0854771005934613,-0.106025606004136,
0.84959198749275));
#18210=CARTESIAN_POINT('Ctrl Pts',(0.0380692928980519,-0.133920149482284,
0.857140709563706));
#18211=CARTESIAN_POINT('Ctrl Pts',(0.133179650076608,-0.0405839661022353,
0.865082877686486));
#18212=CARTESIAN_POINT('Ctrl Pts',(0.106283765719693,0.0899312995767124,
0.873025045809266));
#18213=CARTESIAN_POINT('Ctrl Pts',(-0.0179789669825735,0.138060255849953,
0.880967213932046));
#18214=CARTESIAN_POINT('Ctrl Pts',(-0.105798194743126,0.0742290978659706,
0.887437769153496));
#18215=CARTESIAN_POINT('Ctrl Pts',(-0.117638368248411,0.0175004969839459,
0.891260935000686));
#18216=CARTESIAN_POINT('Ctrl Pts',(-0.117591231449503,3.54948526559117E-5,
0.892436711473616));
#18217=CARTESIAN_POINT('Origin',(0.,0.,-0.0924367114736175));
#18218=CARTESIAN_POINT('',(-0.117598114366551,-4.51832715892789E-5,0.782563288526384));
#18219=CARTESIAN_POINT('',(-0.117874685330111,-8.92836445515327E-5,0.792436711473617));
#18220=CARTESIAN_POINT('',(-0.117775,2.85464118895969E-14,-0.0924367114736175));
#18221=CARTESIAN_POINT('Ctrl Pts',(-0.117598114366551,-4.518327158929E-5,
0.782563288526384));
#18222=CARTESIAN_POINT('Ctrl Pts',(-0.117656123976761,-0.0168608793038394,
0.783695517048678));
#18223=CARTESIAN_POINT('Ctrl Pts',(-0.106420815930739,-0.0729055463807818,
0.787474075450074));
#18224=CARTESIAN_POINT('Ctrl Pts',(-0.0202952816069424,-0.137719814645367,
0.793898963730571));
#18225=CARTESIAN_POINT('Ctrl Pts',(0.104705698854998,-0.0917352845351548,
0.801837953367879));
#18226=CARTESIAN_POINT('Ctrl Pts',(0.133855787965376,0.0382266115373486,
0.809776943005182));
#18227=CARTESIAN_POINT('Ctrl Pts',(0.0404700769297216,0.133194664588195,
0.81771593264249));
#18228=CARTESIAN_POINT('Ctrl Pts',(-0.0843190215395119,0.107398870964955,
0.825311381149555));
#18229=CARTESIAN_POINT('Ctrl Pts',(-0.117623050954756,0.0339016606582783,
0.830260499777521));
#18230=CARTESIAN_POINT('Ctrl Pts',(-0.11789232318732,-8.18790992476734E-5,
0.832563288526384));
#18231=CARTESIAN_POINT('Ctrl Pts',(-0.117874685330111,-8.9283644551537E-5,
0.792436711473617));
#18232=CARTESIAN_POINT('Ctrl Pts',(-0.11792303416021,-0.00583050672374999,
0.7928255958429));
#18233=CARTESIAN_POINT('Ctrl Pts',(-0.114931453360353,-0.0506053896743902,
0.795861869586443));
#18234=CARTESIAN_POINT('Ctrl Pts',(-0.0575513573065257,-0.126774282767806,
0.801545532704245));
#18235=CARTESIAN_POINT('Ctrl Pts',(0.0753527000357912,-0.117071978271622,
0.809487700827026));
#18236=CARTESIAN_POINT('Ctrl Pts',(0.139225942868322,-0.000119714417332432,
0.817429868949805));
#18237=CARTESIAN_POINT('Ctrl Pts',(0.0755539188089132,0.116942220141962,
0.825372037072586));
#18238=CARTESIAN_POINT('Ctrl Pts',(-0.0573332568284509,0.12687306712048,
0.833314205195366));
#18239=CARTESIAN_POINT('Ctrl Pts',(-0.114890414736801,0.0507419104293215,
0.839002429995709));
#18240=CARTESIAN_POINT('Ctrl Pts',(-0.117921990994851,0.00589875908008548,
0.842043265421793));
#18241=CARTESIAN_POINT('Ctrl Pts',(-0.117872825429845,8.99519344067998E-5,
0.842436711473616));
#18242=CARTESIAN_POINT('Origin',(0.,0.,-0.0924367114736175));
#18243=CARTESIAN_POINT('',(-0.11772691567491,0.000105512987197037,0.732563288526384));
#18244=CARTESIAN_POINT('',(-0.117591850253004,-3.65476421498312E-5,0.742436711473616));
#18245=CARTESIAN_POINT('',(-0.117775,2.85464118895969E-14,-0.0924367114736175));
#18246=CARTESIAN_POINT('Ctrl Pts',(-0.11772691567491,0.000105512987197042,
0.732563288526384));
#18247=CARTESIAN_POINT('Ctrl Pts',(-0.117479624464894,-0.0283451130369189,
0.734484204440733));
#18248=CARTESIAN_POINT('Ctrl Pts',(-0.0928318426870313,-0.096374559506161,
0.739051450234184));
#18249=CARTESIAN_POINT('Ctrl Pts',(0.0209425314183671,-0.137622876656644,
0.746265025906738));
#18250=CARTESIAN_POINT('Ctrl Pts',(0.126986869252672,-0.0570349089493802,
0.754204015544043));
#18251=CARTESIAN_POINT('Ctrl Pts',(0.11678343126468,0.0757646090434518,
0.762143005181349));
#18252=CARTESIAN_POINT('Ctrl Pts',(-0.000327234354877375,0.139206819944772,
0.770081994818654));
#18253=CARTESIAN_POINT('Ctrl Pts',(-0.100479183608201,0.0843410365921374,
0.776888755933667));
#18254=CARTESIAN_POINT('Ctrl Pts',(-0.117520539541507,0.0224420334666934,
0.781049187169576));
#18255=CARTESIAN_POINT('Ctrl Pts',(-0.117598114366551,-4.518327158929E-5,
0.782563288526384));
#18256=CARTESIAN_POINT('Ctrl Pts',(-0.117591850253004,-3.65476421498364E-5,
0.742436711473616));
#18257=CARTESIAN_POINT('Ctrl Pts',(-0.117640211257931,-0.0174335619022046,
0.743607926264006));
#18258=CARTESIAN_POINT('Ctrl Pts',(-0.105863856762799,-0.0740921523660566,
0.747426530428656));
#18259=CARTESIAN_POINT('Ctrl Pts',(-0.0182163644075178,-0.138029133036789,
0.753892523967566));
#18260=CARTESIAN_POINT('Ctrl Pts',(0.106128952536144,-0.0901139441634624,
0.761834692090347));
#18261=CARTESIAN_POINT('Ctrl Pts',(0.133249245915149,0.0403548753208232,
0.769776860213125));
#18262=CARTESIAN_POINT('Ctrl Pts',(0.0382995408207276,0.133854483197375,
0.777719028335907));
#18263=CARTESIAN_POINT('Ctrl Pts',(-0.0853693283863186,0.106155717082476,
0.785272312089402));
#18264=CARTESIAN_POINT('Ctrl Pts',(-0.117593892160246,0.0332537408718532,
0.79017820646864));
#18265=CARTESIAN_POINT('Ctrl Pts',(-0.117874685330111,-8.9283644551537E-5,
0.792436711473617));
#18266=CARTESIAN_POINT('Origin',(0.,0.,-0.0924367114736175));
#18267=CARTESIAN_POINT('',(-0.117964947617991,-1.73329198795185E-5,0.682563288526384));
#18268=CARTESIAN_POINT('',(-0.117740574064672,0.000107068518266168,0.692436711473616));
#18269=CARTESIAN_POINT('',(-0.117775,2.85464118895969E-14,-0.0924367114736175));
#18270=CARTESIAN_POINT('Ctrl Pts',(-0.117964947617991,-1.73329198795367E-5,
0.682563288526384));
#18271=CARTESIAN_POINT('Ctrl Pts',(-0.117966864156947,-0.000949576032666658,
0.682626561953687));
#18272=CARTESIAN_POINT('Ctrl Pts',(-0.117534558560489,-0.0408698671952461,
0.685336165260092));
#18273=CARTESIAN_POINT('Ctrl Pts',(-0.0726787294560835,-0.118728463672822,
0.690692098445597));
#18274=CARTESIAN_POINT('Ctrl Pts',(0.0603425395611779,-0.125448888878168,
0.698631088082904));
#18275=CARTESIAN_POINT('Ctrl Pts',(0.138124349154501,-0.0173294538893964,
0.706570077720209));
#18276=CARTESIAN_POINT('Ctrl Pts',(0.0894627833767505,0.106653908470079,
0.714509067357515));
#18277=CARTESIAN_POINT('Ctrl Pts',(-0.0410958292974484,0.133002927094911,
0.72244805699482));
#18278=CARTESIAN_POINT('Ctrl Pts',(-0.111546724107196,0.0606813038481789,
0.728466130717777));
#18279=CARTESIAN_POINT('Ctrl Pts',(-0.117820302634623,0.0108495967181263,
0.731837874561632));
#18280=CARTESIAN_POINT('Ctrl Pts',(-0.11772691567491,0.000105512987197042,
0.732563288526384));
#18281=CARTESIAN_POINT('Ctrl Pts',(-0.117740574064672,0.000107068518266165,
0.692436711473616));
#18282=CARTESIAN_POINT('Ctrl Pts',(-0.117483171888848,-0.0288182833237499,
0.694390256685113));
#18283=CARTESIAN_POINT('Ctrl Pts',(-0.0921515028359353,-0.0973455904149804,
0.698991191270869));
#18284=CARTESIAN_POINT('Ctrl Pts',(0.022691720100341,-0.137364345221032,
0.706239515230886));
#18285=CARTESIAN_POINT('Ctrl Pts',(0.127740337615313,-0.0553740340325759,
0.714181683353665));
#18286=CARTESIAN_POINT('Ctrl Pts',(0.115765682611161,0.077344581120379,
0.722123851476446));
#18287=CARTESIAN_POINT('Ctrl Pts',(-0.00226223072526165,0.139207614056346,
0.730066019599226));
#18288=CARTESIAN_POINT('Ctrl Pts',(-0.101117998472899,0.083225715609228,
0.736836972931616));
#18289=CARTESIAN_POINT('Ctrl Pts',(-0.117530897055598,0.0218902846491045,
0.740960536889746));
#18290=CARTESIAN_POINT('Ctrl Pts',(-0.117591850253004,-3.65476421498364E-5,
0.742436711473616));
#18291=CARTESIAN_POINT('Origin',(0.,0.,-0.0924367114736175));
#18292=CARTESIAN_POINT('',(-0.117676160015555,-9.46906955630148E-5,0.632563288526383));
#18293=CARTESIAN_POINT('',(-0.117962383120995,-2.41598447144192E-5,0.642436711473616));
#18294=CARTESIAN_POINT('',(-0.117775,2.85464118895969E-14,-0.0924367114736175));
#18295=CARTESIAN_POINT('Ctrl Pts',(-0.117676160015555,-9.46906955630045E-5,
0.632563288526383));
#18296=CARTESIAN_POINT('Ctrl Pts',(-0.117771520970562,-0.0127268345011372,
0.633415249345741));
#18297=CARTESIAN_POINT('Ctrl Pts',(-0.110078248258936,-0.064483421762156,
0.636913540044201));
#18298=CARTESIAN_POINT('Ctrl Pts',(-0.0347063025259737,-0.134811417789573,
0.643058160621763));
#18299=CARTESIAN_POINT('Ctrl Pts',(0.0944472082050275,-0.102266175560326,
0.65099715025907));
#18300=CARTESIAN_POINT('Ctrl Pts',(0.137140772714236,0.0238967416356601,
0.658936139896373));
#18301=CARTESIAN_POINT('Ctrl Pts',(0.054291358674537,0.128183829614862,
0.666875129533682));
#18302=CARTESIAN_POINT('Ctrl Pts',(-0.0772016597727435,0.11523146575827,
0.674750845743682));
#18303=CARTESIAN_POINT('Ctrl Pts',(-0.117886707375211,0.0380402955314478,
0.679980232074585));
#18304=CARTESIAN_POINT('Ctrl Pts',(-0.117964947617991,-1.73329198795367E-5,
0.682563288526384));
#18305=CARTESIAN_POINT('Ctrl Pts',(-0.117962383120995,-2.41598447144253E-5,
0.642436711473616));
#18306=CARTESIAN_POINT('Ctrl Pts',(-0.117966033213387,-0.0013279541977536,
0.642525197731959));
#18307=CARTESIAN_POINT('Ctrl Pts',(-0.117355585052125,-0.0416360146359673,
0.645261073364563));
#18308=CARTESIAN_POINT('Ctrl Pts',(-0.0715088964667609,-0.119458592094588,
0.650644338371427));
#18309=CARTESIAN_POINT('Ctrl Pts',(0.0616402393688536,-0.124837327709565,
0.658586506494205));
#18310=CARTESIAN_POINT('Ctrl Pts',(0.138320583400205,-0.0158522461166236,
0.666528674616987));
#18311=CARTESIAN_POINT('Ctrl Pts',(0.0882850628235238,0.107655121482266,
0.674470842739765));
#18312=CARTESIAN_POINT('Ctrl Pts',(-0.0426286451686149,0.132539337972556,
0.682413010862546));
#18313=CARTESIAN_POINT('Ctrl Pts',(-0.111894847147975,0.059748848130285,
0.68840163377383));
#18314=CARTESIAN_POINT('Ctrl Pts',(-0.117831996057943,0.0103805377030848,
0.691742867310853));
#18315=CARTESIAN_POINT('Ctrl Pts',(-0.117740574064672,0.000107068518266165,
0.692436711473616));
#18316=CARTESIAN_POINT('Origin',(0.,0.,-0.0924367114736175));
#18317=CARTESIAN_POINT('',(-0.117626285855324,7.11112359239178E-5,0.582563288526384));
#18318=CARTESIAN_POINT('',(-0.11766919235599,-9.26074537421634E-5,0.592436711473616));
#18319=CARTESIAN_POINT('',(-0.117775,2.85464118895969E-14,-0.0924367114736175));
#18320=CARTESIAN_POINT('Ctrl Pts',(-0.117626285855324,7.11112359239024E-5,
0.582563288526383));
#18321=CARTESIAN_POINT('Ctrl Pts',(-0.117492102008102,-0.0242809575267813,
0.584203936737797));
#18322=CARTESIAN_POINT('Ctrl Pts',(-0.0982512120079041,-0.0881067492982899,
0.588490914828312));
#18323=CARTESIAN_POINT('Ctrl Pts',(0.00631176444456456,-0.139064040754811,
0.595424222797929));
#18324=CARTESIAN_POINT('Ctrl Pts',(0.120263693490807,-0.0701091280034811,
0.603363212435234));
#18325=CARTESIAN_POINT('Ctrl Pts',(0.124122453355413,0.0630258865426945,
0.611302202072541));
#18326=CARTESIAN_POINT('Ctrl Pts',(0.0143556138404206,0.138465021405133,
0.619241191709845));
#18327=CARTESIAN_POINT('Ctrl Pts',(-0.0953630726970595,0.0926558297308384,
0.626328220527794));
#18328=CARTESIAN_POINT('Ctrl Pts',(-0.117475314221613,0.0265106736450616,
0.630768919466639));
#18329=CARTESIAN_POINT('Ctrl Pts',(-0.117676160015555,-9.46906955630045E-5,
0.632563288526383));
#18330=CARTESIAN_POINT('Ctrl Pts',(-0.11766919235599,-9.26074537421669E-5,
0.592436711473616));
#18331=CARTESIAN_POINT('Ctrl Pts',(-0.117764072896019,-0.0130062487266101,
0.593307528153066));
#18332=CARTESIAN_POINT('Ctrl Pts',(-0.109848366281979,-0.0650658641993071,
0.596825734206776));
#18333=CARTESIAN_POINT('Ctrl Pts',(-0.0336977294021144,-0.135086418755761,
0.602991329634746));
#18334=CARTESIAN_POINT('Ctrl Pts',(0.0952657566843092,-0.101529863106778,
0.610933497757526));
#18335=CARTESIAN_POINT('Ctrl Pts',(0.136956022624868,0.025038477707157,
0.618875665880307));
#18336=CARTESIAN_POINT('Ctrl Pts',(0.0531805018142573,0.128669000640787,
0.626817834003085));
#18337=CARTESIAN_POINT('Ctrl Pts',(-0.0778376600742765,0.114584191752874,
0.634671515867523));
#18338=CARTESIAN_POINT('Ctrl Pts',(-0.117856827377429,0.0376798124439797,
0.639877808357699));
#18339=CARTESIAN_POINT('Ctrl Pts',(-0.117962383120995,-2.41598447144253E-5,
0.642436711473616));
#18340=CARTESIAN_POINT('Origin',(0.,0.,-0.0924367114736175));
#18341=CARTESIAN_POINT('',(-0.117934829819181,5.63106208242181E-5,0.532563288526383));
#18342=CARTESIAN_POINT('',(-0.117629301205424,7.34277634442948E-5,0.542436711473615));
#18343=CARTESIAN_POINT('',(-0.117775,2.85464118895969E-14,-0.0924367114736175));
#18344=CARTESIAN_POINT('Ctrl Pts',(-0.117934829819181,5.63106208242166E-5,
0.532563288526383));
#18345=CARTESIAN_POINT('Ctrl Pts',(-0.117723349859012,-0.0357608023914865,
0.534992624129852));
#18346=CARTESIAN_POINT('Ctrl Pts',(-0.0811985738067347,-0.110967619805887,
0.540068289612422));
#18347=CARTESIAN_POINT('Ctrl Pts',(0.0467759446245483,-0.131113145053959,
0.547790284974095));
#18348=CARTESIAN_POINT('Ctrl Pts',(0.135526478334676,-0.031799677225719,
0.555729274611401));
#18349=CARTESIAN_POINT('Ctrl Pts',(0.100211809365564,0.0966242157284558,
0.563668264248707));
#18350=CARTESIAN_POINT('Ctrl Pts',(-0.0268399031138932,0.136595261273209,
0.571607253886012));
#18351=CARTESIAN_POINT('Ctrl Pts',(-0.108142973925314,0.0691035501437442,
0.577905595311905));
#18352=CARTESIAN_POINT('Ctrl Pts',(-0.117708537635025,0.0149983997031143,
0.581557606858695));
#18353=CARTESIAN_POINT('Ctrl Pts',(-0.117626285855324,7.11112359239024E-5,
0.582563288526383));
#18354=CARTESIAN_POINT('Ctrl Pts',(-0.117629301205424,7.34277634442983E-5,
0.542436711473615));
#18355=CARTESIAN_POINT('Ctrl Pts',(-0.11748956090956,-0.0244625652698295,
0.544089858574172));
#18356=CARTESIAN_POINT('Ctrl Pts',(-0.0980201725405651,-0.0884941619373469,
0.548390395048989));
#18357=CARTESIAN_POINT('Ctrl Pts',(0.00702343738442799,-0.139048728244533,
0.555338320898066));
#18358=CARTESIAN_POINT('Ctrl Pts',(0.12066450826877,-0.0694546898587181,
0.563280489020846));
#18359=CARTESIAN_POINT('Ctrl Pts',(0.123764493242992,0.063766979789076,
0.571222657143626));
#18360=CARTESIAN_POINT('Ctrl Pts',(0.0134834875971477,0.13857154491934,
0.579164825266405));
#18361=CARTESIAN_POINT('Ctrl Pts',(-0.0957036897026042,0.092147346049863,
0.586236176709736));
#18362=CARTESIAN_POINT('Ctrl Pts',(-0.117475624432153,0.0262528025703711,
0.590660138778806));
#18363=CARTESIAN_POINT('Ctrl Pts',(-0.11766919235599,-9.26074537421669E-5,
0.592436711473616));
#18364=CARTESIAN_POINT('Origin',(0.,0.,-0.0924367114736175));
#18365=CARTESIAN_POINT('',(-0.117794891956694,-0.000106411733115368,0.482563288526384));
#18366=CARTESIAN_POINT('',(-0.117936566864074,5.52347650140707E-5,0.492436711473616));
#18367=CARTESIAN_POINT('',(-0.117775,2.85464118895969E-14,-0.0924367114736175));
#18368=CARTESIAN_POINT('Ctrl Pts',(-0.117794891956694,-0.000106411733115381,
0.482563288526384));
#18369=CARTESIAN_POINT('Ctrl Pts',(-0.117872998614688,-0.00856127641466401,
0.483134981642805));
#18370=CARTESIAN_POINT('Ctrl Pts',(-0.113184542395844,-0.0560672187853419,
0.486353004638329));
#18371=CARTESIAN_POINT('Ctrl Pts',(-0.0487302328423073,-0.130399425645183,
0.492217357512954));
#18372=CARTESIAN_POINT('Ctrl Pts',(0.0831353173341669,-0.111656458896056,
0.50015634715026));
#18373=CARTESIAN_POINT('Ctrl Pts',(0.13889618212661,0.00930034365552528,
0.508095336787567));
#18374=CARTESIAN_POINT('Ctrl Pts',(0.0675071113591811,0.12174331898465,
0.516034326424871));
#18375=CARTESIAN_POINT('Ctrl Pts',(-0.0656800932930844,0.122738629397884,
0.523973316062178));
#18376=CARTESIAN_POINT('Ctrl Pts',(-0.116384786286051,0.04545243224792,
0.529482970096015));
#18377=CARTESIAN_POINT('Ctrl Pts',(-0.117953719733239,0.00325558390455253,
0.53234629425075));
#18378=CARTESIAN_POINT('Ctrl Pts',(-0.117934829819181,5.63106208242166E-5,
0.532563288526383));
#18379=CARTESIAN_POINT('Ctrl Pts',(-0.117936566864074,5.52347650140663E-5,
0.492436711473616));
#18380=CARTESIAN_POINT('Ctrl Pts',(-0.117728017843002,-0.0358510361847084,
0.494872188995279));
#18381=CARTESIAN_POINT('Ctrl Pts',(-0.0810366231971402,-0.111156550628637,
0.499955055891203));
#18382=CARTESIAN_POINT('Ctrl Pts',(0.0471380885036503,-0.131003351527116,
0.507685312161385));
#18383=CARTESIAN_POINT('Ctrl Pts',(0.135643160584381,-0.031381690295376,
0.515627480284167));
#18384=CARTESIAN_POINT('Ctrl Pts',(0.0998851624184703,0.0969888232104648,
0.523569648406945));
#18385=CARTESIAN_POINT('Ctrl Pts',(-0.0273779061153799,0.136507610615132,
0.531511816529727));
#18386=CARTESIAN_POINT('Ctrl Pts',(-0.108290992649607,0.0687756007668377,
0.537800837551949));
#18387=CARTESIAN_POINT('Ctrl Pts',(-0.117713344367368,0.0148299618267192,
0.541442469199912));
#18388=CARTESIAN_POINT('Ctrl Pts',(-0.117629301205424,7.34277634442983E-5,
0.542436711473615));
#18389=CARTESIAN_POINT('Origin',(0.,0.,-0.0924367114736175));
#18390=CARTESIAN_POINT('',(-0.117582256074849,9.06819982020624E-6,0.432563288526383));
#18391=CARTESIAN_POINT('',(-0.11779560903417,-0.000106574656651148,0.442436711473616));
#18392=CARTESIAN_POINT('',(-0.117775,2.85464118895969E-14,-0.0924367114736175));
#18393=CARTESIAN_POINT('Ctrl Pts',(-0.117582256074849,9.06819982019261E-6,
0.432563288526383));
#18394=CARTESIAN_POINT('Ctrl Pts',(-0.117568373935691,-0.020201912089319,
0.43392366903486));
#18395=CARTESIAN_POINT('Ctrl Pts',(-0.10300922874285,-0.0797477867736473,
0.437930379422439));
#18396=CARTESIAN_POINT('Ctrl Pts',(-0.00838939967687663,-0.138954178686792,
0.44458341968912));
#18397=CARTESIAN_POINT('Ctrl Pts',(0.11219917790857,-0.0824013973067221,
0.452522409326426));
#18398=CARTESIAN_POINT('Ctrl Pts',(0.13007709763057,0.0495842159710775,
0.460461398963732));
#18399=CARTESIAN_POINT('Ctrl Pts',(0.0288783492374893,0.136178877755608,
0.468400388601037));
#18400=CARTESIAN_POINT('Ctrl Pts',(-0.0895654556576369,0.100852400902523,
0.475767685121922));
#18401=CARTESIAN_POINT('Ctrl Pts',(-0.117511448025972,0.0305757367622385,
0.480488651763704));
#18402=CARTESIAN_POINT('Ctrl Pts',(-0.117794891956694,-0.000106411733115381,
0.482563288526384));
#18403=CARTESIAN_POINT('Ctrl Pts',(-0.11779560903417,-0.000106574656651151,
0.442436711473616));
#18404=CARTESIAN_POINT('Ctrl Pts',(-0.117873644338608,-0.00854245500997505,
0.443007130042126));
#18405=CARTESIAN_POINT('Ctrl Pts',(-0.113196618671047,-0.056044542179559,
0.446224937984896));
#18406=CARTESIAN_POINT('Ctrl Pts',(-0.0487473834415776,-0.130413074907061,
0.452090135301926));
#18407=CARTESIAN_POINT('Ctrl Pts',(0.0831820848081396,-0.111645054821459,
0.460032303424706));
#18408=CARTESIAN_POINT('Ctrl Pts',(0.138908217753341,0.00940130521287039,
0.467974471547486));
#18409=CARTESIAN_POINT('Ctrl Pts',(0.0673801526530663,0.121835103839429,
0.475916639670265));
#18410=CARTESIAN_POINT('Ctrl Pts',(-0.0658750545035054,0.12265543075329,
0.483858807793047));
#18411=CARTESIAN_POINT('Ctrl Pts',(-0.116424939330292,0.0453161125527027,
0.489365498394162));
#18412=CARTESIAN_POINT('Ctrl Pts',(-0.11795471279604,0.00317945345687678,
0.492224799621019));
#18413=CARTESIAN_POINT('Ctrl Pts',(-0.117936566864074,5.52347650140663E-5,
0.492436711473616));
#18414=CARTESIAN_POINT('Origin',(0.,0.,-0.0924367114736175));
#18415=CARTESIAN_POINT('',(-0.117828183671793,0.000101754196006455,0.382563288526383));
#18416=CARTESIAN_POINT('',(-0.117581664177921,7.09484545444172E-6,0.392436711473616));
#18417=CARTESIAN_POINT('',(-0.117775,2.85464118895969E-14,-0.0924367114736175));
#18418=CARTESIAN_POINT('Ctrl Pts',(-0.117828183671793,0.000101754196006446,
0.382563288526384));
#18419=CARTESIAN_POINT('Ctrl Pts',(-0.117538790254565,-0.0316580736410773,
0.384712356426916));
#18420=CARTESIAN_POINT('Ctrl Pts',(-0.0879068326507716,-0.103002379129266,
0.38950775420655));
#18421=CARTESIAN_POINT('Ctrl Pts',(0.0326876424682324,-0.135315053971568,
0.396949481865287));
#18422=CARTESIAN_POINT('Ctrl Pts',(0.13141703692502,-0.0459152284901983,
0.404888471502591));
#18423=CARTESIAN_POINT('Ctrl Pts',(0.109843140674695,0.0855168418978295,
0.412827461139898));
#18424=CARTESIAN_POINT('Ctrl Pts',(-0.0122846228212416,0.13866410438033,
0.420766450777203));
#18425=CARTESIAN_POINT('Ctrl Pts',(-0.104166535924894,0.0775181589932739,
0.427345059906032));
#18426=CARTESIAN_POINT('Ctrl Pts',(-0.117595378674006,0.0191142356295008,
0.431277339155758));
#18427=CARTESIAN_POINT('Ctrl Pts',(-0.117582256074849,9.06819982019261E-6,
0.432563288526383));
#18428=CARTESIAN_POINT('Ctrl Pts',(-0.117581664177921,7.09484545444172E-6,
0.392436711473616));
#18429=CARTESIAN_POINT('Ctrl Pts',(-0.117570873504463,-0.0200907396801347,
0.393789460463232));
#18430=CARTESIAN_POINT('Ctrl Pts',(-0.10312708440739,-0.079535468422451,
0.397789598827109));
#18431=CARTESIAN_POINT('Ctrl Pts',(-0.00873482453528946,-0.138951719454826,
0.404437126565246));
#18432=CARTESIAN_POINT('Ctrl Pts',(0.112042812448737,-0.0826455423945668,
0.412379294688026));
#18433=CARTESIAN_POINT('Ctrl Pts',(0.130177722634257,0.049372441998279,
0.420321462810806));
#18434=CARTESIAN_POINT('Ctrl Pts',(0.0290564652212241,0.136160197297018,
0.428263630933586));
#18435=CARTESIAN_POINT('Ctrl Pts',(-0.0895090212855029,0.100936776489487,
0.435635380487856));
#18436=CARTESIAN_POINT('Ctrl Pts',(-0.117511471984497,0.0306096014671689,
0.440359740667866));
#18437=CARTESIAN_POINT('Ctrl Pts',(-0.11779560903417,-0.000106574656651151,
0.442436711473616));
#18438=CARTESIAN_POINT('Origin',(0.,0.,-0.0924367114736175));
#18439=CARTESIAN_POINT('',(-0.117911328466355,-7.22474488887591E-5,0.332563288526384));
#18440=CARTESIAN_POINT('',(-0.117821685414254,0.000103165543095151,0.342436711473616));
#18441=CARTESIAN_POINT('',(-0.117775,2.85464118895969E-14,-0.0924367114736175));
#18442=CARTESIAN_POINT('Ctrl Pts',(-0.117911328466355,-7.22474488887752E-5,
0.332563288526384));
#18443=CARTESIAN_POINT('Ctrl Pts',(-0.117942332027964,-0.00437115939612809,
0.332854713939869));
#18444=CARTESIAN_POINT('Ctrl Pts',(-0.115777752883067,-0.0476754067323583,
0.335792469232457));
#18445=CARTESIAN_POINT('Ctrl Pts',(-0.0622106591311991,-0.12453304658572,
0.341376554404146));
#18446=CARTESIAN_POINT('Ctrl Pts',(0.0708961914151981,-0.119801401679107,
0.349315544041452));
#18447=CARTESIAN_POINT('Ctrl Pts',(0.1391024375543,-0.00539978406154301,
0.357254533678757));
#18448=CARTESIAN_POINT('Ctrl Pts',(0.0799699354250877,0.113944965792994,
0.365193523316063));
#18449=CARTESIAN_POINT('Ctrl Pts',(-0.0523695618881846,0.128980908622551,
0.373132512953369));
#18450=CARTESIAN_POINT('Ctrl Pts',(-0.113921748517257,0.0538356345748906,
0.378922434690143));
#18451=CARTESIAN_POINT('Ctrl Pts',(-0.117895144954496,0.00745050051778832,
0.382066026547814));
#18452=CARTESIAN_POINT('Ctrl Pts',(-0.117828183671793,0.000101754196006446,
0.382563288526384));
#18453=CARTESIAN_POINT('Ctrl Pts',(-0.117821685414254,0.000103165543095145,
0.342436711473616));
#18454=CARTESIAN_POINT('Ctrl Pts',(-0.117532262555972,-0.0314544122979593,
0.344571790884339));
#18455=CARTESIAN_POINT('Ctrl Pts',(-0.0882170202347594,-0.102616110661261,
0.349354259669323));
#18456=CARTESIAN_POINT('Ctrl Pts',(0.0320320385160992,-0.135491055083419,
0.356784117828566));
#18457=CARTESIAN_POINT('Ctrl Pts',(0.131227975626944,-0.0465090949381858,
0.364726285951346));
#18458=CARTESIAN_POINT('Ctrl Pts',(0.110205605501345,0.0850799742312894,
0.372668454074126));
#18459=CARTESIAN_POINT('Ctrl Pts',(-0.0117764211155082,0.138727046407055,
0.380610622196906));
#18460=CARTESIAN_POINT('Ctrl Pts',(-0.10403099481448,0.0777947493501838,
0.387200041330069));
#18461=CARTESIAN_POINT('Ctrl Pts',(-0.117591991327853,0.019241607989002,
0.391142071088973));
#18462=CARTESIAN_POINT('Ctrl Pts',(-0.117581664177921,7.09484545444172E-6,
0.392436711473616));
#18463=CARTESIAN_POINT('Origin',(0.,0.,-0.0924367114736175));
#18464=CARTESIAN_POINT('',(-0.117608153246896,-5.64262068778628E-5,0.282563288526383));
#18465=CARTESIAN_POINT('',(-0.117918861549493,-6.80329776671096E-5,0.292436711473615));
#18466=CARTESIAN_POINT('',(-0.117775,2.85464118895969E-14,-0.0924367114736175));
#18467=CARTESIAN_POINT('Ctrl Pts',(-0.117608153246896,-5.64262068778604E-5,
0.282563288526383));
#18468=CARTESIAN_POINT('Ctrl Pts',(-0.117677606263852,-0.0160946837114709,
0.283643401331924));
#18469=CARTESIAN_POINT('Ctrl Pts',(-0.107144424846824,-0.0713401098021974,
0.287369844016567));
#18470=CARTESIAN_POINT('Ctrl Pts',(-0.0229969941138309,-0.137294515779738,
0.293742616580312));
#18471=CARTESIAN_POINT('Ctrl Pts',(0.102883268653204,-0.0937746172089793,
0.301681606217617));
#18472=CARTESIAN_POINT('Ctrl Pts',(0.134580950019115,0.0355895166223291,
0.309620595854923));
#18473=CARTESIAN_POINT('Ctrl Pts',(0.0430789950773988,0.13237388709478,
0.317559585492229));
#18474=CARTESIAN_POINT('Ctrl Pts',(-0.0830523456774332,0.10887452531409,
0.325207149716049));
#18475=CARTESIAN_POINT('Ctrl Pts',(-0.11766079978112,0.0346657214219864,
0.330208384060767));
#18476=CARTESIAN_POINT('Ctrl Pts',(-0.117911328466355,-7.22474488887752E-5,
0.332563288526384));
#18477=CARTESIAN_POINT('Ctrl Pts',(-0.117918861549493,-6.80329776671157E-5,
0.292436711473616));
#18478=CARTESIAN_POINT('Ctrl Pts',(-0.117946256357307,-0.00405052459867665,
0.292706731931186));
#18479=CARTESIAN_POINT('Ctrl Pts',(-0.11595553950755,-0.0470512577090033,
0.295624141763016));
#18480=CARTESIAN_POINT('Ctrl Pts',(-0.0631725212350128,-0.124068972994571,
0.301188940969106));
#18481=CARTESIAN_POINT('Ctrl Pts',(0.0700327441786229,-0.12032993078169,
0.309131109091886));
#18482=CARTESIAN_POINT('Ctrl Pts',(0.139080821187468,-0.00635631000930847,
0.317073277214666));
#18483=CARTESIAN_POINT('Ctrl Pts',(0.0807165776729536,0.11344034374014,
0.325015445337446));
#18484=CARTESIAN_POINT('Ctrl Pts',(-0.0515923433190751,0.129313988454311,
0.332957613460226));
#18485=CARTESIAN_POINT('Ctrl Pts',(-0.113774867115171,0.0543021652640841,
0.338764702172283));
#18486=CARTESIAN_POINT('Ctrl Pts',(-0.117891132111753,0.00767537174388221,
0.341924401510079));
#18487=CARTESIAN_POINT('Ctrl Pts',(-0.117821685414254,0.000103165543095145,
0.342436711473616));
#18488=CARTESIAN_POINT('Origin',(0.,0.,-0.0924367114736175));
#18489=CARTESIAN_POINT('',(-0.117705188630573,0.000102098618198066,0.232563288526383));
#18490=CARTESIAN_POINT('',(-0.1176142238744,-6.23262858038681E-5,0.242436711473616));
#18491=CARTESIAN_POINT('',(-0.117775,2.85464118895969E-14,-0.0924367114736175));
#18492=CARTESIAN_POINT('Ctrl Pts',(-0.117705188630573,0.000102098618198071,
0.232563288526383));
#18493=CARTESIAN_POINT('Ctrl Pts',(-0.117475649963863,-0.0275896003179174,
0.234432088723979));
#18494=CARTESIAN_POINT('Ctrl Pts',(-0.0938913217252411,-0.0948462909608301,
0.238947218800678));
#18495=CARTESIAN_POINT('Ctrl Pts',(0.0182347644767634,-0.138007750384372,
0.246108678756477));
#18496=CARTESIAN_POINT('Ctrl Pts',(0.125841858853055,-0.0595186723796334,
0.254047668393783));
#18497=CARTESIAN_POINT('Ctrl Pts',(0.118249355954961,0.073455671106145,
0.261986658031089));
#18498=CARTESIAN_POINT('Ctrl Pts',(0.00240767183786234,0.139186381940956,
0.269925647668394));
#18499=CARTESIAN_POINT('Ctrl Pts',(-0.0995777503027144,0.0858938305448248,
0.27678452450016));
#18500=CARTESIAN_POINT('Ctrl Pts',(-0.117507442931816,0.0231998416616275,
0.280997071452822));
#18501=CARTESIAN_POINT('Ctrl Pts',(-0.117608153246896,-5.64262068778604E-5,
0.282563288526383));
#18502=CARTESIAN_POINT('Ctrl Pts',(-0.1176142238744,-6.2326285803882E-5,
0.242436711473616));
#18503=CARTESIAN_POINT('Ctrl Pts',(-0.117689148257971,-0.0156863246439697,
0.243489062352292));
#18504=CARTESIAN_POINT('Ctrl Pts',(-0.107519643382358,-0.0705218816827611,
0.247188802605229));
#18505=CARTESIAN_POINT('Ctrl Pts',(-0.024381182195918,-0.137074561658528,
0.253535932232426));
#18506=CARTESIAN_POINT('Ctrl Pts',(0.101985705091022,-0.094777599970642,
0.261478100355206));
#18507=CARTESIAN_POINT('Ctrl Pts',(0.134923209124943,0.0343453801629359,
0.269420268477986));
#18508=CARTESIAN_POINT('Ctrl Pts',(0.0442571924125319,0.132004463632409,
0.277362436600766));
#18509=CARTESIAN_POINT('Ctrl Pts',(-0.0824920331482911,0.109525057495754,
0.285034584265976));
#18510=CARTESIAN_POINT('Ctrl Pts',(-0.117677666622401,0.0349954280503056,
0.290059342556926));
#18511=CARTESIAN_POINT('Ctrl Pts',(-0.117918861549493,-6.80329776671157E-5,
0.292436711473616));
#18512=CARTESIAN_POINT('Origin',(0.,0.,-0.0924367114736175));
#18513=CARTESIAN_POINT('',(-0.117967994073432,-3.0724305424694E-6,0.182563288526383));
#18514=CARTESIAN_POINT('',(-0.117691121003631,9.91971943564221E-5,0.192436711473615));
#18515=CARTESIAN_POINT('',(-0.117775,2.85464118895969E-14,-0.0924367114736175));
#18516=CARTESIAN_POINT('Ctrl Pts',(-0.117967994073432,-3.07243054247449E-6,
0.182563288526383));
#18517=CARTESIAN_POINT('Ctrl Pts',(-0.117968057042159,-0.000167453844217198,
0.182574446236933));
#18518=CARTESIAN_POINT('Ctrl Pts',(-0.117893299674953,-0.0393189363008842,
0.185231933826584));
#18519=CARTESIAN_POINT('Ctrl Pts',(-0.0749972298318695,-0.11727771015962,
0.190535751295337));
#18520=CARTESIAN_POINT('Ctrl Pts',(0.0578663373665801,-0.126610160769685,
0.198474740932643));
#18521=CARTESIAN_POINT('Ctrl Pts',(0.13775723856723,-0.0200396862227523,
0.206413730569949));
#18522=CARTESIAN_POINT('Ctrl Pts',(0.091540828968026,0.104875747581476,
0.214352720207254));
#18523=CARTESIAN_POINT('Ctrl Pts',(-0.0384749358425138,0.133784622116252,
0.22229170984456));
#18524=CARTESIAN_POINT('Ctrl Pts',(-0.110955338697302,0.0622468391270206,
0.22836189928427));
#18525=CARTESIAN_POINT('Ctrl Pts',(-0.11780069007939,0.0116234575531164,
0.231785758844877));
#18526=CARTESIAN_POINT('Ctrl Pts',(-0.117705188630573,0.000102098618198071,
0.232563288526383));
#18527=CARTESIAN_POINT('Ctrl Pts',(-0.117691121003631,9.91971943564221E-5,
0.192436711473615));
#18528=CARTESIAN_POINT('Ctrl Pts',(-0.117474218986382,-0.0270951350261672,
0.194271392773399));
#18529=CARTESIAN_POINT('Ctrl Pts',(-0.0945676524372527,-0.0938598508209937,
0.198753463447442));
#18530=CARTESIAN_POINT('Ctrl Pts',(0.0165156171993534,-0.138242945169174,
0.205882923495746));
#18531=CARTESIAN_POINT('Ctrl Pts',(0.125131592687617,-0.061040658666823,
0.213825091618526));
#18532=CARTESIAN_POINT('Ctrl Pts',(0.119114174013628,0.0720811421096423,
0.221767259741306));
#18533=CARTESIAN_POINT('Ctrl Pts',(0.0039759348809324,0.139169211541763,
0.229709427864086));
#18534=CARTESIAN_POINT('Ctrl Pts',(-0.0990660356104632,0.0867677816679632,
0.236599245108189));
#18535=CARTESIAN_POINT('Ctrl Pts',(-0.117500661679058,0.0236188235484957,
0.240841672978032));
#18536=CARTESIAN_POINT('Ctrl Pts',(-0.1176142238744,-6.2326285803882E-5,
0.242436711473616));
#18537=CARTESIAN_POINT('Origin',(0.,0.,-0.0924367114736175));
#18538=CARTESIAN_POINT('',(-0.117696212882312,-0.000100181105204699,0.132563288526383));
#18539=CARTESIAN_POINT('',(-0.117967699956222,8.3697257429456E-6,0.142436711473616));
#18540=CARTESIAN_POINT('',(-0.117775,2.85464118895969E-14,-0.0924367114736175));
#18541=CARTESIAN_POINT('Ctrl Pts',(-0.117696212882312,-0.000100181105204706,
0.132563288526383));
#18542=CARTESIAN_POINT('Ctrl Pts',(-0.117792074781153,-0.0119544960022407,
0.133363133628988));
#18543=CARTESIAN_POINT('Ctrl Pts',(-0.110696412003459,-0.0629173266909915,
0.136809308610694));
#18544=CARTESIAN_POINT('Ctrl Pts',(-0.0373480950846616,-0.134103559412242,
0.142901813471503));
#18545=CARTESIAN_POINT('Ctrl Pts',(0.0924198687735613,-0.104101940294199,
0.150840803108809));
#18546=CARTESIAN_POINT('Ctrl Pts',(0.137583777756591,0.0211978768359354,
0.158779792746114));
#18547=CARTESIAN_POINT('Ctrl Pts',(0.0567991668878991,0.127092487218924,
0.16671878238342));
#18548=CARTESIAN_POINT('Ctrl Pts',(-0.0757945745091616,0.116657324056303,
0.174646614310176));
#18549=CARTESIAN_POINT('Ctrl Pts',(-0.117953122434976,0.0388197061692436,
0.179928116357831));
#18550=CARTESIAN_POINT('Ctrl Pts',(-0.117967994073432,-3.07243054247449E-6,
0.182563288526383));
#18551=CARTESIAN_POINT('Ctrl Pts',(-0.117967699956222,8.3697257429579E-6,
0.142436711473616));
#18552=CARTESIAN_POINT('Ctrl Pts',(-0.117928252023989,-0.038547130539091,
0.145053723194506));
#18553=CARTESIAN_POINT('Ctrl Pts',(-0.0762804946418446,-0.116178754198862,
0.150318124289656));
#18554=CARTESIAN_POINT('Ctrl Pts',(0.0559861945572589,-0.127473226882309,
0.158229914759066));
#18555=CARTESIAN_POINT('Ctrl Pts',(0.137471621702818,-0.0220324926503626,
0.166172082881846));
#18556=CARTESIAN_POINT('Ctrl Pts',(0.0930189202108026,0.103592267873211,
0.174114251004626));
#18557=CARTESIAN_POINT('Ctrl Pts',(-0.0366486683060043,0.134315868829211,
0.182056419127406));
#18558=CARTESIAN_POINT('Ctrl Pts',(-0.110544190454925,0.0633195416932908,
0.188163905950403));
#18559=CARTESIAN_POINT('Ctrl Pts',(-0.11778720200735,0.0121454601492482,
0.191624003399139));
#18560=CARTESIAN_POINT('Ctrl Pts',(-0.117691121003631,9.91971943564221E-5,
0.192436711473615));
#18561=CARTESIAN_POINT('Origin',(0.,0.,-0.0924367114736175));
#18562=CARTESIAN_POINT('',(-0.117613109409711,6.11591708146705E-5,0.0825632885263832));
#18563=CARTESIAN_POINT('',(-0.117715749944134,-0.000104199409386274,0.0924367114736155));
#18564=CARTESIAN_POINT('',(-0.117775,2.85464118895969E-14,-0.0924367114736175));
#18565=CARTESIAN_POINT('Ctrl Pts',(-0.117613109409711,6.11591708146765E-5,
0.0825632885263832));
#18566=CARTESIAN_POINT('Ctrl Pts',(-0.117502393620717,-0.0235240259785673,
0.0841518210210431));
#18567=CARTESIAN_POINT('Ctrl Pts',(-0.0991849320095013,-0.0865581493706475,
0.088386683394805));
#18568=CARTESIAN_POINT('Ctrl Pts',(0.00357853460314598,-0.139161043603659,
0.0952678756476685));
#18569=CARTESIAN_POINT('Ctrl Pts',(0.118863112008681,-0.0724583686054966,
0.103206865284975));
#18570=CARTESIAN_POINT('Ctrl Pts',(0.125336705278751,0.0605752693714656,
0.11114585492228));
#18571=CARTESIAN_POINT('Ctrl Pts',(0.0170731091066207,0.138156245709763,
0.119084844559586));
#18572=CARTESIAN_POINT('Ctrl Pts',(-0.094337657277608,0.0941904991302726,
0.126223989094287));
#18573=CARTESIAN_POINT('Ctrl Pts',(-0.11747491061231,0.0272661325996615,
0.130716803749886));
#18574=CARTESIAN_POINT('Ctrl Pts',(-0.117696212882312,-0.000100181105204706,
0.132563288526383));
#18575=CARTESIAN_POINT('Ctrl Pts',(-0.117715749944134,-0.000104199409386274,
0.0924367114736155));
#18576=CARTESIAN_POINT('Ctrl Pts',(-0.117810584636384,-0.011244028442556,
0.0931886642413524));
#18577=CARTESIAN_POINT('Ctrl Pts',(-0.111246641208053,-0.0614941526881817,
0.0965880063833492));
#18578=CARTESIAN_POINT('Ctrl Pts',(-0.0397151780004399,-0.133441281507892,
0.102634737899606));
#18579=CARTESIAN_POINT('Ctrl Pts',(0.0906220264938673,-0.105695447092796,
0.110576906022386));
#18580=CARTESIAN_POINT('Ctrl Pts',(0.137940159127448,0.0188783162799928,
0.118519074145166));
#18581=CARTESIAN_POINT('Ctrl Pts',(0.0588909273047484,0.126157580947307,
0.126461242267946));
#18582=CARTESIAN_POINT('Ctrl Pts',(-0.074108440039672,0.117863552156501,
0.134403410390726));
#18583=CARTESIAN_POINT('Ctrl Pts',(-0.117763087033452,0.0399060678969832,
0.139728566792616));
#18584=CARTESIAN_POINT('Ctrl Pts',(-0.117968157858494,0.000455912857932787,
0.142406333820246));
#18585=CARTESIAN_POINT('Ctrl Pts',(-0.117967699956222,8.3697257429579E-6,
0.142436711473616));
#18586=CARTESIAN_POINT('Origin',(0.,0.,-0.0924367114736175));
#18587=CARTESIAN_POINT('',(-0.117917485785546,7.60014832213593E-5,0.0325632885263832));
#18588=CARTESIAN_POINT('',(-0.117600989619072,5.04992496179954E-5,0.0424367114736154));
#18589=CARTESIAN_POINT('',(-0.117775,2.85464118895969E-14,-0.0924367114736175));
#18590=CARTESIAN_POINT('Ctrl Pts',(-0.117917485785546,7.60014832213644E-5,
0.0325632885263832));
#18591=CARTESIAN_POINT('Ctrl Pts',(-0.117676727567847,-0.0349830640657269,
0.0349405084130983));
#18592=CARTESIAN_POINT('Ctrl Pts',(-0.0825043195215805,-0.109517225708346,
0.0399640581789154));
#18593=CARTESIAN_POINT('Ctrl Pts',(0.0441923146003338,-0.131999388615902,
0.0476339378238343));
#18594=CARTESIAN_POINT('Ctrl Pts',(0.134874939024977,-0.034459980695041,
0.0555729274611401));
#18595=CARTESIAN_POINT('Ctrl Pts',(0.102091080224759,0.094638871230671,
0.0635119170984456));
#18596=CARTESIAN_POINT('Ctrl Pts',(-0.0241513666277066,0.137095110112719,
0.0714509067357516));
#18597=CARTESIAN_POINT('Ctrl Pts',(-0.107448046275642,0.0706698818446754,
0.0778013638783972));
#18598=CARTESIAN_POINT('Ctrl Pts',(-0.117686834607281,0.0157664388843013,
0.0815054911419412));
#18599=CARTESIAN_POINT('Ctrl Pts',(-0.117613109409711,6.11591708146765E-5,
0.0825632885263832));
#18600=CARTESIAN_POINT('Ctrl Pts',(-0.117600989619072,5.04992496179954E-5,
0.0424367114736154));
#18601=CARTESIAN_POINT('Ctrl Pts',(-0.117514779739531,-0.0227353060542692,
0.043970994662459));
#18602=CARTESIAN_POINT('Ctrl Pts',(-0.100129952091853,-0.0849605109884783,
0.0481526672255625));
#18603=CARTESIAN_POINT('Ctrl Pts',(0.000787973702835166,-0.139222729671589,
0.054981729162926));
#18604=CARTESIAN_POINT('Ctrl Pts',(0.117431922513572,-0.0747907597173192,
0.0629238972857061));
#18605=CARTESIAN_POINT('Ctrl Pts',(0.126496838785129,0.0581591461343325,
0.070866065408486));
#18606=CARTESIAN_POINT('Ctrl Pts',(0.0196773008918215,0.137828289815661,
0.0788082335312661));
#18607=CARTESIAN_POINT('Ctrl Pts',(-0.0933482651079043,0.0956446566614129,
0.085998448886309));
#18608=CARTESIAN_POINT('Ctrl Pts',(-0.11747670148927,0.0279758085988667,
0.0905412748670923));
#18609=CARTESIAN_POINT('Ctrl Pts',(-0.117715749944134,-0.000104199409386274,
0.0924367114736155));
#18610=CARTESIAN_POINT('Origin',(0.,0.,1.55));
#18611=CARTESIAN_POINT('',(-0.143211704627722,-5.70397197726547E-6,1.50700023576178));
#18612=CARTESIAN_POINT('Ctrl Pts',(-0.0334019664626774,0.112939183906323,
1.532225));
#18613=CARTESIAN_POINT('Ctrl Pts',(-0.0250606930336426,0.115799676338094,
1.53184761307169));
#18614=CARTESIAN_POINT('Ctrl Pts',(-0.0164287086124659,0.117635554524944,
1.53147359869818));
#18615=CARTESIAN_POINT('Ctrl Pts',(-0.00767226928320402,0.118510614220874,
1.53110056493424));
#18616=CARTESIAN_POINT('Ctrl Pts',(-0.0042150196872779,0.118856108509867,
1.53095328237096));
#18617=CARTESIAN_POINT('Ctrl Pts',(-0.000736351480830917,0.119051293525916,
1.53080607672538));
#18618=CARTESIAN_POINT('Ctrl Pts',(0.00274830211697625,0.119097943881266,
1.53065904037218));
#18619=CARTESIAN_POINT('Ctrl Pts',(0.00972321854123044,0.119191319684798,
1.53036473098213));
#18620=CARTESIAN_POINT('Ctrl Pts',(0.0166907125456733,0.118690968429664,
1.53007241075126));
#18621=CARTESIAN_POINT('Ctrl Pts',(0.0235721318645625,0.11762150546261,
1.52978094357425));
#18622=CARTESIAN_POINT('Ctrl Pts',(0.0273478463565568,0.117034709826966,
1.52962102062912));
#18623=CARTESIAN_POINT('Ctrl Pts',(0.0310977188904398,0.116276259986281,
1.52946135449799));
#18624=CARTESIAN_POINT('Ctrl Pts',(0.0348087249896146,0.115347945392283,
1.52930175751644));
#18625=CARTESIAN_POINT('Ctrl Pts',(0.0378768737129624,0.114580442682688,
1.52916980751093));
#18626=CARTESIAN_POINT('Ctrl Pts',(0.0409182562642153,0.113696477767379,
1.52903790896105));
#18627=CARTESIAN_POINT('Ctrl Pts',(0.0439120268522727,0.112701821307647,
1.52890655030309));
#18628=CARTESIAN_POINT('Ctrl Pts',(0.0504861734289241,0.110517613410832,
1.52861809430882));
#18629=CARTESIAN_POINT('Ctrl Pts',(0.0568477403450367,0.107796947733889,
1.528331525126));
#18630=CARTESIAN_POINT('Ctrl Pts',(0.0629211062797432,0.10455513280498,
1.52804576869741));
#18631=CARTESIAN_POINT('Ctrl Pts',(0.0667529140263229,0.102509807084265,
1.52786547926507));
#18632=CARTESIAN_POINT('Ctrl Pts',(0.0704699809867569,0.100256700264741,
1.52768551335768));
#18633=CARTESIAN_POINT('Ctrl Pts',(0.0740519796445933,0.0977963961590643,
1.52750560123222));
#18634=CARTESIAN_POINT('Ctrl Pts',(0.0761474027326905,0.0963571499395001,
1.52740035495562));
#18635=CARTESIAN_POINT('Ctrl Pts',(0.0781972522873126,0.0948464165467323,
1.52729509152825));
#18636=CARTESIAN_POINT('Ctrl Pts',(0.0801950758490376,0.0932655888959708,
1.52718986717129));
#18637=CARTESIAN_POINT('Ctrl Pts',(0.0872135629190184,0.0877120362002772,
1.52682020700562));
#18638=CARTESIAN_POINT('Ctrl Pts',(0.0935342345834078,0.0813437113039547,
1.52645409167081));
#18639=CARTESIAN_POINT('Ctrl Pts',(0.0991216768718319,0.0743433873765979,
1.52608928877518));
#18640=CARTESIAN_POINT('Ctrl Pts',(0.101857856375295,0.0709153174549959,
1.52591064420861));
#18641=CARTESIAN_POINT('Ctrl Pts',(0.104417791592617,0.0673349702414553,
1.52573231437502));
#18642=CARTESIAN_POINT('Ctrl Pts',(0.106794530290299,0.0636205708890664,
1.52555403711528));
#18643=CARTESIAN_POINT('Ctrl Pts',(0.108394385735532,0.0611202951812291,
1.52543403324399));
#18644=CARTESIAN_POINT('Ctrl Pts',(0.109912312880749,0.0585571637778213,
1.52531395827658));
#18645=CARTESIAN_POINT('Ctrl Pts',(0.111341951189028,0.0559432008961949,
1.5251940432238));
#18646=CARTESIAN_POINT('Ctrl Pts',(0.115894033640165,0.0476201345006791,
1.52481222412716));
#18647=CARTESIAN_POINT('Ctrl Pts',(0.119530893641226,0.0388304356906876,
1.52443409356659));
#18648=CARTESIAN_POINT('Ctrl Pts',(0.122195159250079,0.0297595052710396,
1.52405718851832));
#18649=CARTESIAN_POINT('Ctrl Pts',(0.123464283518865,0.0254385629829291,
1.52387764960816));
#18650=CARTESIAN_POINT('Ctrl Pts',(0.124512110981915,0.0210533134598664,
1.52369838877875));
#18651=CARTESIAN_POINT('Ctrl Pts',(0.12532867129748,0.0166220814218575,
1.52351913980531));
#18652=CARTESIAN_POINT('Ctrl Pts',(0.126067828800149,0.012610891624201,
1.52335688207487));
#18653=CARTESIAN_POINT('Ctrl Pts',(0.12661735951473,0.00855739899605222,
1.52319445303817));
#18654=CARTESIAN_POINT('Ctrl Pts',(0.126966826155483,0.00450415768051923,
1.52303280899981));
#18655=CARTESIAN_POINT('Ctrl Pts',(0.127602972227412,-0.00287409603749457,
1.52273856283131));
#18656=CARTESIAN_POINT('Ctrl Pts',(0.12758177643555,-0.010267620141741,
1.52244625042084));
#18657=CARTESIAN_POINT('Ctrl Pts',(0.126865581413421,-0.0175939782534482,
1.52215473434257));
#18658=CARTESIAN_POINT('Ctrl Pts',(0.126426462283551,-0.0220859726121444,
1.52197599770985));
#18659=CARTESIAN_POINT('Ctrl Pts',(0.12572570473317,-0.0265528301690258,
1.52179756043894));
#18660=CARTESIAN_POINT('Ctrl Pts',(0.124776542651163,-0.0309793260681717,
1.52161916036391));
#18661=CARTESIAN_POINT('Ctrl Pts',(0.124151644840291,-0.0338935887106027,
1.52150170748789));
#18662=CARTESIAN_POINT('Ctrl Pts',(0.123418330834614,-0.0367926408403149,
1.52138417707714));
#18663=CARTESIAN_POINT('Ctrl Pts',(0.122581975874549,-0.0396644408336013,
1.52126680258073));
#18664=CARTESIAN_POINT('Ctrl Pts',(0.120074191833131,-0.0482754427851461,
1.52091485884509));
#18665=CARTESIAN_POINT('Ctrl Pts',(0.116656903439717,-0.0566007293654626,
1.52056600333313));
#18666=CARTESIAN_POINT('Ctrl Pts',(0.112443760417108,-0.0645262187619275,
1.52021830866717));
#18667=CARTESIAN_POINT('Ctrl Pts',(0.109356904590302,-0.0703330102694749,
1.51996356219884));
#18668=CARTESIAN_POINT('Ctrl Pts',(0.105841781173658,-0.0759253337267248,
1.51970943888381));
#18669=CARTESIAN_POINT('Ctrl Pts',(0.101930367117466,-0.0812537151913617,
1.51945518067311));
#18670=CARTESIAN_POINT('Ctrl Pts',(0.100130771446666,-0.0837052409256295,
1.51933819945644));
#18671=CARTESIAN_POINT('Ctrl Pts',(0.0982476276828181,-0.0860996963839449,
1.51922123442864));
#18672=CARTESIAN_POINT('Ctrl Pts',(0.0962924325256194,-0.0884227179472683,
1.51910469697823));
#18673=CARTESIAN_POINT('Ctrl Pts',(0.0906946176521128,-0.0950736369671782,
1.51877104482549));
#18674=CARTESIAN_POINT('Ctrl Pts',(0.0844921899154374,-0.101162815315101,
1.51843983772287));
#18675=CARTESIAN_POINT('Ctrl Pts',(0.0777644521522082,-0.106582693579069,
1.51810941878));
#18676=CARTESIAN_POINT('Ctrl Pts',(0.0731067700043679,-0.110334931124879,
1.5178806663426));
#18677=CARTESIAN_POINT('Ctrl Pts',(0.0681966627772886,-0.113766151308436,
1.51765229166508));
#18678=CARTESIAN_POINT('Ctrl Pts',(0.0630541948599911,-0.116833686038022,
1.5174237449583));
#18679=CARTESIAN_POINT('Ctrl Pts',(0.0607686815400033,-0.118197018118406,
1.51732216988754));
#18680=CARTESIAN_POINT('Ctrl Pts',(0.0584414404741937,-0.119485783651375,
1.51722075040181));
#18681=CARTESIAN_POINT('Ctrl Pts',(0.0560784264268894,-0.12069488199044,
1.51711960151386));
#18682=CARTESIAN_POINT('Ctrl Pts',(0.0475595529450054,-0.125053787850271,
1.51675495087613));
#18683=CARTESIAN_POINT('Ctrl Pts',(0.038563113830939,-0.128389854466075,
1.51639315730301));
#18684=CARTESIAN_POINT('Ctrl Pts',(0.0292711048986314,-0.130741856378471,
1.51603205677802));
#18685=CARTESIAN_POINT('Ctrl Pts',(0.0254547302664753,-0.13170786066222,
1.51588374709674));
#18686=CARTESIAN_POINT('Ctrl Pts',(0.0215881861914954,-0.132507324978224,
1.51573555432397));
#18687=CARTESIAN_POINT('Ctrl Pts',(0.0176832233642019,-0.13314066674995,
1.51558732853105));
#18688=CARTESIAN_POINT('Ctrl Pts',(0.0144414794405867,-0.133666441752394,
1.51546427740745));
#18689=CARTESIAN_POINT('Ctrl Pts',(0.0111713231872828,-0.134077605234841,
1.5153411329761));
#18690=CARTESIAN_POINT('Ctrl Pts',(0.00789687394913892,-0.134372952697723,
1.51521845803943));
#18691=CARTESIAN_POINT('Ctrl Pts',(-0.00208492598009478,-0.135273287095873,
1.51484449692866));
#18692=CARTESIAN_POINT('Ctrl Pts',(-0.0121386692885745,-0.135107999768821,
1.51447364169918));
#18693=CARTESIAN_POINT('Ctrl Pts',(-0.0220717676774029,-0.133899092645375,
1.51410356562093));
#18694=CARTESIAN_POINT('Ctrl Pts',(-0.0271373055616968,-0.133282591671289,
1.51391483957382));
#18695=CARTESIAN_POINT('Ctrl Pts',(-0.0321716696217597,-0.132393849601707,
1.51372631615657));
#18696=CARTESIAN_POINT('Ctrl Pts',(-0.0371491047637803,-0.131230566976147,
1.51353768678866));
#18697=CARTESIAN_POINT('Ctrl Pts',(-0.0401763453142056,-0.130523066780721,
1.51342296375255));
#18698=CARTESIAN_POINT('Ctrl Pts',(-0.0431793745847511,-0.129714439573166,
1.51330831773957));
#18699=CARTESIAN_POINT('Ctrl Pts',(-0.0461427198170546,-0.128807808452418,
1.51319405707679));
#18700=CARTESIAN_POINT('Ctrl Pts',(-0.0557912886485991,-0.125855842991896,
1.51282202756853));
#18701=CARTESIAN_POINT('Ctrl Pts',(-0.0650506639775802,-0.121862017750276,
1.51245293010828));
#18702=CARTESIAN_POINT('Ctrl Pts',(-0.0737251756215706,-0.116823260910032,
1.51208446868514));
#18703=CARTESIAN_POINT('Ctrl Pts',(-0.0774533877539874,-0.114657657224767,
1.51192610791459));
#18704=CARTESIAN_POINT('Ctrl Pts',(-0.0810733781510443,-0.112298364258586,
1.51176786463208));
#18705=CARTESIAN_POINT('Ctrl Pts',(-0.0845783705992567,-0.109758519633299,
1.51160955655689));
#18706=CARTESIAN_POINT('Ctrl Pts',(-0.0871260289206952,-0.107912394030924,
1.51149448786814));
#18707=CARTESIAN_POINT('Ctrl Pts',(-0.0896122610481647,-0.105970921032248,
1.51137940572563));
#18708=CARTESIAN_POINT('Ctrl Pts',(-0.0920243025666997,-0.10394826075131,
1.51126473391974));
#18709=CARTESIAN_POINT('Ctrl Pts',(-0.0995315444015674,-0.0976529296958118,
1.51090782920982));
#18710=CARTESIAN_POINT('Ctrl Pts',(-0.106349817996106,-0.090554906599088,
1.51055366538392));
#18711=CARTESIAN_POINT('Ctrl Pts',(-0.112409916721278,-0.0828189535999138,
1.51020021897155));
#18712=CARTESIAN_POINT('Ctrl Pts',(-0.11567060314877,-0.0786565598680515,
1.51001004419521));
#18713=CARTESIAN_POINT('Ctrl Pts',(-0.118711357121208,-0.0743087544864998,
1.50982007711492));
#18714=CARTESIAN_POINT('Ctrl Pts',(-0.121517490738653,-0.0697974244982526,
1.50963000253165));
#18715=CARTESIAN_POINT('Ctrl Pts',(-0.123184827969132,-0.0671169005197731,
1.50951706477726));
#18716=CARTESIAN_POINT('Ctrl Pts',(-0.124768226583796,-0.064379797453554,
1.50940414472167));
#18717=CARTESIAN_POINT('Ctrl Pts',(-0.12625918933752,-0.0616017405091787,
1.50929161182319));
#18718=CARTESIAN_POINT('Ctrl Pts',(-0.131254477666307,-0.0522942005345653,
1.50891458411209));
#18719=CARTESIAN_POINT('Ctrl Pts',(-0.135235816373665,-0.0424980109473837,
1.50854057440173));
#18720=CARTESIAN_POINT('Ctrl Pts',(-0.138100316247284,-0.0323932585971084,
1.50816719719795));
#18721=CARTESIAN_POINT('Ctrl Pts',(-0.139428601593765,-0.027707625827389,
1.5079940600046));
#18722=CARTESIAN_POINT('Ctrl Pts',(-0.140516076092011,-0.0229552175461711,
1.50782105881478));
#18723=CARTESIAN_POINT('Ctrl Pts',(-0.14134846970832,-0.01815262603916,
1.50764795577689));
#18724=CARTESIAN_POINT('Ctrl Pts',(-0.141840021659925,-0.0153165600461233,
1.5075457335416));
#18725=CARTESIAN_POINT('Ctrl Pts',(-0.142241997144177,-0.0124651428186592,
1.50744355431084));
#18726=CARTESIAN_POINT('Ctrl Pts',(-0.142550993842162,-0.00961078035088443,
1.50734168592779));
#18727=CARTESIAN_POINT('Ctrl Pts',(-0.142847161918882,-0.00687492249914849,
1.50724404681617));
#18728=CARTESIAN_POINT('Ctrl Pts',(-0.143058332724879,-0.00413406598225375,
1.5071466105924));
#18729=CARTESIAN_POINT('Ctrl Pts',(-0.143182669649515,-0.00139134585336764,
1.50704933585643));
#18730=CARTESIAN_POINT('Ctrl Pts',(-0.143203595382121,-0.00092974984559876,
1.50703296465278));
#18731=CARTESIAN_POINT('Ctrl Pts',(-0.143222061023464,-0.000468100854706259,
1.50701659802318));
#18732=CARTESIAN_POINT('Ctrl Pts',(-0.143238079070951,-6.41379011939899E-6,
1.50700023577028));
#18733=CARTESIAN_POINT('',(-0.00156744678985144,0.146109855568756,1.50365));
#18734=CARTESIAN_POINT('Ctrl Pts',(-0.00156962371672063,0.146072546381438,
1.50365));
#18735=CARTESIAN_POINT('Ctrl Pts',(-0.011711474284147,0.144648739717271,
1.50495065132295));
#18736=CARTESIAN_POINT('Ctrl Pts',(-0.0216501921041044,0.142222471223284,
1.50626105010813));
#18737=CARTESIAN_POINT('Ctrl Pts',(-0.0312062965385204,0.138804788898175,
1.50759029209282));
#18738=CARTESIAN_POINT('Ctrl Pts',(-0.0379863325344082,0.136379950477271,
1.50853338648503));
#18739=CARTESIAN_POINT('Ctrl Pts',(-0.0445735484268955,0.133455002060128,
1.5094859663039));
#18740=CARTESIAN_POINT('Ctrl Pts',(-0.0508923708069948,0.130021662144985,
1.51045128011208));
#18741=CARTESIAN_POINT('Ctrl Pts',(-0.053607485163773,0.128546401418451,
1.51086606268101));
#18742=CARTESIAN_POINT('Ctrl Pts',(-0.0562647183424556,0.126981576978965,
1.51128195276517));
#18743=CARTESIAN_POINT('Ctrl Pts',(-0.0588579379029418,0.125328026221608,
1.51169910067666));
#18744=CARTESIAN_POINT('Ctrl Pts',(-0.0624505046767585,0.123037247762191,
1.51227700458785));
#18745=CARTESIAN_POINT('Ctrl Pts',(-0.0659209207101175,0.120575889029892,
1.51285741907924));
#18746=CARTESIAN_POINT('Ctrl Pts',(-0.0692542752175272,0.117943487410649,
1.51344114883776));
#18747=CARTESIAN_POINT('Ctrl Pts',(-0.0735613784355843,0.114542101371374,
1.51419539934302));
#18748=CARTESIAN_POINT('Ctrl Pts',(-0.0776398170223455,0.110855132244726,
1.51495518495604));
#18749=CARTESIAN_POINT('Ctrl Pts',(-0.0814741368103916,0.106911749311875,
1.51572224163114));
#18750=CARTESIAN_POINT('Ctrl Pts',(-0.0845038784997064,0.103795829845314,
1.51632834224744));
#18751=CARTESIAN_POINT('Ctrl Pts',(-0.087381117690253,0.10051973853988,
1.51693898261853));
#18752=CARTESIAN_POINT('Ctrl Pts',(-0.0900959757046659,0.0970973798321736,
1.51755501917095));
#18753=CARTESIAN_POINT('Ctrl Pts',(-0.0920052356275281,0.0946905606587243,
1.51798825505079));
#18754=CARTESIAN_POINT('Ctrl Pts',(-0.093830595110286,0.092215607777745,
1.51842338946406));
#18755=CARTESIAN_POINT('Ctrl Pts',(-0.0955653742165971,0.0896840982544811,
1.51885969689116));
#18756=CARTESIAN_POINT('Ctrl Pts',(-0.0997851775729162,0.0835262696618028,
1.51992100293214));
#18757=CARTESIAN_POINT('Ctrl Pts',(-0.103479134251024,0.0770231540939269,
1.52099120961793));
#18758=CARTESIAN_POINT('Ctrl Pts',(-0.106606394578922,0.0702509006766953,
1.52207541818308));
#18759=CARTESIAN_POINT('Ctrl Pts',(-0.108879606303698,0.0653281362576702,
1.52286353153598));
#18760=CARTESIAN_POINT('Ctrl Pts',(-0.110852991156964,0.0602629640702717,
1.52365904329275));
#18761=CARTESIAN_POINT('Ctrl Pts',(-0.112503888351057,0.0550849881514033,
1.524463912762));
#18762=CARTESIAN_POINT('Ctrl Pts',(-0.113450017754745,0.0521174894567802,
1.52492518356294));
#18763=CARTESIAN_POINT('Ctrl Pts',(-0.114289979676541,0.0491121240008169,
1.52538965304266));
#18764=CARTESIAN_POINT('Ctrl Pts',(-0.115015874151616,0.0460903162170444,
1.52585530945224));
#18765=CARTESIAN_POINT('Ctrl Pts',(-0.117053612444637,0.0376074669234184,
1.52716250482259));
#18766=CARTESIAN_POINT('Ctrl Pts',(-0.118206139871793,0.0289652499882669,
1.52848357355921));
#18767=CARTESIAN_POINT('Ctrl Pts',(-0.11838625730212,0.0202925750432425,
1.52982832573377));
#18768=CARTESIAN_POINT('Ctrl Pts',(-0.118492077855379,0.015197303257165,
1.53061837930521));
#18769=CARTESIAN_POINT('Ctrl Pts',(-0.118261361656021,0.0100916471271278,
1.53141660760476));
#18770=CARTESIAN_POINT('Ctrl Pts',(-0.11766859746431,0.00500517689818842,
1.532225));
#18771=CARTESIAN_POINT('',(-0.115079981391543,0.0902137050004572,1.50365));
#18772=CARTESIAN_POINT('Origin',(0.,0.,1.50365));
#18773=CARTESIAN_POINT('Ctrl Pts',(-0.143238079070951,-6.41379011939899E-6,
1.50700023577028));
#18774=CARTESIAN_POINT('Ctrl Pts',(-0.143514357617001,0.00795674345750163,
1.50671802038504));
#18775=CARTESIAN_POINT('Ctrl Pts',(-0.14306421847979,0.0159310909218757,
1.50643710681857));
#18776=CARTESIAN_POINT('Ctrl Pts',(-0.141940608246003,0.023841490005315,
1.50615648267927));
#18777=CARTESIAN_POINT('Ctrl Pts',(-0.141317731836386,0.0282266413964,1.50600091791928));
#18778=CARTESIAN_POINT('Ctrl Pts',(-0.14048752132733,0.0325921818867556,
1.50584544210227));
#18779=CARTESIAN_POINT('Ctrl Pts',(-0.139456452513291,0.0369250818702156,
1.5056898827608));
#18780=CARTESIAN_POINT('Ctrl Pts',(-0.138790989895207,0.0397215809279161,
1.50558948313156));
#18781=CARTESIAN_POINT('Ctrl Pts',(-0.138042009924554,0.0425029011667524,
1.50548910366784));
#18782=CARTESIAN_POINT('Ctrl Pts',(-0.137214434473447,0.0452564915355094,
1.50538902890071));
#18783=CARTESIAN_POINT('Ctrl Pts',(-0.134176751889031,0.0553637675507716,
1.50502169637912));
#18784=CARTESIAN_POINT('Ctrl Pts',(-0.130076454936343,0.0651325632434767,
1.50465723703036));
#18785=CARTESIAN_POINT('Ctrl Pts',(-0.125018127980614,0.0743940890034878,
1.50429344851366));
#18786=CARTESIAN_POINT('Ctrl Pts',(-0.122034683484208,0.0798566160996726,
1.50407888293545));
#18787=CARTESIAN_POINT('Ctrl Pts',(-0.118716925567465,0.0851425936725427,
1.50386455072235));
#18788=CARTESIAN_POINT('Ctrl Pts',(-0.115078604842436,0.0902138214954005,
1.50365));
#18789=CARTESIAN_POINT('',(-0.05,-6.12323399573677E-18,1.6));
#18790=CARTESIAN_POINT('',(-0.1,-1.22464679914735E-17,1.55));
#18791=CARTESIAN_POINT('Origin',(0.,0.,1.6));
#18792=CARTESIAN_POINT('Ctrl Pts',(0.0850780204044575,-0.11908002747757,
-0.0164977839420936));
#18793=CARTESIAN_POINT('Ctrl Pts',(0.124677800165771,-0.0907875342533835,
-0.0138514540629917));
#18794=CARTESIAN_POINT('Ctrl Pts',(0.172751483861701,0.00791416360185712,
-0.00855879430478784));
#18795=CARTESIAN_POINT('Ctrl Pts',(0.0868617128612901,0.149726167188418,
-0.000619804667482127));
#18796=CARTESIAN_POINT('Ctrl Pts',(-0.078614020905812,0.154028602276276,
0.00731918496982359));
#18797=CARTESIAN_POINT('Ctrl Pts',(-0.172087192378165,0.0175525219725009,
0.0152581746071293));
#18798=CARTESIAN_POINT('Ctrl Pts',(-0.108045720411827,-0.135108484733225,
0.0231971642444351));
#18799=CARTESIAN_POINT('Ctrl Pts',(0.0549144151285058,-0.164025561655164,
0.0311361538817407));
#18800=CARTESIAN_POINT('Ctrl Pts',(0.167598788591005,-0.0428207868793744,
0.0390751435190465));
#18801=CARTESIAN_POINT('Ctrl Pts',(0.126860790413016,0.117600499296196,
0.0470141331563521));
#18802=CARTESIAN_POINT('Ctrl Pts',(-0.0300110592737492,0.170357625684536,
0.054953122793658));
#18803=CARTESIAN_POINT('Ctrl Pts',(-0.159409054995301,0.0671687418111174,
0.0628921124309635));
#18804=CARTESIAN_POINT('Ctrl Pts',(-0.142879399887002,-0.0975110083167992,
0.0708311020682695));
#18805=CARTESIAN_POINT('Ctrl Pts',(0.00444677171871267,-0.172924803493063,
0.078770091705575));
#18806=CARTESIAN_POINT('Ctrl Pts',(0.147702113712341,-0.0900384822365835,
0.0867090813428809));
#18807=CARTESIAN_POINT('Ctrl Pts',(0.155746353789385,0.0752722621313087,
0.0946480709801864));
#18808=CARTESIAN_POINT('Ctrl Pts',(0.021215449100004,0.17167621786987,0.102587060617492));
#18809=CARTESIAN_POINT('Ctrl Pts',(-0.132736728465598,0.110922462699857,
0.110526050254798));
#18810=CARTESIAN_POINT('Ctrl Pts',(-0.165177537004225,-0.0513732581591355,
0.118465039892104));
#18811=CARTESIAN_POINT('Ctrl Pts',(-0.0464096261145344,-0.166640254043574,
0.126404029529409));
#18812=CARTESIAN_POINT('Ctrl Pts',(0.114843114370719,-0.129359532685675,
0.134343019166715));
#18813=CARTESIAN_POINT('Ctrl Pts',(0.170964855654229,0.0263409830179588,
0.142282008804021));
#18814=CARTESIAN_POINT('Ctrl Pts',(0.0705799878925336,0.157928129946847,
0.150220998441327));
#18815=CARTESIAN_POINT('Ctrl Pts',(-0.0944160212638482,0.144942899583874,
0.158159988078632));
#18816=CARTESIAN_POINT('Ctrl Pts',(-0.172980633894512,-0.000727622896455919,
0.166098977715938));
#18817=CARTESIAN_POINT('Ctrl Pts',(-0.0931933312323777,-0.145732055885043,
0.174037967353244));
#18818=CARTESIAN_POINT('Ctrl Pts',(0.0719060791645076,-0.157328779695546,
0.181976956990549));
#18819=CARTESIAN_POINT('Ctrl Pts',(0.171180402159323,-0.0249017879745179,
0.189915946627855));
#18820=CARTESIAN_POINT('Ctrl Pts',(0.113750798721884,0.13032108391891,0.197854936265161));
#18821=CARTESIAN_POINT('Ctrl Pts',(-0.0478098650864174,0.16624393501773,
0.205793925902467));
#18822=CARTESIAN_POINT('Ctrl Pts',(-0.16560387403618,0.0499818570245514,
0.213732915539772));
#18823=CARTESIAN_POINT('Ctrl Pts',(-0.131798885878402,-0.112035185581475,
0.221671905177078));
#18824=CARTESIAN_POINT('Ctrl Pts',(0.0226589495323734,-0.171491694067101,
0.229610894814384));
#18825=CARTESIAN_POINT('Ctrl Pts',(0.156374069566079,-0.073959309724122,
0.237549884451689));
#18826=CARTESIAN_POINT('Ctrl Pts',(0.146939445926624,0.0912777539068999,
0.245488874088995));
#18827=CARTESIAN_POINT('Ctrl Pts',(0.00299182995941577,0.172956289510158,
0.253427863726301));
#18828=CARTESIAN_POINT('Ctrl Pts',(-0.143694601292225,0.0963051955349955,
0.261366853363607));
#18829=CARTESIAN_POINT('Ctrl Pts',(-0.15883847309497,-0.0685067047260848,
0.269305843000912));
#18830=CARTESIAN_POINT('Ctrl Pts',(-0.0285766086907934,-0.170605411881679,
0.277244832638218));
#18831=CARTESIAN_POINT('Ctrl Pts',(0.12784518248692,-0.116526556812001,
0.285183822275524));
#18832=CARTESIAN_POINT('Ctrl Pts',(0.167233470900423,0.0442243749325307,
0.293122811912829));
#18833=CARTESIAN_POINT('Ctrl Pts',(0.0535309779628647,0.164490922320707,
0.301061801550136));
#18834=CARTESIAN_POINT('Ctrl Pts',(-0.109175456582181,0.134177303623408,
0.309000791187441));
#18835=CARTESIAN_POINT('Ctrl Pts',(-0.171939242908932,-0.0189664407699395,
0.316939780824747));
#18836=CARTESIAN_POINT('Ctrl Pts',(-0.0773044361184472,-0.154747708493488,
0.324878770462053));
#18837=CARTESIAN_POINT('Ctrl Pts',(0.0880972839194656,-0.148868054644337,
0.332817760099358));
#18838=CARTESIAN_POINT('Ctrl Pts',(0.172851978230285,-0.00670989936239309,
0.340756749736664));
#18839=CARTESIAN_POINT('Ctrl Pts',(0.0993725327910066,0.141590708926387,
0.34869573937397));
#18840=CARTESIAN_POINT('Ctrl Pts',(-0.0650756559739905,0.160274727038081,
0.356634729011275));
#18841=CARTESIAN_POINT('Ctrl Pts',(-0.169951541620772,0.0322382168908211,
0.364573718648582));
#18842=CARTESIAN_POINT('Ctrl Pts',(-0.119248438453561,-0.125310171390688,
0.372512708285886));
#18843=CARTESIAN_POINT('Ctrl Pts',(0.0406184374886585,-0.168145685830938,
0.380451697923193));
#18844=CARTESIAN_POINT('Ctrl Pts',(0.163301917673335,-0.0570553486694088,
0.388390687560498));
#18845=CARTESIAN_POINT('Ctrl Pts',(0.136493684039406,0.106265249940549,
0.396329677197804));
#18846=CARTESIAN_POINT('Ctrl Pts',(-0.0152651628095069,0.172307295063139,
0.404268666835109));
#18847=CARTESIAN_POINT('Ctrl Pts',(-0.153049799296248,0.0806138205455782,
0.412207656472416));
#18848=CARTESIAN_POINT('Ctrl Pts',(-0.150727833715048,-0.0848760818555219,
0.420146646109721));
#18849=CARTESIAN_POINT('Ctrl Pts',(-0.0104248664208018,-0.172667748255674,
0.428085635747027));
#18850=CARTESIAN_POINT('Ctrl Pts',(0.139421351618932,-0.10239392482138,
0.436024625384332));
#18851=CARTESIAN_POINT('Ctrl Pts',(0.16163687742079,0.0616145192729195,
0.443963615021638));
#18852=CARTESIAN_POINT('Ctrl Pts',(0.0358849196425865,0.169219093691645,
0.451902604658944));
#18853=CARTESIAN_POINT('Ctrl Pts',(-0.122717222714247,0.121915185177559,
0.45984159429625));
#18854=CARTESIAN_POINT('Ctrl Pts',(-0.168980158036723,-0.0369937199732681,
0.467780583933555));
#18855=CARTESIAN_POINT('Ctrl Pts',(-0.0605533396431397,-0.162037409833775,
0.475719573570861));
#18856=CARTESIAN_POINT('Ctrl Pts',(0.103305911202344,-0.138746956140414,
0.483658563208167));
#18857=CARTESIAN_POINT('Ctrl Pts',(0.172595680358559,0.0115568269495825,
0.491597552845473));
#18858=CARTESIAN_POINT('Ctrl Pts',(0.0838859329010004,0.151281127008313,
0.499536542482778));
#18859=CARTESIAN_POINT('Ctrl Pts',(-0.0816156370489812,0.152517923263679,
0.507475532120084));
#18860=CARTESIAN_POINT('Ctrl Pts',(-0.172403684765527,0.0141350135070757,
0.51541452175739));
#18861=CARTESIAN_POINT('Ctrl Pts',(-0.105367974675403,-0.137187532379513,
0.523353511394695));
#18862=CARTESIAN_POINT('Ctrl Pts',(0.0581248948911363,-0.162924294448283,
0.531292501032001));
#18863=CARTESIAN_POINT('Ctrl Pts',(0.168408406744046,-0.039515030880773,
0.539231490669306));
#18864=CARTESIAN_POINT('Ctrl Pts',(0.124525564004667,0.120067535316156,
0.547170480306613));
#18865=CARTESIAN_POINT('Ctrl Pts',(-0.0333518982867267,0.169736501696743,
0.555109469943918));
#18866=CARTESIAN_POINT('Ctrl Pts',(-0.160697983451488,0.0640233335761385,
0.563048459581225));
#18867=CARTESIAN_POINT('Ctrl Pts',(-0.14093607811848,-0.100298808627811,
0.570987449218529));
#18868=CARTESIAN_POINT('Ctrl Pts',(0.00784314775175556,-0.172804265459278,
0.578926438855836));
#18869=CARTESIAN_POINT('Ctrl Pts',(0.149442509381278,-0.0871192603125336,
0.586865428493141));
#18870=CARTESIAN_POINT('Ctrl Pts',(0.154237495636292,0.0783174569774929,
0.594804418130446));
#18871=CARTESIAN_POINT('Ctrl Pts',(0.0178386252221998,0.172059909850489,
0.602743407767753));
#18872=CARTESIAN_POINT('Ctrl Pts',(-0.134890284021987,0.108293307291099,
0.610682397405058));
#18873=CARTESIAN_POINT('Ctrl Pts',(-0.164136382878957,-0.0546083962682395,
0.618621387042364));
#18874=CARTESIAN_POINT('Ctrl Pts',(-0.0431268722112106,-0.167519855601819,
0.62656037667967));
#18875=CARTESIAN_POINT('Ctrl Pts',(0.117362334288317,-0.127078368017432,
0.634499366316975));
#18876=CARTESIAN_POINT('Ctrl Pts',(0.170414367112955,0.0296946562375699,
0.642438355954282));
#18877=CARTESIAN_POINT('Ctrl Pts',(0.0674637261050104,0.159284257814778,
0.650377345591586));
#18878=CARTESIAN_POINT('Ctrl Pts',(-0.0972453325609638,0.143060037825677,
0.658316335228894));
#18879=CARTESIAN_POINT('Ctrl Pts',(-0.172932953925271,-0.00412584224812367,
0.666255324866198));
#18880=CARTESIAN_POINT('Ctrl Pts',(-0.0903123078403481,-0.147534796506203,
0.674194314503505));
#18881=CARTESIAN_POINT('Ctrl Pts',(0.0749830665657334,-0.155885755782802,
0.68213330414081));
#18882=CARTESIAN_POINT('Ctrl Pts',(0.17163658245605,-0.021533989188811,
0.690072293778116));
#18883=CARTESIAN_POINT('Ctrl Pts',(0.11116857013107,0.132530668686874,0.698011283415421));
#18884=CARTESIAN_POINT('Ctrl Pts',(-0.0510666492692211,0.165272582299639,
0.705950273052727));
#18885=CARTESIAN_POINT('Ctrl Pts',(-0.166553851089581,0.0467187736868841,
0.713889262690032));
#18886=CARTESIAN_POINT('Ctrl Pts',(-0.129572416918314,-0.114602870389546,
0.721828252327339));
#18887=CARTESIAN_POINT('Ctrl Pts',(0.0260236847639906,-0.171013440871999,
0.729767241964644));
#18888=CARTESIAN_POINT('Ctrl Pts',(0.157796886564457,-0.0708729265526718,
0.73770623160195));
#18889=CARTESIAN_POINT('Ctrl Pts',(0.145117853242075,0.0941468947867542,
0.745645221239255));
#18890=CARTESIAN_POINT('Ctrl Pts',(-0.000406629147419015,0.172981686256994,
0.753584210876562));
#18891=CARTESIAN_POINT('Ctrl Pts',(-0.145558870420566,0.0934635991681543,
0.761523200513868));
#18892=CARTESIAN_POINT('Ctrl Pts',(-0.157461941624574,-0.0716140074803496,
0.769462190151172));
#18893=CARTESIAN_POINT('Ctrl Pts',(-0.0252193968429213,-0.17113389830906,
0.777401179788479));
#18894=CARTESIAN_POINT('Ctrl Pts',(0.130109777350283,-0.113992433807847,
0.785340169425784));
#18895=CARTESIAN_POINT('Ctrl Pts',(0.166332367384696,0.0475012914327479,
0.793279159063091));
#18896=CARTESIAN_POINT('Ctrl Pts',(0.0502890745800368,0.165510839842773,
0.801218148700395));
#18897=CARTESIAN_POINT('Ctrl Pts',(-0.111790419467279,0.132006557575396,
0.809157138337702));
#18898=CARTESIAN_POINT('Ctrl Pts',(-0.171533445990104,-0.0223406811520247,
0.817096127975007));
#18899=CARTESIAN_POINT('Ctrl Pts',(-0.0742493586638003,-0.156236557391639,
0.825035117612313));
#18900=CARTESIAN_POINT('Ctrl Pts',(0.0910049278783345,-0.147108572929777,
0.832974107249618));
#18901=CARTESIAN_POINT('Ctrl Pts',(0.172950439922886,-0.00331277195964383,
0.840913096886925));
#18902=CARTESIAN_POINT('Ctrl Pts',(0.0965716772857839,0.143515644700454,
0.848852086524229));
#18903=CARTESIAN_POINT('Ctrl Pts',(-0.0682118374171683,0.158965324406771,
0.856791076161536));
#18904=CARTESIAN_POINT('Ctrl Pts',(-0.170552089827228,0.0288931442238776,
0.864730065798841));
#18905=CARTESIAN_POINT('Ctrl Pts',(-0.116763592698541,-0.127628729319482,
0.872669055436147));
#18906=CARTESIAN_POINT('Ctrl Pts',(0.0439139712140358,-0.167315248138923,
0.880608045073453));
#18907=CARTESIAN_POINT('Ctrl Pts',(0.164391304101163,-0.0538361241500125,
0.888547034710759));
#18908=CARTESIAN_POINT('Ctrl Pts',(0.134379664555536,0.108926281867684,
0.896486024348063));
#18909=CARTESIAN_POINT('Ctrl Pts',(-0.018647348250808,0.17197414204115,
0.904425013985371));
#18910=CARTESIAN_POINT('Ctrl Pts',(-0.154603991719776,0.0775914613336281,
0.912364003622676));
#18911=CARTESIAN_POINT('Ctrl Pts',(-0.149031276472826,-0.0878208845346985,
0.920302993259982));
#18912=CARTESIAN_POINT('Ctrl Pts',(-0.00703064139541984,-0.172839229369798,
0.928241982897287));
#18913=CARTESIAN_POINT('Ctrl Pts',(0.141406064038169,-0.099635105162837,
0.936180972534593));
#18914=CARTESIAN_POINT('Ctrl Pts',(0.160395209035295,0.064778129380991,
0.944119962171899));
#18915=CARTESIAN_POINT('Ctrl Pts',(0.03255353276219,0.169891426011666,0.952058951809204));
#18916=CARTESIAN_POINT('Ctrl Pts',(-0.125088671715395,0.119480765548496,
0.959997941446511));
#18917=CARTESIAN_POINT('Ctrl Pts',(-0.168220770124088,-0.040306347222682,
0.967936931083815));
#18918=CARTESIAN_POINT('Ctrl Pts',(-0.0573582824064844,-0.163195761485875,
0.975875920721122));
#18919=CARTESIAN_POINT('Ctrl Pts',(0.106011781834435,-0.136690640644722,
0.983814910358427));
#18920=CARTESIAN_POINT('Ctrl Pts',(0.17233532526783,0.014945393685262,0.991753899995733));
#18921=CARTESIAN_POINT('Ctrl Pts',(0.0808976893297158,0.152899944371113,
0.999692889633039));
#18922=CARTESIAN_POINT('Ctrl Pts',(-0.0845962369090198,0.150885074902754,
1.00763187927034));
#18923=CARTESIAN_POINT('Ctrl Pts',(-0.172648106016301,0.0107452601904448,
1.01557086890765));
#18924=CARTESIAN_POINT('Ctrl Pts',(-0.102652466413112,-0.13923110380544,
1.02350985854496));
#18925=CARTESIAN_POINT('Ctrl Pts',(0.0613144709582997,-0.161750934398167,
1.03144884818226));
#18926=CARTESIAN_POINT('Ctrl Pts',(0.169152212322519,-0.0361988700648799,
1.03938783781957));
#18927=CARTESIAN_POINT('Ctrl Pts',(0.122142696063681,0.12249077894222,1.04732682745687));
#18928=CARTESIAN_POINT('Ctrl Pts',(-0.0366800874558037,0.169048514669047,
1.05526581709418));
#18929=CARTESIAN_POINT('Ctrl Pts',(-0.161924764760067,0.0608539208677085,
1.06320480673148));
#18930=CARTESIAN_POINT('Ctrl Pts',(-0.138938417355371,-0.103048266896446,
1.07114379636879));
#18931=CARTESIAN_POINT('Ctrl Pts',(0.011236529066559,-0.172616828675865,
1.0790827860061));
#18932=CARTESIAN_POINT('Ctrl Pts',(0.151125203217684,-0.0841665140064042,
1.0870217756434));
#18933=CARTESIAN_POINT('Ctrl Pts',(0.152669111109608,0.0813324759279986,
1.09496076528071));
#18934=CARTESIAN_POINT('Ctrl Pts',(0.0144549108781955,0.172377158228925,
1.10289975491801));
#18935=CARTESIAN_POINT('Ctrl Pts',(-0.136991769602464,0.10562236594946,
1.11083874455532));
#18936=CARTESIAN_POINT('Ctrl Pts',(-0.163031873671196,-0.0578224635832477,
1.11877773419263));
#18937=CARTESIAN_POINT('Ctrl Pts',(-0.0398274706979539,-0.168334790537727,
1.12671672382993));
#18938=CARTESIAN_POINT('Ctrl Pts',(0.119836252144435,-0.124748153491552,
1.13465571346724));
#18939=CARTESIAN_POINT('Ctrl Pts',(0.169798099063322,0.0330368685268242,
1.14259470310454));
#18940=CARTESIAN_POINT('Ctrl Pts',(0.0643214233134591,0.160578901573361,
1.15053369274185));
#18941=CARTESIAN_POINT('Ctrl Pts',(-0.100037107244844,0.141121955420339,
1.15847268237915));
#18942=CARTESIAN_POINT('Ctrl Pts',(-0.172818522111203,-0.00752246920075927,
1.16641167201646));
#18943=CARTESIAN_POINT('Ctrl Pts',(-0.0873964240115842,-0.149280588817046,
1.17435066165376));
#18944=CARTESIAN_POINT('Ctrl Pts',(0.0780311106025284,-0.154382560238235,
1.18228965129107));
#18945=CARTESIAN_POINT('Ctrl Pts',(0.172026511281289,-0.01815787828917,
1.19022864092837));
#18946=CARTESIAN_POINT('Ctrl Pts',(0.10854343062882,0.134689096792963,1.19816763056568));
#18947=CARTESIAN_POINT('Ctrl Pts',(-0.0543037217972188,0.164237434607784,
1.20610662020299));
#18948=CARTESIAN_POINT('Ctrl Pts',(-0.167439538594998,0.0434376569656869,
1.21404560984029));
#18949=CARTESIAN_POINT('Ctrl Pts',(-0.127295933190098,-0.117126318651471,
1.2219845994776));
#18950=CARTESIAN_POINT('Ctrl Pts',(0.0293783748903316,-0.170469176734012,
1.2299235891149));
#18951=CARTESIAN_POINT('Ctrl Pts',(0.159158794190081,-0.0677591865323411,
1.23786257875221));
#18952=CARTESIAN_POINT('Ctrl Pts',(0.143240245273553,0.0969796950995427,
1.24580156838952));
#18953=CARTESIAN_POINT('Ctrl Pts',(-0.00380493129617075,0.172940312320012,
1.25374055802682));
#18954=CARTESIAN_POINT('Ctrl Pts',(-0.147366954032488,0.0905859259858403,
1.26167954766413));
#18955=CARTESIAN_POINT('Ctrl Pts',(-0.156024630070406,-0.074693667330688,
1.26961853730143));
#18956=CARTESIAN_POINT('Ctrl Pts',(-0.0218524503424686,-0.171596327294885,
1.27755752693874));
#18957=CARTESIAN_POINT('Ctrl Pts',(0.132324150022753,-0.111414309889572,
1.28549651657604));
#18958=CARTESIAN_POINT('Ctrl Pts',(0.165367059817933,0.0507598725070622,
1.29343550621335));
#18959=CARTESIAN_POINT('Ctrl Pts',(0.0470277596764783,0.166466870408131,
1.30137449585065));
#18960=CARTESIAN_POINT('Ctrl Pts',(-0.114362231391601,0.129784857201791,
1.30931348548797));
#18961=CARTESIAN_POINT('Ctrl Pts',(-0.171061437441431,-0.0257062980954763,
1.31725247512526));
#18962=CARTESIAN_POINT('Ctrl Pts',(-0.071165620995849,-0.157665099140374,
1.32519146476257));
#18963=CARTESIAN_POINT('Ctrl Pts',(0.0938774439379855,-0.145292307632914,
1.33313045439988));
#18964=CARTESIAN_POINT('Ctrl Pts',(0.172982143233999,8.56343898915854E-5,
1.34106944403719));
#18965=CARTESIAN_POINT('Ctrl Pts',(0.0937335447930804,0.145385183220099,
1.34900843367449));
#18966=CARTESIAN_POINT('Ctrl Pts',(-0.0713216883190155,0.157594562185848,
1.3569474233118));
#18967=CARTESIAN_POINT('Ctrl Pts',(-0.171086806821499,0.0255369173285507,
1.3648864129491));
#18968=CARTESIAN_POINT('Ctrl Pts',(-0.114233673229396,-0.129898019862958,
1.37282540258641));
#18969=CARTESIAN_POINT('Ctrl Pts',(0.0471925482590101,-0.166420232464351,
1.38076439222371));
#18970=CARTESIAN_POINT('Ctrl Pts',(0.165417247017141,-0.0505961085897048,
1.38870338186102));
#18971=CARTESIAN_POINT('Ctrl Pts',(0.132213753266125,0.111545248710567,
1.39664237149832));
#18972=CARTESIAN_POINT('Ctrl Pts',(-0.0220222951247444,0.17157464463752,
1.40458136113563));
#18973=CARTESIAN_POINT('Ctrl Pts',(-0.156098584526576,0.0745390809398717,
1.41252035077293));
#18974=CARTESIAN_POINT('Ctrl Pts',(-0.147277046608992,-0.0907316537045687,
1.42045934041024));
#18975=CARTESIAN_POINT('Ctrl Pts',(-0.00363398118293899,-0.172944250658386,
1.42839833004755));
#18976=CARTESIAN_POINT('Ctrl Pts',(0.143336722904634,-0.0968373407211472,
1.43633731968485));
#18977=CARTESIAN_POINT('Ctrl Pts',(0.159090624036536,0.0679158129692223,
1.44427630932216));
#18978=CARTESIAN_POINT('Ctrl Pts',(0.0292114869387437,0.170499931406899,
1.45221529895946));
#18979=CARTESIAN_POINT('Ctrl Pts',(-0.127415456569397,0.116996902323752,
1.46015428859677));
#18980=CARTESIAN_POINT('Ctrl Pts',(-0.167389576437263,-0.0435971050111283,
1.46809327823408));
#18981=CARTESIAN_POINT('Ctrl Pts',(-0.0541541359620402,-0.164303103757731,
1.47603226787138));
#18982=CARTESIAN_POINT('Ctrl Pts',(0.108701533888403,-0.13455879509903,
1.48397125750869));
#18983=CARTESIAN_POINT('Ctrl Pts',(0.171961157005542,0.0182848320604298,
1.49191024714599));
#18984=CARTESIAN_POINT('Ctrl Pts',(0.0779697431325927,0.154543202561513,
1.4998492367833));
#18985=CARTESIAN_POINT('Ctrl Pts',(-0.0877325682749983,0.149025855561406,
1.5077882264206));
#18986=CARTESIAN_POINT('Ctrl Pts',(-0.144149484752264,0.0548439265155397,
1.51308088617881));
#18987=CARTESIAN_POINT('Ctrl Pts',(-0.146217781693078,0.00621955116994065,
1.51572721605791));
#18988=CARTESIAN_POINT('Ctrl Pts',(0.0795408277542855,-0.111329858282327,
-0.0109985226280624));
#18989=CARTESIAN_POINT('Ctrl Pts',(0.116563307192903,-0.0848787452970238,
-0.00835219274896048));
#18990=CARTESIAN_POINT('Ctrl Pts',(0.16150817751539,0.00739908052493189,
-0.00305953299075667));
#18991=CARTESIAN_POINT('Ctrl Pts',(0.0812084309002137,0.139981433724326,
0.00487945664654907));
#18992=CARTESIAN_POINT('Ctrl Pts',(-0.0734975292821143,0.144003850402812,
0.0128184462838548));
#18993=CARTESIAN_POINT('Ctrl Pts',(-0.160887120581772,0.0164101388376342,
0.0207574359211605));
#18994=CARTESIAN_POINT('Ctrl Pts',(-0.101013704785435,-0.126315124179183,
0.0286964255584662));
#18995=CARTESIAN_POINT('Ctrl Pts',(0.0513403816191153,-0.153350170642076,
0.0366354151957719));
#18996=CARTESIAN_POINT('Ctrl Pts',(0.156690838735662,-0.0400338514845966,
0.0445744048330777));
#18997=CARTESIAN_POINT('Ctrl Pts',(0.118604220350264,0.109946623274354,
0.0525133944703833));
#18998=CARTESIAN_POINT('Ctrl Pts',(-0.0280578283917351,0.15927012049393,
0.0604523841076892));
#18999=CARTESIAN_POINT('Ctrl Pts',(-0.14903412333264,0.0627971513379326,
0.0683913737449947));
#19000=CARTESIAN_POINT('Ctrl Pts',(-0.133580279395553,-0.0911646307683348,
0.0763303633823007));
#19001=CARTESIAN_POINT('Ctrl Pts',(0.0041573593468571,-0.161670216863261,
0.0842693530196062));
#19002=CARTESIAN_POINT('Ctrl Pts',(0.138089113144455,-0.0841784443595545,
0.0922083426569122));
#19003=CARTESIAN_POINT('Ctrl Pts',(0.14560980428584,0.0703732645446943,
0.100147332294218));
#19004=CARTESIAN_POINT('Ctrl Pts',(0.0198346691022095,0.160502893816501,
0.108086321931524));
#19005=CARTESIAN_POINT('Ctrl Pts',(-0.124097730593135,0.103703218031488,
0.116025311568829));
#19006=CARTESIAN_POINT('Ctrl Pts',(-0.154427171169137,-0.0480296962598115,
0.123964301206135));
#19007=CARTESIAN_POINT('Ctrl Pts',(-0.0433891157712434,-0.155794689166463,
0.13190329084344));
#19008=CARTESIAN_POINT('Ctrl Pts',(0.107368699171666,-0.12094033522185,
0.139842280480747));
#19009=CARTESIAN_POINT('Ctrl Pts',(0.15983782968835,0.0246266142906177,
0.147781270118052));
#19010=CARTESIAN_POINT('Ctrl Pts',(0.0659863808909888,0.147649582370873,
0.155720259755358));
#19011=CARTESIAN_POINT('Ctrl Pts',(-0.0882710769349216,0.135509478890084,
0.163659249392663));
#19012=CARTESIAN_POINT('Ctrl Pts',(-0.161722413615419,-0.00068026650363694,
0.171598239029969));
#19013=CARTESIAN_POINT('Ctrl Pts',(-0.0871279640988751,-0.136247273976568,
0.179537228667275));
#19014=CARTESIAN_POINT('Ctrl Pts',(0.0672261652318651,-0.147089240053593,
0.187476218304581));
#19015=CARTESIAN_POINT('Ctrl Pts',(0.160039347628626,-0.023281087390596,
0.195415207941886));
#19016=CARTESIAN_POINT('Ctrl Pts',(0.106347475470598,0.121839305139765,
0.203354197579192));
#19017=CARTESIAN_POINT('Ctrl Pts',(-0.0446982220051161,0.15542416405057,
0.211293187216498));
#19018=CARTESIAN_POINT('Ctrl Pts',(-0.154825760608133,0.0467288526640558,
0.219232176853804));
#19019=CARTESIAN_POINT('Ctrl Pts',(-0.12322092627477,-0.104743520787053,
0.227171166491109));
#19020=CARTESIAN_POINT('Ctrl Pts',(0.0211842211805034,-0.160330379506191,
0.235110156128415));
#19021=CARTESIAN_POINT('Ctrl Pts',(0.146196665995071,-0.0691457639426259,
0.24304914576572));
#19022=CARTESIAN_POINT('Ctrl Pts',(0.137376082602736,0.0853370596399817,
0.250988135403027));
#19023=CARTESIAN_POINT('Ctrl Pts',(0.00279711058556459,0.161699653653757,
0.258927125040332));
#19024=CARTESIAN_POINT('Ctrl Pts',(-0.134342424474264,0.0900372967480426,
0.266866114677638));
#19025=CARTESIAN_POINT('Ctrl Pts',(-0.148500677015507,-0.0640480346713102,
0.274805104314944));
#19026=CARTESIAN_POINT('Ctrl Pts',(-0.0267167371651392,-0.159501779847699,
0.282744093952249));
#19027=CARTESIAN_POINT('Ctrl Pts',(0.119524544542348,-0.108942576944327,
0.290683083589556));
#19028=CARTESIAN_POINT('Ctrl Pts',(0.156349297273321,0.0413460888291301,
0.29862207322686));
#19029=CARTESIAN_POINT('Ctrl Pts',(0.0500469836677093,0.153785243912065,
0.306561062864167));
#19030=CARTESIAN_POINT('Ctrl Pts',(-0.102069913541897,0.125444547784578,
0.314500052501472));
#19031=CARTESIAN_POINT('Ctrl Pts',(-0.160748800211922,-0.0177320345633525,
0.322439042138778));
#19032=CARTESIAN_POINT('Ctrl Pts',(-0.0722731771226978,-0.144676154524232,
0.330378031776084));
#19033=CARTESIAN_POINT('Ctrl Pts',(0.082363586418043,-0.139179170322594,
0.338317021413389));
#19034=CARTESIAN_POINT('Ctrl Pts',(0.16160213133829,-0.00627319426210969,
0.346256011050695));
#19035=CARTESIAN_POINT('Ctrl Pts',(0.0929050003357002,0.132375461215256,
0.354195000688001));
#19036=CARTESIAN_POINT('Ctrl Pts',(-0.0608402912787218,0.149843454232904,
0.362133990325306));
#19037=CARTESIAN_POINT('Ctrl Pts',(-0.158890465884947,0.0301400343429239,
0.370072979962613));
#19038=CARTESIAN_POINT('Ctrl Pts',(-0.1114873084483,-0.117154521356547,
0.378011969599918));
#19039=CARTESIAN_POINT('Ctrl Pts',(0.0379748391485164,-0.157202141877815,
0.385950959237223));
#19040=CARTESIAN_POINT('Ctrl Pts',(0.152673624090564,-0.0533419752763387,
0.39388994887453));
#19041=CARTESIAN_POINT('Ctrl Pts',(0.127610169584502,0.0993491139263089,
0.401828938511835));
#19042=CARTESIAN_POINT('Ctrl Pts',(-0.014271649480085,0.16109289816887,
0.409767928149142));
#19043=CARTESIAN_POINT('Ctrl Pts',(-0.143088751545671,0.0753671745551693,
0.417706917786446));
#19044=CARTESIAN_POINT('Ctrl Pts',(-0.140917908083783,-0.0793520321139836,
0.425645907423752));
#19045=CARTESIAN_POINT('Ctrl Pts',(-0.00974637750615997,-0.161429891732714,
0.433584897061058));
#19046=CARTESIAN_POINT('Ctrl Pts',(0.130347293715478,-0.0957297489831606,
0.441523886698364));
#19047=CARTESIAN_POINT('Ctrl Pts',(0.15111695082405,0.0576044181723055,
0.449462876335669));
#19048=CARTESIAN_POINT('Ctrl Pts',(0.0335493961742207,0.158205688379633,
0.457401865972975));
#19049=CARTESIAN_POINT('Ctrl Pts',(-0.114730331382826,0.113980493419335,
0.465340855610281));
#19050=CARTESIAN_POINT('Ctrl Pts',(-0.157982303542021,-0.03458603167299,
0.473279845247587));
#19051=CARTESIAN_POINT('Ctrl Pts',(-0.0566123040428622,-0.151491415104245,
0.481218834884892));
#19052=CARTESIAN_POINT('Ctrl Pts',(0.0965823799129518,-0.129716790392294,
0.489157824522198));
#19053=CARTESIAN_POINT('Ctrl Pts',(0.161362514281243,0.0108046658515635,
0.497096814159504));
#19054=CARTESIAN_POINT('Ctrl Pts',(0.0784263257203939,0.141435191000425,
0.50503580379681));
#19055=CARTESIAN_POINT('Ctrl Pts',(-0.076303789130349,0.14259149197508,
0.512974793434115));
#19056=CARTESIAN_POINT('Ctrl Pts',(-0.161183014472451,0.0132150544797126,
0.520913783071421));
#19057=CARTESIAN_POINT('Ctrl Pts',(-0.0985102366584373,-0.128258859705,
0.528852772708727));
#19058=CARTESIAN_POINT('Ctrl Pts',(0.0543419114689404,-0.152320577983508,
0.536791762346032));
#19059=CARTESIAN_POINT('Ctrl Pts',(0.157447763940923,-0.0369432463290883,
0.544730751983338));
#19060=CARTESIAN_POINT('Ctrl Pts',(0.116420979124965,0.112253095453589,
0.552669741620643));
#19061=CARTESIAN_POINT('Ctrl Pts',(-0.0311812332291155,0.158689421555565,
0.56060873125795));
#19062=CARTESIAN_POINT('Ctrl Pts',(-0.150239163551416,0.0598564579197502,
0.568547720895255));
#19063=CARTESIAN_POINT('Ctrl Pts',(-0.131763436204723,-0.0937709907106254,
0.576486710532561));
#19064=CARTESIAN_POINT('Ctrl Pts',(0.00733268664935855,-0.161557523891122,
0.584425700169866));
#19065=CARTESIAN_POINT('Ctrl Pts',(0.139716237417787,-0.0814492162095161,
0.592364689807173));
#19066=CARTESIAN_POINT('Ctrl Pts',(0.144199148209332,0.0732202668325601,
0.600303679444478));
#19067=CARTESIAN_POINT('Ctrl Pts',(0.0166776214282734,0.160861613702037,
0.608242669081784));
#19068=CARTESIAN_POINT('Ctrl Pts',(-0.126111124778327,0.101245177793678,
0.616181658719089));
#19069=CARTESIAN_POINT('Ctrl Pts',(-0.153453779210204,-0.0510542795996006,
0.624120648356396));
#19070=CARTESIAN_POINT('Ctrl Pts',(-0.0403200156494649,-0.156617042997737,
0.6320596379937));
#19071=CARTESIAN_POINT('Ctrl Pts',(0.10972395892722,-0.118807637198397,
0.639998627631007));
#19072=CARTESIAN_POINT('Ctrl Pts',(0.159323168980049,0.0277620180369333,
0.647937617268312));
#19073=CARTESIAN_POINT('Ctrl Pts',(0.0630729369615192,0.148917448414806,
0.655876606905618));
#19074=CARTESIAN_POINT('Ctrl Pts',(-0.0909162461746061,0.133749160748195,
0.663815596542924));
#19075=CARTESIAN_POINT('Ctrl Pts',(-0.161677836835157,-0.00385731715476066,
0.671754586180229));
#19076=CARTESIAN_POINT('Ctrl Pts',(-0.0844344483789265,-0.137932685561743,
0.679693575817536));
#19077=CARTESIAN_POINT('Ctrl Pts',(0.0701028908975481,-0.145740133481257,
0.687632565454841));
#19078=CARTESIAN_POINT('Ctrl Pts',(0.1604658380222,-0.0201324774223393,
0.695571555092147));
#19079=CARTESIAN_POINT('Ctrl Pts',(0.10393330787963,0.123905081947942,0.703510544729453));
#19080=CARTESIAN_POINT('Ctrl Pts',(-0.0477430426119635,0.15451603056473,
0.711449534366758));
#19081=CARTESIAN_POINT('Ctrl Pts',(-0.155713909636705,0.0436781428746717,
0.719388524004064));
#19082=CARTESIAN_POINT('Ctrl Pts',(-0.121139364160222,-0.10714409115852,
0.72732751364137));
#19083=CARTESIAN_POINT('Ctrl Pts',(0.0243299669821161,-0.159883252800214,
0.735266503278675));
#19084=CARTESIAN_POINT('Ctrl Pts',(0.147526880793862,-0.0662602540182413,
0.743205492915981));
#19085=CARTESIAN_POINT('Ctrl Pts',(0.135673045916277,0.0880194662056535,
0.751144482553287));
#19086=CARTESIAN_POINT('Ctrl Pts',(-0.000380164216571841,0.161723397486253,
0.759083472190592));
#19087=CARTESIAN_POINT('Ctrl Pts',(-0.136085360063504,0.0873806419964673,
0.767022461827899));
#19088=CARTESIAN_POINT('Ctrl Pts',(-0.147213735311121,-0.0669531026545853,
0.774961451465203));
#19089=CARTESIAN_POINT('Ctrl Pts',(-0.023578025097595,-0.159995870421162,
0.78290044110251));
#19090=CARTESIAN_POINT('Ctrl Pts',(0.121641751185188,-0.106573384050283,
0.790839430739816));
#19091=CARTESIAN_POINT('Ctrl Pts',(0.155506840911589,0.0444097314676148,
0.798778420377121));
#19092=CARTESIAN_POINT('Ctrl Pts',(0.047016075363265,0.15473878142458,0.806717410014428));
#19093=CARTESIAN_POINT('Ctrl Pts',(-0.104514684958047,0.123415081928621,
0.814656399651731));
#19094=CARTESIAN_POINT('Ctrl Pts',(-0.16036941405942,-0.020886666885039,
0.82259538928904));
#19095=CARTESIAN_POINT('Ctrl Pts',(-0.0694169354231278,-0.146068103622213,
0.830534378926343));
#19096=CARTESIAN_POINT('Ctrl Pts',(0.085081990139753,-0.137534202194171,
0.838473368563651));
#19097=CARTESIAN_POINT('Ctrl Pts',(0.161694184779289,-0.00309716449182502,
0.846412358200955));
#19098=CARTESIAN_POINT('Ctrl Pts',(0.0902864348795877,0.134175115040242,
0.854351347838261));
#19099=CARTESIAN_POINT('Ctrl Pts',(-0.0637723584188847,0.148619272374149,
0.862290337475567));
#19100=CARTESIAN_POINT('Ctrl Pts',(-0.159451928190027,0.0270126713934565,
0.870229327112872));
#19101=CARTESIAN_POINT('Ctrl Pts',(-0.109164185657521,-0.119322178948671,
0.878168316750179));
#19102=CARTESIAN_POINT('Ctrl Pts',(0.0410558873341998,-0.156425752146281,
0.886107306387484));
#19103=CARTESIAN_POINT('Ctrl Pts',(0.153692109215179,-0.0503322698109037,
0.894046296024789));
#19104=CARTESIAN_POINT('Ctrl Pts',(0.125633738317809,0.101836956040625,
0.901985285662096));
#19105=CARTESIAN_POINT('Ctrl Pts',(-0.0174337097671096,0.160781427979367,
0.909924275299401));
#19106=CARTESIAN_POINT('Ctrl Pts',(-0.144541791370401,0.072541521673891,
0.917863264936708));
#19107=CARTESIAN_POINT('Ctrl Pts',(-0.13933176907,-0.082105176128868,0.925802254574012));
#19108=CARTESIAN_POINT('Ctrl Pts',(-0.00657306121577474,-0.161590212220858,
0.933741244211319));
#19109=CARTESIAN_POINT('Ctrl Pts',(0.132202833700187,-0.0931504835251481,
0.941680233848624));
#19110=CARTESIAN_POINT('Ctrl Pts',(0.149956094815541,0.0605621288182698,
0.949619223485929));
#19111=CARTESIAN_POINT('Ctrl Pts',(0.0304348282896272,0.158834262822317,
0.957558213123236));
#19112=CARTESIAN_POINT('Ctrl Pts',(-0.116947437700435,0.111704514835484,
0.965497202760542));
#19113=CARTESIAN_POINT('Ctrl Pts',(-0.157272339407096,-0.0376830608728604,
0.973436192397847));
#19114=CARTESIAN_POINT('Ctrl Pts',(-0.0536251929639052,-0.152574376940928,
0.981375182035153));
#19115=CARTESIAN_POINT('Ctrl Pts',(0.0991121424632477,-0.127794307524525,
0.989314171672459));
#19116=CARTESIAN_POINT('Ctrl Pts',(0.161119104064031,0.0139726921146952,
0.997253161309763));
#19117=CARTESIAN_POINT('Ctrl Pts',(0.0756325681075411,0.142948649734045,
1.00519215094707));
#19118=CARTESIAN_POINT('Ctrl Pts',(-0.0790904005129918,0.141064915432658,
1.01313114058437));
#19119=CARTESIAN_POINT('Ctrl Pts',(-0.161411527883023,0.0100459188627121,
1.02107013022168));
#19120=CARTESIAN_POINT('Ctrl Pts',(-0.095971463730607,-0.130169427934261,
1.02900911985899));
#19121=CARTESIAN_POINT('Ctrl Pts',(0.0573238981132153,-0.151223584550935,
1.03694810949629));
#19122=CARTESIAN_POINT('Ctrl Pts',(0.158143159897702,-0.0338429135403315,
1.0448870991336));
#19123=CARTESIAN_POINT('Ctrl Pts',(0.114193197054413,0.114518625410106,
1.0528260887709));
#19124=CARTESIAN_POINT('Ctrl Pts',(-0.0342928115212847,0.158046211271557,
1.06076507840821));
#19125=CARTESIAN_POINT('Ctrl Pts',(-0.151386101389109,0.0568933223281485,
1.06870406804552));
#19126=CARTESIAN_POINT('Ctrl Pts',(-0.129895790602315,-0.0963415040526547,
1.07664305768282));
#19127=CARTESIAN_POINT('Ctrl Pts',(0.0105052141409744,-0.161382286187737,
1.08458204732013));
#19128=CARTESIAN_POINT('Ctrl Pts',(0.141289415307547,-0.0786886455683398,
1.09252103695743));
#19129=CARTESIAN_POINT('Ctrl Pts',(0.14273283995608,0.076039057183793,1.10046002659474));
#19130=CARTESIAN_POINT('Ctrl Pts',(0.013514131745196,0.161158214381091,
1.10839901623204));
#19131=CARTESIAN_POINT('Ctrl Pts',(-0.128075837894479,0.0987480712062529,
1.11633800586935));
#19132=CARTESIAN_POINT('Ctrl Pts',(-0.152421155552179,-0.0540591635106084,
1.12427699550666));
#19133=CARTESIAN_POINT('Ctrl Pts',(-0.0372353514058616,-0.157378938949945,
1.13221598514396));
#19134=CARTESIAN_POINT('Ctrl Pts',(0.11203686504723,-0.116629081663695,
1.14015497478127));
#19135=CARTESIAN_POINT('Ctrl Pts',(0.158747009937404,0.0308867067726846,
1.14809396441857));
#19136=CARTESIAN_POINT('Ctrl Pts',(0.0601351468730053,0.150127831962932,
1.15603295405588));
#19137=CARTESIAN_POINT('Ctrl Pts',(-0.0935263218228598,0.13193721592339,
1.16397194369318));
#19138=CARTESIAN_POINT('Ctrl Pts',(-0.161570852667341,-0.00703287904607843,
1.17191093333049));
#19139=CARTESIAN_POINT('Ctrl Pts',(-0.0817083410685703,-0.13956485524354,
1.17984992296779));
#19140=CARTESIAN_POINT('Ctrl Pts',(0.0729525569401478,-0.144334771469742,
1.1877889126051));
#19141=CARTESIAN_POINT('Ctrl Pts',(0.160830388835411,-0.016976096323307,
1.19572790224241));
#19142=CARTESIAN_POINT('Ctrl Pts',(0.101479022178261,0.125923031559255,
1.20366689187971));
#19143=CARTESIAN_POINT('Ctrl Pts',(-0.0507694344715009,0.153548254118279,
1.21160588151702));
#19144=CARTESIAN_POINT('Ctrl Pts',(-0.15654195331917,0.0406105733811438,
1.21954487115432));
#19145=CARTESIAN_POINT('Ctrl Pts',(-0.119011042423884,-0.109503304062093,
1.22748386079163));
#19146=CARTESIAN_POINT('Ctrl Pts',(0.0274663214511058,-0.159374411387982,
1.23542285042894));
#19147=CARTESIAN_POINT('Ctrl Pts',(0.148800150427453,-0.0633491677300162,
1.24336184006624));
#19148=CARTESIAN_POINT('Ctrl Pts',(0.133917639627974,0.0906678973829495,
1.25130082970354));
#19149=CARTESIAN_POINT('Ctrl Pts',(-0.00355729227603857,0.161684716318317,
1.25923981934086));
#19150=CARTESIAN_POINT('Ctrl Pts',(-0.137775766897813,0.0846902584421788,
1.26717880897816));
#19151=CARTESIAN_POINT('Ctrl Pts',(-0.14586996931591,-0.0698323268364953,
1.27511779861547));
#19152=CARTESIAN_POINT('Ctrl Pts',(-0.0204302119447119,-0.160428202816007,
1.28305678825277));
#19153=CARTESIAN_POINT('Ctrl Pts',(0.123712004283314,-0.104163053984564,
1.29099577789008));
#19154=CARTESIAN_POINT('Ctrl Pts',(0.15460435913624,0.0474562320176185,
1.29893476752738));
#19155=CARTESIAN_POINT('Ctrl Pts',(0.043967018911749,0.155632589980133,
1.30687375716469));
#19156=CARTESIAN_POINT('Ctrl Pts',(-0.106919113837756,0.121337978043289,
1.31481274680199));
#19157=CARTESIAN_POINT('Ctrl Pts',(-0.159928125575155,-0.0240332370134145,
1.3227517364393));
#19158=CARTESIAN_POINT('Ctrl Pts',(-0.0665338988230771,-0.147403670583407,
1.33069072607661));
#19159=CARTESIAN_POINT('Ctrl Pts',(0.0877675522160205,-0.135836146169277,
1.33862971571391));
#19160=CARTESIAN_POINT('Ctrl Pts',(0.161723824721502,8.00609866524728E-5,
1.34656870535122));
#19161=CARTESIAN_POINT('Ctrl Pts',(0.0876330185603928,0.135922977069285,
1.35450769498852));
#19162=CARTESIAN_POINT('Ctrl Pts',(-0.0666798087068602,0.147337724435113,
1.36244668462583));
#19163=CARTESIAN_POINT('Ctrl Pts',(-0.159951843822013,0.0238748801740983,
1.37038567426313));
#19164=CARTESIAN_POINT('Ctrl Pts',(-0.106798922716859,-0.121443775659372,
1.37832466390044));
#19165=CARTESIAN_POINT('Ctrl Pts',(0.0441210824430389,-0.155588987406456,
1.38626365353774));
#19166=CARTESIAN_POINT('Ctrl Pts',(0.154651279966657,-0.0473031264624986,
1.39420264317505));
#19167=CARTESIAN_POINT('Ctrl Pts',(0.123608792556459,0.10428547082216,1.40214163281236));
#19168=CARTESIAN_POINT('Ctrl Pts',(-0.020589002599541,0.160407931346284,
1.41008062244966));
#19169=CARTESIAN_POINT('Ctrl Pts',(-0.145939110542184,0.0696878015005003,
1.41801961208697));
#19170=CARTESIAN_POINT('Ctrl Pts',(-0.137691710982408,-0.0848265016612731,
1.42595860172427));
#19171=CARTESIAN_POINT('Ctrl Pts',(-0.00339746822928561,-0.161688398335044,
1.43389759136158));
#19172=CARTESIAN_POINT('Ctrl Pts',(0.134007838137522,-0.0905348079547059,
1.44183658099889));
#19173=CARTESIAN_POINT('Ctrl Pts',(0.148736417039967,0.0634956003383226,
1.44977557063619));
#19174=CARTESIAN_POINT('Ctrl Pts',(0.0273102951854726,0.159403164432859,
1.4577145602735));
#19175=CARTESIAN_POINT('Ctrl Pts',(-0.119122786779006,0.109382310628272,
1.4656535499108));
#19176=CARTESIAN_POINT('Ctrl Pts',(-0.156495242883694,-0.0407596439572756,
1.47359253954811));
#19177=CARTESIAN_POINT('Ctrl Pts',(-0.0506295842364637,-0.153609649276743,
1.48153152918541));
#19178=CARTESIAN_POINT('Ctrl Pts',(0.10162683549218,-0.125801210382132,
1.48947051882272));
#19179=CARTESIAN_POINT('Ctrl Pts',(0.160769288057966,0.017094787472962,
1.49740950846002));
#19180=CARTESIAN_POINT('Ctrl Pts',(0.0728951834924312,0.144484958595688,
1.50534849809733));
#19181=CARTESIAN_POINT('Ctrl Pts',(-0.0820226078184241,0.139326700971572,
1.51328748773464));
#19182=CARTESIAN_POINT('Ctrl Pts',(-0.134767702434085,0.0512744806661359,
1.51858014749284));
#19183=CARTESIAN_POINT('Ctrl Pts',(-0.136701386950156,0.00581475974600206,
1.52122647737194));
#19184=CARTESIAN_POINT('Ctrl Pts',(0.0740036351041134,-0.103579689087085,
-0.0054992613140312));
#19185=CARTESIAN_POINT('Ctrl Pts',(0.108448814220036,-0.0789699563406641,
-0.00285293143492929));
#19186=CARTESIAN_POINT('Ctrl Pts',(0.150264871169078,0.00688399744800666,
0.00243972832327453));
#19187=CARTESIAN_POINT('Ctrl Pts',(0.0755551489391376,0.130236700260234,
0.0103787179605803));
#19188=CARTESIAN_POINT('Ctrl Pts',(-0.0683810376584167,0.133979098529349,
0.0183177075978859));
#19189=CARTESIAN_POINT('Ctrl Pts',(-0.14968704878538,0.0152677557027674,
0.0262566972351917));
#19190=CARTESIAN_POINT('Ctrl Pts',(-0.0939816891590436,-0.11752176362514,
0.0341956868724974));
#19191=CARTESIAN_POINT('Ctrl Pts',(0.0477663481097245,-0.142674779628989,
0.0421346765098031));
#19192=CARTESIAN_POINT('Ctrl Pts',(0.14578288888032,-0.0372469160898187,
0.0500736661471088));
#19193=CARTESIAN_POINT('Ctrl Pts',(0.110347650287512,0.102292747252513,
0.0580126557844146));
#19194=CARTESIAN_POINT('Ctrl Pts',(-0.0261045975097209,0.148182615303324,
0.0659516454217203));
#19195=CARTESIAN_POINT('Ctrl Pts',(-0.13865919166998,0.0584255608647477,
0.073890635059026));
#19196=CARTESIAN_POINT('Ctrl Pts',(-0.124281158904105,-0.0848182532198701,
0.0818296246963318));
#19197=CARTESIAN_POINT('Ctrl Pts',(0.00386794697500161,-0.15041563023346,
0.0897686143336374));
#19198=CARTESIAN_POINT('Ctrl Pts',(0.128476112576568,-0.0783184064825255,
0.0977076039709433));
#19199=CARTESIAN_POINT('Ctrl Pts',(0.135473254782295,0.0654742669580799,
0.105646593608249));
#19200=CARTESIAN_POINT('Ctrl Pts',(0.0184538891044151,0.149329569763132,
0.113585583245555));
#19201=CARTESIAN_POINT('Ctrl Pts',(-0.115458732720671,0.096483973363118,
0.12152457288286));
#19202=CARTESIAN_POINT('Ctrl Pts',(-0.143676805334049,-0.0446861343604874,
0.129463562520166));
#19203=CARTESIAN_POINT('Ctrl Pts',(-0.0403686054279526,-0.144949124289353,
0.137402552157472));
#19204=CARTESIAN_POINT('Ctrl Pts',(0.0998942839726139,-0.112521137758025,
0.145341541794778));
#19205=CARTESIAN_POINT('Ctrl Pts',(0.14871080372247,0.0229122455632766,
0.153280531432083));
#19206=CARTESIAN_POINT('Ctrl Pts',(0.0613927738894439,0.137371034794898,
0.161219521069389));
#19207=CARTESIAN_POINT('Ctrl Pts',(-0.0821261326059948,0.126076058196294,
0.169158510706695));
#19208=CARTESIAN_POINT('Ctrl Pts',(-0.150464193336327,-0.000632910110818063,
0.177097500344));
#19209=CARTESIAN_POINT('Ctrl Pts',(-0.0810625969653723,-0.126762492068094,
0.185036489981306));
#19210=CARTESIAN_POINT('Ctrl Pts',(0.0625462512992226,-0.136849700411639,
0.192975479618612));
#19211=CARTESIAN_POINT('Ctrl Pts',(0.148898293097928,-0.0216603868066741,
0.200914469255917));
#19212=CARTESIAN_POINT('Ctrl Pts',(0.0989441522193119,0.113357526360621,
0.208853458893223));
#19213=CARTESIAN_POINT('Ctrl Pts',(-0.0415865789238149,0.144604393083411,
0.216792448530529));
#19214=CARTESIAN_POINT('Ctrl Pts',(-0.144047647180085,0.0434758483035601,
0.224731438167835));
#19215=CARTESIAN_POINT('Ctrl Pts',(-0.114642966671137,-0.0974518559926297,
0.232670427805141));
#19216=CARTESIAN_POINT('Ctrl Pts',(0.0197094928286333,-0.149169064945282,
0.240609417442446));
#19217=CARTESIAN_POINT('Ctrl Pts',(0.136019262424063,-0.0643322181611298,
0.248548407079752));
#19218=CARTESIAN_POINT('Ctrl Pts',(0.127812719278849,0.0793963653730636,
0.256487396717058));
#19219=CARTESIAN_POINT('Ctrl Pts',(0.00260239121171357,0.150443017797356,
0.264426386354363));
#19220=CARTESIAN_POINT('Ctrl Pts',(-0.124990247656303,0.0837693979610897,
0.272365375991669));
#19221=CARTESIAN_POINT('Ctrl Pts',(-0.138162880936044,-0.0595893646165358,
0.280304365628975));
#19222=CARTESIAN_POINT('Ctrl Pts',(-0.0248568656394851,-0.148398147813718,
0.288243355266281));
#19223=CARTESIAN_POINT('Ctrl Pts',(0.111203906597776,-0.101358597076653,
0.296182344903586));
#19224=CARTESIAN_POINT('Ctrl Pts',(0.145465123646218,0.0384678027257296,
0.304121334540892));
#19225=CARTESIAN_POINT('Ctrl Pts',(0.0465629893725541,0.143079565503422,
0.312060324178198));
#19226=CARTESIAN_POINT('Ctrl Pts',(-0.0949643705016135,0.116711791945748,
0.319999313815503));
#19227=CARTESIAN_POINT('Ctrl Pts',(-0.149558357514911,-0.0164976283567656,
0.327938303452809));
#19228=CARTESIAN_POINT('Ctrl Pts',(-0.0672419181269484,-0.134604600554976,
0.335877293090115));
#19229=CARTESIAN_POINT('Ctrl Pts',(0.0766298889166206,-0.12949028600085,
0.343816282727421));
#19230=CARTESIAN_POINT('Ctrl Pts',(0.150352284446295,-0.00583648916182633,
0.351755272364726));
#19231=CARTESIAN_POINT('Ctrl Pts',(0.0864374678803939,0.123160213504125,
0.359694262002032));
#19232=CARTESIAN_POINT('Ctrl Pts',(-0.0566049265834532,0.139412181427728,
0.367633251639338));
#19233=CARTESIAN_POINT('Ctrl Pts',(-0.147829390149123,0.0280418517950267,
0.375572241276644));
#19234=CARTESIAN_POINT('Ctrl Pts',(-0.103726178443039,-0.108998871322406,
0.383511230913949));
#19235=CARTESIAN_POINT('Ctrl Pts',(0.0353312408083745,-0.146258597924691,
0.391450220551255));
#19236=CARTESIAN_POINT('Ctrl Pts',(0.142045330507792,-0.0496286018832686,
0.399389210188561));
#19237=CARTESIAN_POINT('Ctrl Pts',(0.118726655129599,0.0924329779120693,
0.407328199825866));
#19238=CARTESIAN_POINT('Ctrl Pts',(-0.0132781361506635,0.1498785012746,
0.415267189463172));
#19239=CARTESIAN_POINT('Ctrl Pts',(-0.133127703795094,0.0701205285647604,
0.423206179100478));
#19240=CARTESIAN_POINT('Ctrl Pts',(-0.131107982452518,-0.0738279823724454,
0.431145168737783));
#19241=CARTESIAN_POINT('Ctrl Pts',(-0.00906788859151817,-0.150192035209753,
0.439084158375089));
#19242=CARTESIAN_POINT('Ctrl Pts',(0.121273235812024,-0.0890655731449414,
0.447023148012395));
#19243=CARTESIAN_POINT('Ctrl Pts',(0.14059702422731,0.0535943170716914,
0.4549621376497));
#19244=CARTESIAN_POINT('Ctrl Pts',(0.031213872705855,0.14719228306762,0.462901127287006));
#19245=CARTESIAN_POINT('Ctrl Pts',(-0.106743440051405,0.106045801661112,
0.470840116924312));
#19246=CARTESIAN_POINT('Ctrl Pts',(-0.146984449047318,-0.0321783433727119,
0.478779106561618));
#19247=CARTESIAN_POINT('Ctrl Pts',(-0.0526712684425847,-0.140945420374714,
0.486718096198923));
#19248=CARTESIAN_POINT('Ctrl Pts',(0.0898588486235595,-0.120686624644175,
0.49465708583623));
#19249=CARTESIAN_POINT('Ctrl Pts',(0.150129348203927,0.0100525047535443,
0.502596075473534));
#19250=CARTESIAN_POINT('Ctrl Pts',(0.0729667185397875,0.131589254992538,
0.510535065110842));
#19251=CARTESIAN_POINT('Ctrl Pts',(-0.0709919412117167,0.132665060686482,
0.518474054748145));
#19252=CARTESIAN_POINT('Ctrl Pts',(-0.149962344179375,0.0122950954523496,
0.526413044385453));
#19253=CARTESIAN_POINT('Ctrl Pts',(-0.0916524986414713,-0.119330187030486,
0.534352034022757));
#19254=CARTESIAN_POINT('Ctrl Pts',(0.0505589280467443,-0.141716861518734,
0.542291023660064));
#19255=CARTESIAN_POINT('Ctrl Pts',(0.146487121137799,-0.0343714617774037,
0.550230013297369));
#19256=CARTESIAN_POINT('Ctrl Pts',(0.108316394245265,0.104438655591022,
0.558169002934674));
#19257=CARTESIAN_POINT('Ctrl Pts',(-0.0290105681715044,0.147642341414387,
0.566107992571982));
#19258=CARTESIAN_POINT('Ctrl Pts',(-0.139780343651344,0.0556895822633619,
0.574046982209285));
#19259=CARTESIAN_POINT('Ctrl Pts',(-0.122590794290966,-0.0872431727934394,
0.581985971846593));
#19260=CARTESIAN_POINT('Ctrl Pts',(0.00682222554696161,-0.150310782322966,
0.589924961483898));
#19261=CARTESIAN_POINT('Ctrl Pts',(0.129989965454297,-0.0757791721064987,
0.597863951121203));
#19262=CARTESIAN_POINT('Ctrl Pts',(0.134160800782372,0.0681230766876274,
0.60580294075851));
#19263=CARTESIAN_POINT('Ctrl Pts',(0.015516617634347,0.149663317553585,
0.613741930395814));
#19264=CARTESIAN_POINT('Ctrl Pts',(-0.117331965534667,0.0941970482962578,
0.621680920033121));
#19265=CARTESIAN_POINT('Ctrl Pts',(-0.142771175541451,-0.0475001629309618,
0.629619909670426));
#19266=CARTESIAN_POINT('Ctrl Pts',(-0.0375131590877193,-0.145714230393655,
0.637558899307733));
#19267=CARTESIAN_POINT('Ctrl Pts',(0.102085583566124,-0.110536906379362,
0.645497888945037));
#19268=CARTESIAN_POINT('Ctrl Pts',(0.148231970847143,0.0258293798362968,
0.653436878582344));
#19269=CARTESIAN_POINT('Ctrl Pts',(0.0586821478180281,0.138550639014834,
0.661375868219649));
#19270=CARTESIAN_POINT('Ctrl Pts',(-0.0845871597882484,0.124438283670714,
0.669314857856955));
#19271=CARTESIAN_POINT('Ctrl Pts',(-0.150422719745043,-0.00358879206139753,
0.67725384749426));
#19272=CARTESIAN_POINT('Ctrl Pts',(-0.078556588917505,-0.128330574617282,
0.685192837131567));
#19273=CARTESIAN_POINT('Ctrl Pts',(0.065222715229363,-0.135594511179713,
0.693131826768872));
#19274=CARTESIAN_POINT('Ctrl Pts',(0.149295093588351,-0.0187309656558678,
0.701070816406178));
#19275=CARTESIAN_POINT('Ctrl Pts',(0.0966980456281902,0.11527949520901,
0.709009806043483));
#19276=CARTESIAN_POINT('Ctrl Pts',(-0.044419435954706,0.14375947882982,
0.716948795680789));
#19277=CARTESIAN_POINT('Ctrl Pts',(-0.144873968183829,0.0406375120624596,
0.724887785318095));
#19278=CARTESIAN_POINT('Ctrl Pts',(-0.112706311402131,-0.099685311927494,
0.732826774955401));
#19279=CARTESIAN_POINT('Ctrl Pts',(0.0226362492002416,-0.148753064728429,
0.740765764592706));
#19280=CARTESIAN_POINT('Ctrl Pts',(0.137256875023267,-0.0616475814838108,
0.748704754230013));
#19281=CARTESIAN_POINT('Ctrl Pts',(0.126228238590478,0.0818920376245527,
0.756643743867318));
#19282=CARTESIAN_POINT('Ctrl Pts',(-0.000353699285724532,0.150465108715513,
0.764582733504624));
#19283=CARTESIAN_POINT('Ctrl Pts',(-0.126611849706441,0.0812976848247803,
0.772521723141928));
#19284=CARTESIAN_POINT('Ctrl Pts',(-0.136965528997667,-0.0622921978288208,
0.780460712779236));
#19285=CARTESIAN_POINT('Ctrl Pts',(-0.0219366533522686,-0.148857842533265,
0.788399702416541));
#19286=CARTESIAN_POINT('Ctrl Pts',(0.113173725020093,-0.0991543342927188,
0.796338692053846));
#19287=CARTESIAN_POINT('Ctrl Pts',(0.144681314438483,0.0413181715024817,
0.804277681691154));
#19288=CARTESIAN_POINT('Ctrl Pts',(0.0437430761464933,0.143966723006387,
0.812216671328456));
#19289=CARTESIAN_POINT('Ctrl Pts',(-0.0972389504488157,0.114823606281847,
0.820155660965765));
#19290=CARTESIAN_POINT('Ctrl Pts',(-0.149205382128735,-0.0194326526180533,
0.828094650603069));
#19291=CARTESIAN_POINT('Ctrl Pts',(-0.0645845121824554,-0.135899649852787,
0.836033640240376));
#19292=CARTESIAN_POINT('Ctrl Pts',(0.0791590524011713,-0.127959831458565,
0.843972629877681));
#19293=CARTESIAN_POINT('Ctrl Pts',(0.150437929635691,-0.00288155702400619,
0.851911619514986));
#19294=CARTESIAN_POINT('Ctrl Pts',(0.0840011924733913,0.12483458538003,
0.859850609152293));
#19295=CARTESIAN_POINT('Ctrl Pts',(-0.0593328794206009,0.138273220341526,
0.867789598789597));
#19296=CARTESIAN_POINT('Ctrl Pts',(-0.148351766552825,0.0251321985630355,
0.875728588426904));
#19297=CARTESIAN_POINT('Ctrl Pts',(-0.1015647786165,-0.111015628577859,
0.883667578064211));
#19298=CARTESIAN_POINT('Ctrl Pts',(0.0381978034543637,-0.145536256153639,
0.891606567701514));
#19299=CARTESIAN_POINT('Ctrl Pts',(0.142992914329196,-0.046828415471795,
0.899545557338823));
#19300=CARTESIAN_POINT('Ctrl Pts',(0.116887812080083,0.0947476302135675,
0.907484546976125));
#19301=CARTESIAN_POINT('Ctrl Pts',(-0.0162200712834111,0.149588713917584,
0.915423536613434));
#19302=CARTESIAN_POINT('Ctrl Pts',(-0.134479591021026,0.067491582014154,
0.923362526250738));
#19303=CARTESIAN_POINT('Ctrl Pts',(-0.129632261667175,-0.0763894677230377,
0.931301515888044));
#19304=CARTESIAN_POINT('Ctrl Pts',(-0.00611548103612966,-0.150341195071919,
0.93924050552535));
#19305=CARTESIAN_POINT('Ctrl Pts',(0.122999603362204,-0.0866658618874593,
0.947179495162656));
#19306=CARTESIAN_POINT('Ctrl Pts',(0.139516980595786,0.0563461282555487,
0.95511848479996));
#19307=CARTESIAN_POINT('Ctrl Pts',(0.0283161238170646,0.147777099632969,
0.963057474437267));
#19308=CARTESIAN_POINT('Ctrl Pts',(-0.108806203685475,0.103928264122473,
0.970996464074573));
#19309=CARTESIAN_POINT('Ctrl Pts',(-0.146323908690103,-0.0350597745230392,
0.978935453711877));
#19310=CARTESIAN_POINT('Ctrl Pts',(-0.049892103521326,-0.14195299239598,
0.986874443349185));
#19311=CARTESIAN_POINT('Ctrl Pts',(0.0922125030920605,-0.118897974404329,
0.994813432986488));
#19312=CARTESIAN_POINT('Ctrl Pts',(0.149902882860231,0.0129999905441286,
1.0027524226238));
#19313=CARTESIAN_POINT('Ctrl Pts',(0.0703674468853664,0.132997355096976,
1.0106914122611));
#19314=CARTESIAN_POINT('Ctrl Pts',(-0.0735845641169637,0.131244755962562,
1.01863040189841));
#19315=CARTESIAN_POINT('Ctrl Pts',(-0.150174949749745,0.00934657753497952,
1.02656939153571));
#19316=CARTESIAN_POINT('Ctrl Pts',(-0.0892904610481016,-0.121107752063083,
1.03450838117302));
#19317=CARTESIAN_POINT('Ctrl Pts',(0.0533333252681307,-0.140696234703703,
1.04244737081032));
#19318=CARTESIAN_POINT('Ctrl Pts',(0.147134107472884,-0.031486957015783,
1.05038636044763));
#19319=CARTESIAN_POINT('Ctrl Pts',(0.106243698045146,0.106546471877992,
1.05832535008494));
#19320=CARTESIAN_POINT('Ctrl Pts',(-0.0319055355867657,0.147043907874068,
1.06626433972224));
#19321=CARTESIAN_POINT('Ctrl Pts',(-0.14084743801815,0.0529327237885883,
1.07420332935955));
#19322=CARTESIAN_POINT('Ctrl Pts',(-0.120853163849259,-0.0896347412088629,
1.08214231899685));
#19323=CARTESIAN_POINT('Ctrl Pts',(0.00977389921538986,-0.150147743699608,
1.09008130863416));
#19324=CARTESIAN_POINT('Ctrl Pts',(0.13145362739741,-0.0732107771302755,
1.09802029827146));
#19325=CARTESIAN_POINT('Ctrl Pts',(0.132796568802552,0.0707456384395876,
1.10595928790877));
#19326=CARTESIAN_POINT('Ctrl Pts',(0.0125733526121963,0.149939270533256,
1.11389827754607));
#19327=CARTESIAN_POINT('Ctrl Pts',(-0.119159906186493,0.0918737764630459,
1.12183726718338));
#19328=CARTESIAN_POINT('Ctrl Pts',(-0.141810437433163,-0.0502958634379693,
1.12977625682069));
#19329=CARTESIAN_POINT('Ctrl Pts',(-0.0346432321137694,-0.146423087362162,
1.13771524645799));
#19330=CARTESIAN_POINT('Ctrl Pts',(0.104237477950025,-0.108510009835838,
1.1456542360953));
#19331=CARTESIAN_POINT('Ctrl Pts',(0.147695920811486,0.0287365450185451,
1.1535932257326));
#19332=CARTESIAN_POINT('Ctrl Pts',(0.0559488704325515,0.139676762352502,
1.16153221536991));
#19333=CARTESIAN_POINT('Ctrl Pts',(-0.0870155364008756,0.12275247642644,
1.16947120500722));
#19334=CARTESIAN_POINT('Ctrl Pts',(-0.150323183223479,-0.00654328889139735,
1.17741019464452));
#19335=CARTESIAN_POINT('Ctrl Pts',(-0.0760202581255566,-0.129849121670035,
1.18534918428183));
#19336=CARTESIAN_POINT('Ctrl Pts',(0.0678740032777675,-0.134286982701248,
1.19328817391913));
#19337=CARTESIAN_POINT('Ctrl Pts',(0.149634266389533,-0.0157943143574443,
1.20122716355644));
#19338=CARTESIAN_POINT('Ctrl Pts',(0.0944146137277022,0.117156966325547,
1.20916615319374));
#19339=CARTESIAN_POINT('Ctrl Pts',(-0.047235147145783,0.142859073628774,
1.21710514283105));
#19340=CARTESIAN_POINT('Ctrl Pts',(-0.145644368043342,0.037783489796601,
1.22504413246835));
#19341=CARTESIAN_POINT('Ctrl Pts',(-0.11072615165767,-0.101880289472715,
1.23298312210566));
#19342=CARTESIAN_POINT('Ctrl Pts',(0.0255542680118797,-0.148279646041953,
1.24092211174296));
#19343=CARTESIAN_POINT('Ctrl Pts',(0.138441506664824,-0.0589391489276913,
1.24886110138027));
#19344=CARTESIAN_POINT('Ctrl Pts',(0.124595033982396,0.0843560996663564,
1.25680009101758));
#19345=CARTESIAN_POINT('Ctrl Pts',(-0.00330965325590636,0.150429120316621,
1.26473908065488));
#19346=CARTESIAN_POINT('Ctrl Pts',(-0.128184579763139,0.0787945908985174,
1.27267807029219));
#19347=CARTESIAN_POINT('Ctrl Pts',(-0.135715308561414,-0.0649709863423027,
1.2806170599295));
#19348=CARTESIAN_POINT('Ctrl Pts',(-0.0190079735469551,-0.149260078337129,
1.2885560495668));
#19349=CARTESIAN_POINT('Ctrl Pts',(0.115099858543875,-0.0969117980795561,
1.29649503920411));
#19350=CARTESIAN_POINT('Ctrl Pts',(0.143841658454547,0.0441525915281748,
1.30443402884141));
#19351=CARTESIAN_POINT('Ctrl Pts',(0.0409062781470196,0.144798309552134,
1.31237301847872));
#19352=CARTESIAN_POINT('Ctrl Pts',(-0.0994759962839106,0.112891098884786,
1.32031200811602));
#19353=CARTESIAN_POINT('Ctrl Pts',(-0.148794813708878,-0.0223601759313527,
1.32825099775333));
#19354=CARTESIAN_POINT('Ctrl Pts',(-0.0619021766503053,-0.13714224202644,
1.33618998739064));
#19355=CARTESIAN_POINT('Ctrl Pts',(0.0816576604940555,-0.126379984705639,
1.34412897702794));
#19356=CARTESIAN_POINT('Ctrl Pts',(0.150465506209006,7.4487583413377E-5,
1.35206796666525));
#19357=CARTESIAN_POINT('Ctrl Pts',(0.0815324923277053,0.126460770918471,
1.36000695630255));
#19358=CARTESIAN_POINT('Ctrl Pts',(-0.062037929094705,0.137080886684378,
1.36794594593986));
#19359=CARTESIAN_POINT('Ctrl Pts',(-0.148816880822527,0.0222128430196456,
1.37588493557716));
#19360=CARTESIAN_POINT('Ctrl Pts',(-0.0993641722043223,-0.112989531455785,
1.38382392521447));
#19361=CARTESIAN_POINT('Ctrl Pts',(0.0410496166270677,-0.144757742348562,
1.39176291485178));
#19362=CARTESIAN_POINT('Ctrl Pts',(0.143885312916173,-0.0440101443352923,
1.39970190448908));
#19363=CARTESIAN_POINT('Ctrl Pts',(0.115003831846793,0.0970256929337524,
1.40764089412639));
#19364=CARTESIAN_POINT('Ctrl Pts',(-0.0191557100743377,0.149241218055048,
1.41557988376369));
#19365=CARTESIAN_POINT('Ctrl Pts',(-0.135779636557791,0.0648365220611291,
1.423518873401));
#19366=CARTESIAN_POINT('Ctrl Pts',(-0.128106375355825,-0.0789213496179777,
1.4314578630383));
#19367=CARTESIAN_POINT('Ctrl Pts',(-0.00316095527563228,-0.150432546011701,
1.43939685267561));
#19368=CARTESIAN_POINT('Ctrl Pts',(0.12467895337041,-0.0842322751882648,
1.44733584231291));
#19369=CARTESIAN_POINT('Ctrl Pts',(0.138382210043398,0.0590753877074232,
1.45527483195022));
#19370=CARTESIAN_POINT('Ctrl Pts',(0.0254091034322018,0.148306397458819,
1.46321382158753));
#19371=CARTESIAN_POINT('Ctrl Pts',(-0.110830116988615,0.101767718932792,
1.47115281122483));
#19372=CARTESIAN_POINT('Ctrl Pts',(-0.145600909330124,-0.0379221829034233,
1.47909180086214));
#19373=CARTESIAN_POINT('Ctrl Pts',(-0.0471050325108872,-0.142916194795756,
1.48703079049945));
#19374=CARTESIAN_POINT('Ctrl Pts',(0.0945521370959566,-0.117043625665234,
1.49496978013675));
#19375=CARTESIAN_POINT('Ctrl Pts',(0.14957741911039,0.0159047428854941,
1.50290876977406));
#19376=CARTESIAN_POINT('Ctrl Pts',(0.0678206238522695,0.134426714629862,
1.51084775941136));
#19377=CARTESIAN_POINT('Ctrl Pts',(-0.0763126473618499,0.129627546381738,
1.51878674904867));
#19378=CARTESIAN_POINT('Ctrl Pts',(-0.125385920115907,0.0477050348167321,
1.52407940880687));
#19379=CARTESIAN_POINT('Ctrl Pts',(-0.127184992207234,0.00540996832206346,
1.52672573868597));
#19380=CARTESIAN_POINT('Ctrl Pts',(0.0684664424539414,-0.095829519891843,
-1.38777878078145E-17));
#19381=CARTESIAN_POINT('Ctrl Pts',(0.100334321247169,-0.0730611673843044,
0.00264632987910189));
#19382=CARTESIAN_POINT('Ctrl Pts',(0.139021564822767,0.00636891437108143,
0.00793898963730573));
#19383=CARTESIAN_POINT('Ctrl Pts',(0.0699018669780613,0.120491966796142,
0.0158779792746114));
#19384=CARTESIAN_POINT('Ctrl Pts',(-0.0632645460347191,0.123954346655885,
0.0238169689119172));
#19385=CARTESIAN_POINT('Ctrl Pts',(-0.138486976988987,0.0141253725679007,
0.0317559585492228));
#19386=CARTESIAN_POINT('Ctrl Pts',(-0.0869496735326521,-0.108728403071097,
0.0396949481865287));
#19387=CARTESIAN_POINT('Ctrl Pts',(0.0441923146003338,-0.131999388615902,
0.0476339378238343));
#19388=CARTESIAN_POINT('Ctrl Pts',(0.134874939024977,-0.034459980695041,
0.0555729274611401));
#19389=CARTESIAN_POINT('Ctrl Pts',(0.102091080224759,0.094638871230671,
0.0635119170984456));
#19390=CARTESIAN_POINT('Ctrl Pts',(-0.0241513666277066,0.137095110112719,
0.0714509067357516));
#19391=CARTESIAN_POINT('Ctrl Pts',(-0.128284260007319,0.0540539703915629,
0.0793898963730571));
#19392=CARTESIAN_POINT('Ctrl Pts',(-0.114982038412656,-0.0784718756714057,
0.0873288860103631));
#19393=CARTESIAN_POINT('Ctrl Pts',(0.00357853460314598,-0.139161043603659,
0.0952678756476685));
#19394=CARTESIAN_POINT('Ctrl Pts',(0.118863112008681,-0.0724583686054966,
0.103206865284975));
#19395=CARTESIAN_POINT('Ctrl Pts',(0.125336705278751,0.0605752693714656,
0.11114585492228));
#19396=CARTESIAN_POINT('Ctrl Pts',(0.0170731091066207,0.138156245709763,
0.119084844559586));
#19397=CARTESIAN_POINT('Ctrl Pts',(-0.106819734848208,0.0892647286947484,
0.127023834196891));
#19398=CARTESIAN_POINT('Ctrl Pts',(-0.132926439498961,-0.0413425724611633,
0.134962823834197));
#19399=CARTESIAN_POINT('Ctrl Pts',(-0.0373480950846616,-0.134103559412242,
0.142901813471503));
#19400=CARTESIAN_POINT('Ctrl Pts',(0.0924198687735613,-0.104101940294199,
0.150840803108809));
#19401=CARTESIAN_POINT('Ctrl Pts',(0.137583777756591,0.0211978768359354,
0.158779792746114));
#19402=CARTESIAN_POINT('Ctrl Pts',(0.0567991668878991,0.127092487218924,
0.16671878238342));
#19403=CARTESIAN_POINT('Ctrl Pts',(-0.075981188277068,0.116642637502503,
0.174657772020726));
#19404=CARTESIAN_POINT('Ctrl Pts',(-0.139205973057234,-0.000585553717998882,
0.182596761658032));
#19405=CARTESIAN_POINT('Ctrl Pts',(-0.0749972298318695,-0.11727771015962,
0.190535751295337));
#19406=CARTESIAN_POINT('Ctrl Pts',(0.0578663373665801,-0.126610160769685,
0.198474740932643));
#19407=CARTESIAN_POINT('Ctrl Pts',(0.13775723856723,-0.0200396862227523,
0.206413730569949));
#19408=CARTESIAN_POINT('Ctrl Pts',(0.091540828968026,0.104875747581476,
0.214352720207254));
#19409=CARTESIAN_POINT('Ctrl Pts',(-0.0384749358425138,0.133784622116252,
0.22229170984456));
#19410=CARTESIAN_POINT('Ctrl Pts',(-0.133269533752038,0.0402228439430644,
0.230230699481866));
#19411=CARTESIAN_POINT('Ctrl Pts',(-0.106065007067505,-0.0901601911982067,
0.238169689119172));
#19412=CARTESIAN_POINT('Ctrl Pts',(0.0182347644767634,-0.138007750384372,
0.246108678756477));
#19413=CARTESIAN_POINT('Ctrl Pts',(0.125841858853055,-0.0595186723796334,
0.254047668393783));
#19414=CARTESIAN_POINT('Ctrl Pts',(0.118249355954961,0.073455671106145,
0.261986658031089));
#19415=CARTESIAN_POINT('Ctrl Pts',(0.00240767183786234,0.139186381940956,
0.269925647668394));
#19416=CARTESIAN_POINT('Ctrl Pts',(-0.115638070838342,0.0775014991741366,
0.277864637305701));
#19417=CARTESIAN_POINT('Ctrl Pts',(-0.12782508485658,-0.0551306945617612,
0.285803626943006));
#19418=CARTESIAN_POINT('Ctrl Pts',(-0.0229969941138309,-0.137294515779738,
0.293742616580312));
#19419=CARTESIAN_POINT('Ctrl Pts',(0.102883268653204,-0.0937746172089793,
0.301681606217617));
#19420=CARTESIAN_POINT('Ctrl Pts',(0.134580950019115,0.0355895166223291,
0.309620595854923));
#19421=CARTESIAN_POINT('Ctrl Pts',(0.0430789950773988,0.13237388709478,
0.317559585492229));
#19422=CARTESIAN_POINT('Ctrl Pts',(-0.0878588274613298,0.107979036106918,
0.325498575129534));
#19423=CARTESIAN_POINT('Ctrl Pts',(-0.1383679148179,-0.0152632221501787,
0.33343756476684));
#19424=CARTESIAN_POINT('Ctrl Pts',(-0.0622106591311991,-0.12453304658572,
0.341376554404146));
#19425=CARTESIAN_POINT('Ctrl Pts',(0.0708961914151981,-0.119801401679107,
0.349315544041452));
#19426=CARTESIAN_POINT('Ctrl Pts',(0.1391024375543,-0.00539978406154301,
0.357254533678757));
#19427=CARTESIAN_POINT('Ctrl Pts',(0.0799699354250877,0.113944965792994,
0.365193523316063));
#19428=CARTESIAN_POINT('Ctrl Pts',(-0.0523695618881846,0.128980908622551,
0.373132512953369));
#19429=CARTESIAN_POINT('Ctrl Pts',(-0.136768314413298,0.0259436692471295,
0.381071502590675));
#19430=CARTESIAN_POINT('Ctrl Pts',(-0.0959650484377783,-0.100843221288265,
0.38901049222798));
#19431=CARTESIAN_POINT('Ctrl Pts',(0.0326876424682324,-0.135315053971568,
0.396949481865287));
#19432=CARTESIAN_POINT('Ctrl Pts',(0.13141703692502,-0.0459152284901983,
0.404888471502591));
#19433=CARTESIAN_POINT('Ctrl Pts',(0.109843140674695,0.0855168418978295,
0.412827461139898));
#19434=CARTESIAN_POINT('Ctrl Pts',(-0.0122846228212416,0.13866410438033,
0.420766450777203));
#19435=CARTESIAN_POINT('Ctrl Pts',(-0.123166656044517,0.0648738825743514,
0.428705440414509));
#19436=CARTESIAN_POINT('Ctrl Pts',(-0.121298056821252,-0.0683039326309071,
0.436644430051815));
#19437=CARTESIAN_POINT('Ctrl Pts',(-0.00838939967687663,-0.138954178686792,
0.44458341968912));
#19438=CARTESIAN_POINT('Ctrl Pts',(0.11219917790857,-0.0824013973067221,
0.452522409326426));
#19439=CARTESIAN_POINT('Ctrl Pts',(0.13007709763057,0.0495842159710775,
0.460461398963732));
#19440=CARTESIAN_POINT('Ctrl Pts',(0.0288783492374893,0.136178877755608,
0.468400388601037));
#19441=CARTESIAN_POINT('Ctrl Pts',(-0.0987565487199846,0.0981111099028881,
0.476339378238344));
#19442=CARTESIAN_POINT('Ctrl Pts',(-0.135986594552616,-0.0297706550724338,
0.484278367875649));
#19443=CARTESIAN_POINT('Ctrl Pts',(-0.0487302328423073,-0.130399425645183,
0.492217357512954));
#19444=CARTESIAN_POINT('Ctrl Pts',(0.0831353173341669,-0.111656458896056,
0.50015634715026));
#19445=CARTESIAN_POINT('Ctrl Pts',(0.13889618212661,0.00930034365552528,
0.508095336787567));
#19446=CARTESIAN_POINT('Ctrl Pts',(0.0675071113591811,0.12174331898465,
0.516034326424871));
#19447=CARTESIAN_POINT('Ctrl Pts',(-0.0656800932930844,0.122738629397884,
0.523973316062178));
#19448=CARTESIAN_POINT('Ctrl Pts',(-0.138741673886299,0.0113751364249866,
0.531912305699483));
#19449=CARTESIAN_POINT('Ctrl Pts',(-0.0847947606245053,-0.110401514355972,
0.539851295336789));
#19450=CARTESIAN_POINT('Ctrl Pts',(0.0467759446245483,-0.131113145053959,
0.547790284974095));
#19451=CARTESIAN_POINT('Ctrl Pts',(0.135526478334676,-0.031799677225719,
0.555729274611401));
#19452=CARTESIAN_POINT('Ctrl Pts',(0.100211809365564,0.0966242157284558,
0.563668264248707));
#19453=CARTESIAN_POINT('Ctrl Pts',(-0.0268399031138932,0.136595261273209,
0.571607253886012));
#19454=CARTESIAN_POINT('Ctrl Pts',(-0.129321523751272,0.0515227066069736,
0.579546243523318));
#19455=CARTESIAN_POINT('Ctrl Pts',(-0.113418152377209,-0.0807153548762533,
0.587485233160623));
#19456=CARTESIAN_POINT('Ctrl Pts',(0.00631176444456456,-0.139064040754811,
0.595424222797929));
#19457=CARTESIAN_POINT('Ctrl Pts',(0.120263693490807,-0.0701091280034811,
0.603363212435234));
#19458=CARTESIAN_POINT('Ctrl Pts',(0.124122453355413,0.0630258865426945,
0.611302202072541));
#19459=CARTESIAN_POINT('Ctrl Pts',(0.0143556138404206,0.138465021405133,
0.619241191709845));
#19460=CARTESIAN_POINT('Ctrl Pts',(-0.108552806291007,0.0871489187988374,
0.627180181347153));
#19461=CARTESIAN_POINT('Ctrl Pts',(-0.132088571872698,-0.043946046262323,
0.635119170984457));
#19462=CARTESIAN_POINT('Ctrl Pts',(-0.0347063025259737,-0.134811417789573,
0.643058160621763));
#19463=CARTESIAN_POINT('Ctrl Pts',(0.0944472082050275,-0.102266175560326,
0.65099715025907));
#19464=CARTESIAN_POINT('Ctrl Pts',(0.137140772714236,0.0238967416356601,
0.658936139896373));
#19465=CARTESIAN_POINT('Ctrl Pts',(0.054291358674537,0.128183829614862,
0.666875129533682));
#19466=CARTESIAN_POINT('Ctrl Pts',(-0.0782580734018908,0.115127406593233,
0.674814119170985));
#19467=CARTESIAN_POINT('Ctrl Pts',(-0.139167602654929,-0.00332026696803425,
0.682753108808293));
#19468=CARTESIAN_POINT('Ctrl Pts',(-0.0726787294560835,-0.118728463672822,
0.690692098445597));
#19469=CARTESIAN_POINT('Ctrl Pts',(0.0603425395611779,-0.125448888878168,
0.698631088082904));
#19470=CARTESIAN_POINT('Ctrl Pts',(0.138124349154501,-0.0173294538893964,
0.706570077720209));
#19471=CARTESIAN_POINT('Ctrl Pts',(0.0894627833767505,0.106653908470079,
0.714509067357515));
#19472=CARTESIAN_POINT('Ctrl Pts',(-0.0410958292974484,0.133002927094911,
0.72244805699482));
#19473=CARTESIAN_POINT('Ctrl Pts',(-0.134034026730954,0.0375968812502473,
0.730387046632127));
#19474=CARTESIAN_POINT('Ctrl Pts',(-0.104273258644039,-0.0922265326964679,
0.738326036269432));
#19475=CARTESIAN_POINT('Ctrl Pts',(0.0209425314183671,-0.137622876656644,
0.746265025906738));
#19476=CARTESIAN_POINT('Ctrl Pts',(0.126986869252672,-0.0570349089493802,
0.754204015544043));
#19477=CARTESIAN_POINT('Ctrl Pts',(0.11678343126468,0.0757646090434518,
0.762143005181349));
#19478=CARTESIAN_POINT('Ctrl Pts',(-0.000327234354877375,0.139206819944772,
0.770081994818654));
#19479=CARTESIAN_POINT('Ctrl Pts',(-0.117138339349379,0.0752147276530931,
0.778020984455961));
#19480=CARTESIAN_POINT('Ctrl Pts',(-0.126717322684213,-0.0576312930030564,
0.785959974093266));
#19481=CARTESIAN_POINT('Ctrl Pts',(-0.0202952816069424,-0.137719814645367,
0.793898963730571));
#19482=CARTESIAN_POINT('Ctrl Pts',(0.104705698854998,-0.0917352845351548,
0.801837953367879));
#19483=CARTESIAN_POINT('Ctrl Pts',(0.133855787965376,0.0382266115373486,
0.809776943005182));
#19484=CARTESIAN_POINT('Ctrl Pts',(0.0404700769297216,0.133194664588195,
0.81771593264249));
#19485=CARTESIAN_POINT('Ctrl Pts',(-0.0899632159395838,0.106232130635072,
0.825654922279794));
#19486=CARTESIAN_POINT('Ctrl Pts',(-0.13804135019805,-0.0179786383510676,
0.833593911917101));
#19487=CARTESIAN_POINT('Ctrl Pts',(-0.059752088941783,-0.125731196083361,
0.841532901554406));
#19488=CARTESIAN_POINT('Ctrl Pts',(0.0732361146625898,-0.118385460722959,
0.849471891191712));
#19489=CARTESIAN_POINT('Ctrl Pts',(0.139181674492094,-0.00266594955618734,
0.857410880829018));
#19490=CARTESIAN_POINT('Ctrl Pts',(0.077715950067195,0.115494055719818,
0.865349870466323));
#19491=CARTESIAN_POINT('Ctrl Pts',(-0.0548934004223171,0.127927168308903,
0.87328886010363));
#19492=CARTESIAN_POINT('Ctrl Pts',(-0.137251604915624,0.0232517257326144,
0.881227849740934));
#19493=CARTESIAN_POINT('Ctrl Pts',(-0.0939653715754795,-0.102709078207047,
0.889166839378241));
#19494=CARTESIAN_POINT('Ctrl Pts',(0.0353397195745277,-0.134646760160997,
0.897105829015547));
#19495=CARTESIAN_POINT('Ctrl Pts',(0.132293719443212,-0.0433245611326863,
0.905044818652852));
#19496=CARTESIAN_POINT('Ctrl Pts',(0.108141885842356,0.0876583043865096,
0.912983808290157));
#19497=CARTESIAN_POINT('Ctrl Pts',(-0.0150064327997127,0.138395999855801,
0.920922797927463));
#19498=CARTESIAN_POINT('Ctrl Pts',(-0.124417390671652,0.0624416423544169,
0.928861787564769));
#19499=CARTESIAN_POINT('Ctrl Pts',(-0.119932754264349,-0.0706737593172073,
0.936800777202075));
#19500=CARTESIAN_POINT('Ctrl Pts',(-0.00565790085648466,-0.139092177922979,
0.944739766839381));
#19501=CARTESIAN_POINT('Ctrl Pts',(0.113796373024222,-0.0801812402497705,
0.952678756476687));
#19502=CARTESIAN_POINT('Ctrl Pts',(0.129077866376032,0.0521301276928276,
0.960617746113992));
#19503=CARTESIAN_POINT('Ctrl Pts',(0.026197419344502,0.13671993644362,0.968556735751298));
#19504=CARTESIAN_POINT('Ctrl Pts',(-0.100664969670515,0.0961520134094621,
0.976495725388603));
#19505=CARTESIAN_POINT('Ctrl Pts',(-0.13537547797311,-0.0324364881732178,
0.98443471502591));
#19506=CARTESIAN_POINT('Ctrl Pts',(-0.0461590140787468,-0.131331607851033,
0.992373704663214));
#19507=CARTESIAN_POINT('Ctrl Pts',(0.0853128637208732,-0.110001641284132,
1.00031269430052));
#19508=CARTESIAN_POINT('Ctrl Pts',(0.138686661656432,0.0120272889735618,
1.00825168393783));
#19509=CARTESIAN_POINT('Ctrl Pts',(0.0651023256631918,0.123046060459907,
1.01619067357513));
#19510=CARTESIAN_POINT('Ctrl Pts',(-0.0680787277209358,0.121424596492465,
1.02412966321244));
#19511=CARTESIAN_POINT('Ctrl Pts',(-0.138938371616466,0.00864723620724691,
1.03206865284975));
#19512=CARTESIAN_POINT('Ctrl Pts',(-0.0826094583655966,-0.112046076191904,
1.04000764248705));
#19513=CARTESIAN_POINT('Ctrl Pts',(0.0493427524230464,-0.130168884856471,
1.04794663212436));
#19514=CARTESIAN_POINT('Ctrl Pts',(0.136125055048066,-0.0291310004912345,
1.05588562176166));
#19515=CARTESIAN_POINT('Ctrl Pts',(0.0982941990358779,0.0985743183458784,
1.06382461139897));
#19516=CARTESIAN_POINT('Ctrl Pts',(-0.0295182596522469,0.136041604476578,
1.07176360103627));
#19517=CARTESIAN_POINT('Ctrl Pts',(-0.130308774647192,0.0489721252490281,
1.07970259067358));
#19518=CARTESIAN_POINT('Ctrl Pts',(-0.111810537096203,-0.0829279783650712,
1.08764158031088));
#19519=CARTESIAN_POINT('Ctrl Pts',(0.00904258428980543,-0.13891320121148,
1.09558056994819));
#19520=CARTESIAN_POINT('Ctrl Pts',(0.121617839487272,-0.067732908692211,
1.1035195595855));
#19521=CARTESIAN_POINT('Ctrl Pts',(0.122860297649024,0.0654522196953821,
1.1114585492228));
#19522=CARTESIAN_POINT('Ctrl Pts',(0.0116325734791967,0.138720326685422,
1.11939753886011));
#19523=CARTESIAN_POINT('Ctrl Pts',(-0.110243974478508,0.0849994817198388,
1.12733652849741));
#19524=CARTESIAN_POINT('Ctrl Pts',(-0.131199719314147,-0.0465325633653302,
1.13527551813472));
#19525=CARTESIAN_POINT('Ctrl Pts',(-0.0320511128216771,-0.13546723577438,
1.14321450777202));
#19526=CARTESIAN_POINT('Ctrl Pts',(0.0964380908528195,-0.100390938007982,
1.15115349740933));
#19527=CARTESIAN_POINT('Ctrl Pts',(0.136644831685568,0.0265863832644056,
1.15909248704664));
#19528=CARTESIAN_POINT('Ctrl Pts',(0.0517625939920979,0.129225692742072,
1.16703147668394));
#19529=CARTESIAN_POINT('Ctrl Pts',(-0.0805047509788913,0.113567736929491,
1.17497046632125));
#19530=CARTESIAN_POINT('Ctrl Pts',(-0.139075513779617,-0.00605369873671642,
1.18290945595855));
#19531=CARTESIAN_POINT('Ctrl Pts',(-0.0703321751825429,-0.12013338809653,
1.19084844559586));
#19532=CARTESIAN_POINT('Ctrl Pts',(0.0627954496153871,-0.124239193932754,
1.19878743523316));
#19533=CARTESIAN_POINT('Ctrl Pts',(0.138438143943654,-0.0146125323915816,
1.20672642487047));
#19534=CARTESIAN_POINT('Ctrl Pts',(0.0873502052771435,0.108390901091839,
1.21466541450777));
#19535=CARTESIAN_POINT('Ctrl Pts',(-0.043700859820065,0.132169893139269,
1.22260440414508));
#19536=CARTESIAN_POINT('Ctrl Pts',(-0.134746782767514,0.0349564062120582,
1.23054339378239));
#19537=CARTESIAN_POINT('Ctrl Pts',(-0.102441260891455,-0.0942572748833364,
1.23848238341969));
#19538=CARTESIAN_POINT('Ctrl Pts',(0.0236422145726536,-0.137184880695923,
1.246421373057));
#19539=CARTESIAN_POINT('Ctrl Pts',(0.128082862902196,-0.0545291301253663,
1.2543603626943));
#19540=CARTESIAN_POINT('Ctrl Pts',(0.115272428336817,0.0780443019497631,
1.26229935233161));
#19541=CARTESIAN_POINT('Ctrl Pts',(-0.00306201423577413,0.139173524314926,
1.27023834196891));
#19542=CARTESIAN_POINT('Ctrl Pts',(-0.118593392628464,0.0728989233548558,
1.27817733160622));
#19543=CARTESIAN_POINT('Ctrl Pts',(-0.125560647806918,-0.06010964584811,
1.28611632124353));
#19544=CARTESIAN_POINT('Ctrl Pts',(-0.0175857351491984,-0.138091953858251,
1.29405531088083));
#19545=CARTESIAN_POINT('Ctrl Pts',(0.106487712804436,-0.089660542174548,
1.30199430051814));
#19546=CARTESIAN_POINT('Ctrl Pts',(0.133078957772855,0.0408489510387311,
1.30993329015544));
#19547=CARTESIAN_POINT('Ctrl Pts',(0.0378455373822902,0.133964029124136,
1.31787227979275));
#19548=CARTESIAN_POINT('Ctrl Pts',(-0.0920328787300654,0.104444219726284,
1.32581126943006));
#19549=CARTESIAN_POINT('Ctrl Pts',(-0.137661501842601,-0.0206871148492911,
1.33375025906736));
#19550=CARTESIAN_POINT('Ctrl Pts',(-0.0572704544775333,-0.126880813469472,
1.34168924870467));
#19551=CARTESIAN_POINT('Ctrl Pts',(0.0755477687720905,-0.116923823242002,
1.34962823834197));
#19552=CARTESIAN_POINT('Ctrl Pts',(0.13920718769651,6.89141801743488E-5,
1.35756722797928));
#19553=CARTESIAN_POINT('Ctrl Pts',(0.0754319660950179,0.116998564767658,
1.36550621761658));
#19554=CARTESIAN_POINT('Ctrl Pts',(-0.0573960494825499,0.126824048933643,
1.37344520725389));
#19555=CARTESIAN_POINT('Ctrl Pts',(-0.13768191782304,0.0205508058651932,
1.38138419689119));
#19556=CARTESIAN_POINT('Ctrl Pts',(-0.0919294216917856,-0.104535287252199,
1.3893231865285));
#19557=CARTESIAN_POINT('Ctrl Pts',(0.0379781508110965,-0.133926497290667,
1.39726217616581));
#19558=CARTESIAN_POINT('Ctrl Pts',(0.133119345865688,-0.0407171622080862,
1.40520116580311));
#19559=CARTESIAN_POINT('Ctrl Pts',(0.106398871137127,0.0897659150453452,
1.41314015544042));
#19560=CARTESIAN_POINT('Ctrl Pts',(-0.0177224175491345,0.138074504763813,
1.42107914507772));
#19561=CARTESIAN_POINT('Ctrl Pts',(-0.125620162573399,0.0599852426217579,
1.42901813471503));
#19562=CARTESIAN_POINT('Ctrl Pts',(-0.118521039729242,-0.0730161975746823,
1.43695712435233));
#19563=CARTESIAN_POINT('Ctrl Pts',(-0.00292444232197888,-0.139176693688359,
1.44489611398964));
#19564=CARTESIAN_POINT('Ctrl Pts',(0.115350068603298,-0.0779297424218237,
1.45283510362695));
#19565=CARTESIAN_POINT('Ctrl Pts',(0.128028003046829,0.0546551750765237,
1.46077409326425));
#19566=CARTESIAN_POINT('Ctrl Pts',(0.0235079116789307,0.137209630484779,
1.46871308290156));
#19567=CARTESIAN_POINT('Ctrl Pts',(-0.102537447198224,0.0941531272373115,
1.47665207253886));
#19568=CARTESIAN_POINT('Ctrl Pts',(-0.134706575776555,-0.0350847218495708,
1.48459106217617));
#19569=CARTESIAN_POINT('Ctrl Pts',(-0.0435804807853106,-0.132222740314769,
1.49253005181348));
#19570=CARTESIAN_POINT('Ctrl Pts',(0.0874774386997331,-0.108286040948335,
1.50046904145078));
#19571=CARTESIAN_POINT('Ctrl Pts',(0.138385550162814,0.0147146982980264,
1.50840803108809));
#19572=CARTESIAN_POINT('Ctrl Pts',(0.0627460642121078,0.124368470664037,
1.51634702072539));
#19573=CARTESIAN_POINT('Ctrl Pts',(-0.0706026869052757,0.119928391791904,
1.5242860103627));
#19574=CARTESIAN_POINT('Ctrl Pts',(-0.116004137797729,0.0441355889673283,
1.5295786701209));
#19575=CARTESIAN_POINT('Ctrl Pts',(-0.117668597464313,0.00500517689812487,
1.532225));
#19576=CARTESIAN_POINT('',(0.0684664424539461,-0.0958295198918396,0.));
#19577=CARTESIAN_POINT('Ctrl Pts',(0.0684664424539414,-0.095829519891843,
-1.38777878078145E-17));
#19578=CARTESIAN_POINT('Ctrl Pts',(0.100334321247169,-0.0730611673843044,
0.00264632987910189));
#19579=CARTESIAN_POINT('Ctrl Pts',(0.139021564822767,0.00636891437108143,
0.00793898963730573));
#19580=CARTESIAN_POINT('Ctrl Pts',(0.0699018669780613,0.120491966796142,
0.0158779792746114));
#19581=CARTESIAN_POINT('Ctrl Pts',(-0.0632645460347191,0.123954346655885,
0.0238169689119172));
#19582=CARTESIAN_POINT('Ctrl Pts',(-0.11596266760442,0.0470121293552651,
0.0293787386625077));
#19583=CARTESIAN_POINT('Ctrl Pts',(-0.117944740497024,0.00404481602818191,
0.0322941785339964));
#19584=CARTESIAN_POINT('Ctrl Pts',(-0.117917485785546,7.60014832213644E-5,
0.0325632885263832));
#19585=CARTESIAN_POINT('Ctrl Pts',(0.0635546915223951,0.132092229195826,
-2.16840434497101E-19));
#19586=CARTESIAN_POINT('Ctrl Pts',(0.0668114782730532,0.13015255741457,
-1.00603861447787E-18));
#19587=CARTESIAN_POINT('Ctrl Pts',(0.0699821360194518,0.12808121947321,
-2.9262196004085E-17));
#19588=CARTESIAN_POINT('Ctrl Pts',(0.0730575207853233,0.125877721325919,
-2.71050543121376E-17));
#19589=CARTESIAN_POINT('Ctrl Pts',(0.0789281193465506,0.121671466161783,
-2.36378102375718E-17));
#19590=CARTESIAN_POINT('Ctrl Pts',(0.0844522091809674,0.11698398814956,
1.43782932504085E-18));
#19591=CARTESIAN_POINT('Ctrl Pts',(0.0895990070394484,0.111875963994554,
9.97465998686664E-18));
#19592=CARTESIAN_POINT('Ctrl Pts',(0.0928865546640729,0.108613183302742,
1.54276111490851E-17));
#19593=CARTESIAN_POINT('Ctrl Pts',(0.0960206821069302,0.105176950779614,
-2.53636710091701E-17));
#19594=CARTESIAN_POINT('Ctrl Pts',(0.098978417360439,0.101599719103904,
-1.56125112837913E-17));
#19595=CARTESIAN_POINT('Ctrl Pts',(0.103148772110026,0.0965558852815647,
-1.86354736740503E-18));
#19596=CARTESIAN_POINT('Ctrl Pts',(0.106976174326278,0.0912251680483688,
1.1337629845105E-17));
#19597=CARTESIAN_POINT('Ctrl Pts',(0.110435561611279,0.0856523061447448,
2.03830008427275E-17));
#19598=CARTESIAN_POINT('Ctrl Pts',(0.112407683932559,0.0824753373788608,
2.55395723911076E-17));
#19599=CARTESIAN_POINT('Ctrl Pts',(0.114261188142284,0.0792174064057451,
2.29308760465575E-17));
#19600=CARTESIAN_POINT('Ctrl Pts',(0.115986535786665,0.0758936579718971,
2.08166817117217E-17));
#19601=CARTESIAN_POINT('Ctrl Pts',(0.120573220307724,0.0670577659456877,
1.51962825639422E-17));
#19602=CARTESIAN_POINT('Ctrl Pts',(0.124235263225439,0.0578042025119142,
2.52358375750583E-18));
#19603=CARTESIAN_POINT('Ctrl Pts',(0.126883306113679,0.0482911783993335,
1.30104260698261E-17));
#19604=CARTESIAN_POINT('Ctrl Pts',(0.128478610866444,0.0425600882242624,
1.93281898253259E-17));
#19605=CARTESIAN_POINT('Ctrl Pts',(0.129704960854084,0.0367345196138549,
-5.78096029915021E-19));
#19606=CARTESIAN_POINT('Ctrl Pts',(0.130533291754837,0.0308494671050701,
0.));
#19607=CARTESIAN_POINT('Ctrl Pts',(0.131003715791213,0.0275072397983871,
3.2831114661813E-19));
#19608=CARTESIAN_POINT('Ctrl Pts',(0.131345346899704,0.0241444941465381,
-1.7128612844445E-18));
#19609=CARTESIAN_POINT('Ctrl Pts',(0.131551728167405,0.0207857616715298,
2.60208521396521E-18));
#19610=CARTESIAN_POINT('Ctrl Pts',(0.131851321606701,0.0159100565018035,
8.86587880453295E-18));
#19611=CARTESIAN_POINT('Ctrl Pts',(0.131867617692795,0.0110341713389591,
-1.68111772803455E-17));
#19612=CARTESIAN_POINT('Ctrl Pts',(0.131586936334964,0.0061777758930637,
-6.93889390390723E-18));
#19613=CARTESIAN_POINT('Ctrl Pts',(0.131099036368572,-0.00226395031615145,
9.98510028643051E-18));
#19614=CARTESIAN_POINT('Ctrl Pts',(0.129715139118287,-0.0106479390144509,
1.03491660509995E-17));
#19615=CARTESIAN_POINT('Ctrl Pts',(0.127493709984164,-0.018859987399606,
1.04083408558608E-17));
#19616=CARTESIAN_POINT('Ctrl Pts',(0.126553994220251,-0.0223338732882013,
1.04333731632617E-17));
#19617=CARTESIAN_POINT('Ctrl Pts',(0.125463061762623,-0.0257782540966497,
1.75224609115742E-17));
#19618=CARTESIAN_POINT('Ctrl Pts',(0.124232565886791,-0.0291638780753137,
1.73472347597681E-17));
#19619=CARTESIAN_POINT('Ctrl Pts',(0.12170396813588,-0.0361211392462112,
1.69871551674183E-17));
#19620=CARTESIAN_POINT('Ctrl Pts',(0.118582485980247,-0.0428512226170345,
-6.45748389186585E-19));
#19621=CARTESIAN_POINT('Ctrl Pts',(0.114911168983798,-0.0492778939609075,
3.46944695195361E-18));
#19622=CARTESIAN_POINT('Ctrl Pts',(0.112347970921096,-0.0537647937721124,
6.34254691478841E-18));
#19623=CARTESIAN_POINT('Ctrl Pts',(0.109516356061708,-0.0581036184196785,
-1.05628593522785E-17));
#19624=CARTESIAN_POINT('Ctrl Pts',(0.106427098863261,-0.0622637901458048,
-1.21430643318376E-17));
#19625=CARTESIAN_POINT('Ctrl Pts',(0.104287070791936,-0.0651456752410043,
-1.32377232732828E-17));
#19626=CARTESIAN_POINT('Ctrl Pts',(0.102021590876101,-0.067943056099314,
-1.03088264066386E-17));
#19627=CARTESIAN_POINT('Ctrl Pts',(0.0996491962474235,-0.0706287444932102,
-1.04083408558608E-17));
#19628=CARTESIAN_POINT('Ctrl Pts',(0.0938611946766418,-0.0771810981592459,
-1.06511292104842E-17));
#19629=CARTESIAN_POINT('Ctrl Pts',(0.0874218747326319,-0.0830961188460978,
9.460259835177E-18));
#19630=CARTESIAN_POINT('Ctrl Pts',(0.0803902102994179,-0.0882260767030795,
2.94902990916057E-17));
#19631=CARTESIAN_POINT('Ctrl Pts',(0.0765868618375105,-0.091000813397402,
4.03243227742548E-17));
#19632=CARTESIAN_POINT('Ctrl Pts',(0.0726097989303321,-0.0935451549285004,
-2.49510848448888E-18));
#19633=CARTESIAN_POINT('Ctrl Pts',(0.0684664424539416,-0.0958295198918429,
0.));
#19634=CARTESIAN_POINT('Ctrl Pts',(-0.00156962371674571,0.146072546381438,
1.50365));
#19635=CARTESIAN_POINT('Ctrl Pts',(0.0218361081466035,0.146362061217761,
1.50238307892777));
#19636=CARTESIAN_POINT('Ctrl Pts',(0.0452966847593804,0.141345883428421,
1.50111615785553));
#19637=CARTESIAN_POINT('Ctrl Pts',(0.0660179268768178,0.130913916311315,
1.4998492367833));
#19638=CARTESIAN_POINT('Ctrl Pts',(0.109300214423576,0.109123745727819,
1.4972029069042));
#19639=CARTESIAN_POINT('Ctrl Pts',(0.140630685714559,0.0637042888941242,
1.49455657702509));
#19640=CARTESIAN_POINT('Ctrl Pts',(0.145752650840527,0.0155206226173656,
1.49191024714599));
#19641=CARTESIAN_POINT('Ctrl Pts',(0.150874615966495,-0.0326630436593903,
1.48926391726689));
#19642=CARTESIAN_POINT('Ctrl Pts',(0.129788074927449,-0.0836109193792113,
1.48661758738779));
#19643=CARTESIAN_POINT('Ctrl Pts',(0.0921021927661857,-0.114042242015571,
1.48397125750869));
#19644=CARTESIAN_POINT('Ctrl Pts',(0.0544163106049216,-0.144473564651931,
1.48132492762959));
#19645=CARTESIAN_POINT('Ctrl Pts',(0.000131087321441313,-0.154388334204831,
1.47867859775048));
#19646=CARTESIAN_POINT('Ctrl Pts',(-0.0458840977328367,-0.139228052523514,
1.47603226787138));
#19647=CARTESIAN_POINT('Ctrl Pts',(-0.0918992827871148,-0.124067770842196,
1.47338593799228));
#19648=CARTESIAN_POINT('Ctrl Pts',(-0.129644429612189,-0.0838324379266627,
1.47073960811318));
#19649=CARTESIAN_POINT('Ctrl Pts',(-0.141854649713415,-0.0369491035797489,
1.46809327823408));
#19650=CARTESIAN_POINT('Ctrl Pts',(-0.14497337938942,-0.0249741805295802,
1.46741735368415));
#19651=CARTESIAN_POINT('Ctrl Pts',(-0.146426231435716,-0.0125655473306973,
1.46674142913422));
#19652=CARTESIAN_POINT('Ctrl Pts',(-0.14631473222987,-0.000131398079681141,
1.46606550458429));
#19653=CARTESIAN_POINT('Origin',(0.,0.,-0.0924367114736175));
#19654=CARTESIAN_POINT('',(-0.0684664424539507,-0.0958295198918364,0.));
#19655=CARTESIAN_POINT('Ctrl Pts',(-0.0686146973663072,-0.0959584553529141,
8.16675286424706E-17));
#19656=CARTESIAN_POINT('Ctrl Pts',(-0.0391968190522335,-0.116741470120209,
0.00244290680874874));
#19657=CARTESIAN_POINT('Ctrl Pts',(0.0436301113039178,-0.130476273073809,
0.0075332029917574));
#19658=CARTESIAN_POINT('Ctrl Pts',(0.134092250525203,-0.0374520209666004,
0.0152708885490261));
#19659=CARTESIAN_POINT('Ctrl Pts',(0.104134301645602,0.0924305194826295,
0.023213056671806));
#19660=CARTESIAN_POINT('Ctrl Pts',(-0.0212379681243542,0.137589894578696,
0.0311552247945861));
#19661=CARTESIAN_POINT('Ctrl Pts',(-0.106685947947232,0.0723488109778776,
0.0375631097285225));
#19662=CARTESIAN_POINT('Ctrl Pts',(-0.117663533972591,0.0165813593984342,
0.041323605288199));
#19663=CARTESIAN_POINT('Ctrl Pts',(-0.117600989619072,5.04992496179954E-5,
0.0424367114736154));
#19664=CARTESIAN_POINT('Origin',(0.,0.,0.));
#19665=CARTESIAN_POINT('Ctrl Pts',(-0.0510216505388318,0.106149619882943,
-0.0164977839420939));
#19666=CARTESIAN_POINT('Ctrl Pts',(-0.0863355867949722,0.0891756983861136,
-0.0138503945678339));
#19667=CARTESIAN_POINT('Ctrl Pts',(-0.13808023131828,0.0175094743621551,
-0.00855561581931395));
#19668=CARTESIAN_POINT('Ctrl Pts',(-0.0894531427980795,-0.106808298616542,
-0.000613447696533924));
#19669=CARTESIAN_POINT('Ctrl Pts',(0.0412394829729132,-0.132934609947913,
0.00732872042624606));
#19670=CARTESIAN_POINT('Ctrl Pts',(0.134092250525203,-0.0374520209666004,
0.0152708885490261));
#19671=CARTESIAN_POINT('Ctrl Pts',(0.104134301645602,0.0924305194826295,
0.023213056671806));
#19672=CARTESIAN_POINT('Ctrl Pts',(-0.0212379681243542,0.137589894578696,
0.0311552247945861));
#19673=CARTESIAN_POINT('Ctrl Pts',(-0.127145335141994,0.0567276974868182,
0.039097392917366));
#19674=CARTESIAN_POINT('Ctrl Pts',(-0.116579117211717,-0.0761160149501382,
0.0470395610401461));
#19675=CARTESIAN_POINT('Ctrl Pts',(0.000787973702835166,-0.139222729671589,
0.054981729162926));
#19676=CARTESIAN_POINT('Ctrl Pts',(0.117431922513572,-0.0747907597173192,
0.0629238972857061));
#19677=CARTESIAN_POINT('Ctrl Pts',(0.126496838785129,0.0581591461343325,
0.070866065408486));
#19678=CARTESIAN_POINT('Ctrl Pts',(0.0196773008918215,0.137828289815661,
0.0788082335312661));
#19679=CARTESIAN_POINT('Ctrl Pts',(-0.105168479521776,0.0912330920368172,
0.0867504016540459));
#19680=CARTESIAN_POINT('Ctrl Pts',(-0.133669226619255,-0.0389412707994331,
0.0946925697768262));
#19681=CARTESIAN_POINT('Ctrl Pts',(-0.0397151780004399,-0.133441281507892,
0.102634737899606));
#19682=CARTESIAN_POINT('Ctrl Pts',(0.0906220264938673,-0.105695447092796,
0.110576906022386));
#19683=CARTESIAN_POINT('Ctrl Pts',(0.137940159127448,0.0188783162799928,
0.118519074145166));
#19684=CARTESIAN_POINT('Ctrl Pts',(0.0588909273047484,0.126157580947307,
0.126461242267946));
#19685=CARTESIAN_POINT('Ctrl Pts',(-0.074108440039672,0.117863552156501,
0.134403410390726));
#19686=CARTESIAN_POINT('Ctrl Pts',(-0.139216864956951,0.00159439502933392,
0.142345578513506));
#19687=CARTESIAN_POINT('Ctrl Pts',(-0.0767883381764272,-0.116135388594389,
0.150287746636286));
#19688=CARTESIAN_POINT('Ctrl Pts',(0.0559861945572589,-0.127473226882309,
0.158229914759066));
#19689=CARTESIAN_POINT('Ctrl Pts',(0.137471621702818,-0.0220324926503626,
0.166172082881846));
#19690=CARTESIAN_POINT('Ctrl Pts',(0.0930189202108026,0.103592267873211,
0.174114251004626));
#19691=CARTESIAN_POINT('Ctrl Pts',(-0.0366486683060043,0.134315868829211,
0.182056419127406));
#19692=CARTESIAN_POINT('Ctrl Pts',(-0.132742311638566,0.0419923350165386,
0.189998587250186));
#19693=CARTESIAN_POINT('Ctrl Pts',(-0.107230360350792,-0.0888004916405464,
0.197940755372966));
#19694=CARTESIAN_POINT('Ctrl Pts',(0.0165156171993534,-0.138242945169174,
0.205882923495746));
#19695=CARTESIAN_POINT('Ctrl Pts',(0.125131592687617,-0.061040658666823,
0.213825091618526));
#19696=CARTESIAN_POINT('Ctrl Pts',(0.119114174013628,0.0720811421096423,
0.221767259741306));
#19697=CARTESIAN_POINT('Ctrl Pts',(0.0039759348809324,0.139169211541763,
0.229709427864086));
#19698=CARTESIAN_POINT('Ctrl Pts',(-0.114804669066963,0.0787639858025777,
0.237651595986866));
#19699=CARTESIAN_POINT('Ctrl Pts',(-0.128412401817242,-0.0537971426620367,
0.245593764109646));
#19700=CARTESIAN_POINT('Ctrl Pts',(-0.024381182195918,-0.137074561658528,
0.253535932232426));
#19701=CARTESIAN_POINT('Ctrl Pts',(0.101985705091022,-0.094777599970642,
0.261478100355206));
#19702=CARTESIAN_POINT('Ctrl Pts',(0.134923209124943,0.0343453801629359,
0.269420268477986));
#19703=CARTESIAN_POINT('Ctrl Pts',(0.0442571924125319,0.132004463632409,
0.277362436600766));
#19704=CARTESIAN_POINT('Ctrl Pts',(-0.0869529592639067,0.108733897080731,
0.285304604723546));
#19705=CARTESIAN_POINT('Ctrl Pts',(-0.138505267237684,-0.0141480898545381,
0.293246772846326));
#19706=CARTESIAN_POINT('Ctrl Pts',(-0.0631725212350128,-0.124068972994571,
0.301188940969106));
#19707=CARTESIAN_POINT('Ctrl Pts',(0.0700327441786229,-0.12032993078169,
0.309131109091886));
#19708=CARTESIAN_POINT('Ctrl Pts',(0.139080821187468,-0.00635631000930847,
0.317073277214666));
#19709=CARTESIAN_POINT('Ctrl Pts',(0.0807165776729536,0.11344034374014,
0.325015445337446));
#19710=CARTESIAN_POINT('Ctrl Pts',(-0.0515923433190751,0.129313988454311,
0.332957613460226));
#19711=CARTESIAN_POINT('Ctrl Pts',(-0.136637377548019,0.026722734813544,
0.340899781583006));
#19712=CARTESIAN_POINT('Ctrl Pts',(-0.0965085366518414,-0.100349289247285,
0.348841949705786));
#19713=CARTESIAN_POINT('Ctrl Pts',(0.0320320385160992,-0.135491055083419,
0.356784117828566));
#19714=CARTESIAN_POINT('Ctrl Pts',(0.131227975626944,-0.0465090949381858,
0.364726285951346));
#19715=CARTESIAN_POINT('Ctrl Pts',(0.110205605501345,0.0850799742312894,
0.372668454074126));
#19716=CARTESIAN_POINT('Ctrl Pts',(-0.0117764211155082,0.138727046407055,
0.380610622196906));
#19717=CARTESIAN_POINT('Ctrl Pts',(-0.122970036152848,0.065285892102983,
0.388552790319686));
#19718=CARTESIAN_POINT('Ctrl Pts',(-0.121510464882371,-0.0679638464419502,
0.396494958442466));
#19719=CARTESIAN_POINT('Ctrl Pts',(-0.00873482453528946,-0.138951719454826,
0.404437126565246));
#19720=CARTESIAN_POINT('Ctrl Pts',(0.112042812448737,-0.0826455423945668,
0.412379294688026));
#19721=CARTESIAN_POINT('Ctrl Pts',(0.130177722634257,0.049372441998279,
0.420321462810806));
#19722=CARTESIAN_POINT('Ctrl Pts',(0.0290564652212241,0.136160197297018,
0.428263630933586));
#19723=CARTESIAN_POINT('Ctrl Pts',(-0.098683499418539,0.098211223603141,
0.436205799056366));
#19724=CARTESIAN_POINT('Ctrl Pts',(-0.136019240449831,-0.0297093205335648,
0.444147967179146));
#19725=CARTESIAN_POINT('Ctrl Pts',(-0.0487473834415776,-0.130413074907061,
0.452090135301926));
#19726=CARTESIAN_POINT('Ctrl Pts',(0.0831820848081396,-0.111645054821459,
0.460032303424706));
#19727=CARTESIAN_POINT('Ctrl Pts',(0.138908217753341,0.00940130521287039,
0.467974471547486));
#19728=CARTESIAN_POINT('Ctrl Pts',(0.0673801526530663,0.121835103839429,
0.475916639670265));
#19729=CARTESIAN_POINT('Ctrl Pts',(-0.0658750545035054,0.12265543075329,
0.483858807793047));
#19730=CARTESIAN_POINT('Ctrl Pts',(-0.138781944133385,0.0111107822259715,
0.491800975915825));
#19731=CARTESIAN_POINT('Ctrl Pts',(-0.084550315326251,-0.110612484274364,
0.499743144038607));
#19732=CARTESIAN_POINT('Ctrl Pts',(0.0471380885036503,-0.131003351527116,
0.507685312161385));
#19733=CARTESIAN_POINT('Ctrl Pts',(0.135643160584381,-0.031381690295376,
0.515627480284167));
#19734=CARTESIAN_POINT('Ctrl Pts',(0.0998851624184703,0.0969888232104648,
0.523569648406945));
#19735=CARTESIAN_POINT('Ctrl Pts',(-0.0273779061153799,0.136507610615132,
0.531511816529727));
#19736=CARTESIAN_POINT('Ctrl Pts',(-0.129560000008381,0.0509714027366644,
0.539453984652505));
#19737=CARTESIAN_POINT('Ctrl Pts',(-0.113051823689188,-0.0812598465397498,
0.547396152775286));
#19738=CARTESIAN_POINT('Ctrl Pts',(0.00702343738442799,-0.139048728244533,
0.555338320898066));
#19739=CARTESIAN_POINT('Ctrl Pts',(0.12066450826877,-0.0694546898587181,
0.563280489020846));
#19740=CARTESIAN_POINT('Ctrl Pts',(0.123764493242992,0.063766979789076,
0.571222657143626));
#19741=CARTESIAN_POINT('Ctrl Pts',(0.0134834875971477,0.13857154491934,
0.579164825266405));
#19742=CARTESIAN_POINT('Ctrl Pts',(-0.109149777898995,0.0864303389077871,
0.587106993389186));
#19743=CARTESIAN_POINT('Ctrl Pts',(-0.131790633456927,-0.0448899368693808,
0.595049161511966));
#19744=CARTESIAN_POINT('Ctrl Pts',(-0.0336977294021144,-0.135086418755761,
0.602991329634746));
#19745=CARTESIAN_POINT('Ctrl Pts',(0.0952657566843092,-0.101529863106778,
0.610933497757526));
#19746=CARTESIAN_POINT('Ctrl Pts',(0.136956022624868,0.025038477707157,
0.618875665880307));
#19747=CARTESIAN_POINT('Ctrl Pts',(0.0531805018142573,0.128669000640787,
0.626817834003085));
#19748=CARTESIAN_POINT('Ctrl Pts',(-0.0793138220987445,0.114425500318782,
0.634760002125867));
#19749=CARTESIAN_POINT('Ctrl Pts',(-0.139148536750765,-0.00464351367351466,
0.642702170248646));
#19750=CARTESIAN_POINT('Ctrl Pts',(-0.0715088964667609,-0.119458592094588,
0.650644338371427));
#19751=CARTESIAN_POINT('Ctrl Pts',(0.0616402393688536,-0.124837327709565,
0.658586506494205));
#19752=CARTESIAN_POINT('Ctrl Pts',(0.138320583400205,-0.0158522461166236,
0.666528674616987));
#19753=CARTESIAN_POINT('Ctrl Pts',(0.0882850628235238,0.107655121482266,
0.674470842739765));
#19754=CARTESIAN_POINT('Ctrl Pts',(-0.0426286451686149,0.132539337972556,
0.682413010862546));
#19755=CARTESIAN_POINT('Ctrl Pts',(-0.13449013477919,0.0360039045964495,
0.690355178985326));
#19756=CARTESIAN_POINT('Ctrl Pts',(-0.103144844235522,-0.0935148042116587,
0.698297347108106));
#19757=CARTESIAN_POINT('Ctrl Pts',(0.022691720100341,-0.137364345221032,
0.706239515230886));
#19758=CARTESIAN_POINT('Ctrl Pts',(0.127740337615313,-0.0553740340325759,
0.714181683353665));
#19759=CARTESIAN_POINT('Ctrl Pts',(0.115765682611161,0.077344581120379,
0.722123851476446));
#19760=CARTESIAN_POINT('Ctrl Pts',(-0.00226223072526165,0.139207614056346,
0.730066019599226));
#19761=CARTESIAN_POINT('Ctrl Pts',(-0.118217708309552,0.0735421711751344,
0.738008187722006));
#19762=CARTESIAN_POINT('Ctrl Pts',(-0.125873620115675,-0.059495455776806,
0.745950355844786));
#19763=CARTESIAN_POINT('Ctrl Pts',(-0.0182163644075178,-0.138029133036789,
0.753892523967566));
#19764=CARTESIAN_POINT('Ctrl Pts',(0.106128952536144,-0.0901139441634624,
0.761834692090347));
#19765=CARTESIAN_POINT('Ctrl Pts',(0.133249245915149,0.0403548753208232,
0.769776860213125));
#19766=CARTESIAN_POINT('Ctrl Pts',(0.0382995408207276,0.133854483197375,
0.777719028335907));
#19767=CARTESIAN_POINT('Ctrl Pts',(-0.0917364783268051,0.104729633071593,
0.785661196458685));
#19768=CARTESIAN_POINT('Ctrl Pts',(-0.137732458880487,-0.0203383202317681,
0.793603364581467));
#19769=CARTESIAN_POINT('Ctrl Pts',(-0.0575513573065257,-0.126774282767806,
0.801545532704245));
#19770=CARTESIAN_POINT('Ctrl Pts',(0.0753527000357912,-0.117071978271622,
0.809487700827026));
#19771=CARTESIAN_POINT('Ctrl Pts',(0.139225942868322,-0.000119714417332432,
0.817429868949805));
#19772=CARTESIAN_POINT('Ctrl Pts',(0.0755539188089132,0.116942220141962,
0.825372037072586));
#19773=CARTESIAN_POINT('Ctrl Pts',(-0.0573332568284509,0.12687306712048,
0.833314205195366));
#19774=CARTESIAN_POINT('Ctrl Pts',(-0.13769727914169,0.0205751504512258,
0.841256373318145));
#19775=CARTESIAN_POINT('Ctrl Pts',(-0.0919164475821765,-0.104571717796869,
0.849198541440926));
#19776=CARTESIAN_POINT('Ctrl Pts',(0.0380692928980519,-0.133920149482284,
0.857140709563706));
#19777=CARTESIAN_POINT('Ctrl Pts',(0.133179650076608,-0.0405839661022353,
0.865082877686486));
#19778=CARTESIAN_POINT('Ctrl Pts',(0.106283765719693,0.0899312995767124,
0.873025045809266));
#19779=CARTESIAN_POINT('Ctrl Pts',(-0.0179789669825735,0.138060255849953,
0.880967213932046));
#19780=CARTESIAN_POINT('Ctrl Pts',(-0.125771118879347,0.0597118342956578,
0.888909382054826));
#19781=CARTESIAN_POINT('Ctrl Pts',(-0.118344004924669,-0.0733387619032726,
0.896851550177606));
#19782=CARTESIAN_POINT('Ctrl Pts',(-0.00250162451743248,-0.139203517821528,
0.904793718300386));
#19783=CARTESIAN_POINT('Ctrl Pts',(0.115632500949424,-0.0775435504945224,
0.912735886423165));
#19784=CARTESIAN_POINT('Ctrl Pts',(0.127835376168433,0.0551542754370876,
0.920678054545947));
#19785=CARTESIAN_POINT('Ctrl Pts',(0.0229279137899797,0.137325118854324,
0.928620222668725));
#19786=CARTESIAN_POINT('Ctrl Pts',(-0.102983873094174,0.0936920454555137,
0.936562390791507));
#19787=CARTESIAN_POINT('Ctrl Pts',(-0.134551852288801,-0.0357725669300891,
0.944504558914285));
#19788=CARTESIAN_POINT('Ctrl Pts',(-0.0428565117498991,-0.132465832952297,
0.952446727037066));
#19789=CARTESIAN_POINT('Ctrl Pts',(0.0880997963686447,-0.107806787258123,
0.960388895159846));
#19790=CARTESIAN_POINT('Ctrl Pts',(0.138347640177547,0.0156143509765511,
0.968331063282625));
#19791=CARTESIAN_POINT('Ctrl Pts',(0.061854832590724,0.124731139593481,
0.976273231405407));
#19792=CARTESIAN_POINT('Ctrl Pts',(-0.0713033562375951,0.119581390225944,
0.984215399528185));
#19793=CARTESIAN_POINT('Ctrl Pts',(-0.139140345480169,0.00488280234845834,
0.992157567650966));
#19794=CARTESIAN_POINT('Ctrl Pts',(-0.0795104838321055,-0.114288934109561,
1.00009973577375));
#19795=CARTESIAN_POINT('Ctrl Pts',(0.0529591494285269,-0.128760265574912,
1.00804190389653));
#19796=CARTESIAN_POINT('Ctrl Pts',(0.136912761112491,-0.0252739657289669,
1.0159840720193));
#19797=CARTESIAN_POINT('Ctrl Pts',(0.0954402180350474,0.101365883217864,
1.02392624014209));
#19798=CARTESIAN_POINT('Ctrl Pts',(-0.0334653697086341,0.135144169424284,
1.03186840826486));
#19799=CARTESIAN_POINT('Ctrl Pts',(-0.131713240771149,0.0451165125500212,
1.03981057638765));
#19800=CARTESIAN_POINT('Ctrl Pts',(-0.109298251871946,-0.0862425048155002,
1.04775274451043));
#19801=CARTESIAN_POINT('Ctrl Pts',(0.0132451643780021,-0.13859452774087,
1.05569491263321));
#19802=CARTESIAN_POINT('Ctrl Pts',(0.123654649330263,-0.0639797248987874,
1.06363708075599));
#19803=CARTESIAN_POINT('Ctrl Pts',(0.120783771971213,0.0692470788374567,
1.07157924887876));
#19804=CARTESIAN_POINT('Ctrl Pts',(0.00726255089817806,0.139036444335888,
1.07952141700155));
#19805=CARTESIAN_POINT('Ctrl Pts',(-0.112911912907791,0.0814541430660127,
1.08746358512433));
#19806=CARTESIAN_POINT('Ctrl Pts',(-0.129647464608677,-0.0507485213543897,
1.09540575324711));
#19807=CARTESIAN_POINT('Ctrl Pts',(-0.0276126195379174,-0.136460326620484,
1.10334792136989));
#19808=CARTESIAN_POINT('Ctrl Pts',(0.0997182217817603,-0.0971604536002107,
1.11129008949267));
#19809=CARTESIAN_POINT('Ctrl Pts',(0.135696927507188,0.0311483765905046,
1.11923225761545));
#19810=CARTESIAN_POINT('Ctrl Pts',(0.0473633069609982,0.130922093830007,
1.12717442573822));
#19811=CARTESIAN_POINT('Ctrl Pts',(-0.0843599685788644,0.110757722983492,
1.13511659386101));
#19812=CARTESIAN_POINT('Ctrl Pts',(-0.138800846271631,-0.0108721006891078,
1.14305876198379));
#19813=CARTESIAN_POINT('Ctrl Pts',(-0.0660858892268601,-0.122541963197144,
1.15100093010657));
#19814=CARTESIAN_POINT('Ctrl Pts',(0.0671705316110708,-0.121950798202395,
1.15894309822935));
#19815=CARTESIAN_POINT('Ctrl Pts',(0.138891844802359,-0.00964017357273747,
1.16688526635212));
#19816=CARTESIAN_POINT('Ctrl Pts',(0.0833739592533277,0.111501840422208,
1.17482743447491));
#19817=CARTESIAN_POINT('Ctrl Pts',(-0.0485230383040216,0.130496713571114,
1.18276960259768));
#19818=CARTESIAN_POINT('Ctrl Pts',(-0.135967947813762,0.0299431906521225,
1.19071177072047));
#19819=CARTESIAN_POINT('Ctrl Pts',(-0.0988522486080867,-0.0980413710850678,
1.19865393884324));
#19820=CARTESIAN_POINT('Ctrl Pts',(0.0288222657999454,-0.136209964735594,
1.20659610696603));
#19821=CARTESIAN_POINT('Ctrl Pts',(0.130092623711363,-0.0495962373069701,
1.21453827508881));
#19822=CARTESIAN_POINT('Ctrl Pts',(0.112184773380136,0.082452738709893,
1.22248044321158));
#19823=CARTESIAN_POINT('Ctrl Pts',(-0.00849585454694533,0.138966535376798,
1.23042261133437));
#19824=CARTESIAN_POINT('Ctrl Pts',(-0.121393406896754,0.0681727090639588,
1.23836477945715));
#19825=CARTESIAN_POINT('Ctrl Pts',(-0.123082127310551,-0.0650743223999996,
1.24630694757992));
#19826=CARTESIAN_POINT('Ctrl Pts',(-0.0120149744006178,-0.138706589206355,
1.25424911570271));
#19827=CARTESIAN_POINT('Ctrl Pts',(0.110059129405696,-0.0852693704304675,
1.26219128382548));
#19828=CARTESIAN_POINT('Ctrl Pts',(0.13130776387206,0.0462833517151888,
1.27013345194827));
#19829=CARTESIAN_POINT('Ctrl Pts',(0.0322649968732001,0.135435768819968,
1.27807562007105));
#19830=CARTESIAN_POINT('Ctrl Pts',(-0.0963358219719167,0.100515107841202,
1.28601778819382));
#19831=CARTESIAN_POINT('Ctrl Pts',(-0.136683130933199,-0.0264877182308561,
1.29395995631661));
#19832=CARTESIAN_POINT('Ctrl Pts',(-0.0518146499729274,-0.129225073214149,
1.30190212443939));
#19833=CARTESIAN_POINT('Ctrl Pts',(0.0805213734929343,-0.11357898534207,
1.30984429256217));
#19834=CARTESIAN_POINT('Ctrl Pts',(0.1390915465469,0.0061171215252809,1.31778646068495));
#19835=CARTESIAN_POINT('Ctrl Pts',(0.0702395735793815,0.120209316621791,
1.32572862880773));
#19836=CARTESIAN_POINT('Ctrl Pts',(-0.0629590648350173,0.124177428154433,
1.33367079693051));
#19837=CARTESIAN_POINT('Ctrl Pts',(-0.138480731711197,0.0143862582011507,
1.34161296505328));
#19838=CARTESIAN_POINT('Ctrl Pts',(-0.0871398218994898,-0.108584202098263,
1.34955513317607));
#19839=CARTESIAN_POINT('Ctrl Pts',(0.0440301174146577,-0.132080378229483,
1.35749730129884));
#19840=CARTESIAN_POINT('Ctrl Pts',(0.13486394497766,-0.0345773583278084,
1.36543946942163));
#19841=CARTESIAN_POINT('Ctrl Pts',(0.102148545386143,0.0946020732301706,
1.3733816375444));
#19842=CARTESIAN_POINT('Ctrl Pts',(-0.0241454188302812,0.137116288461919,
1.38132380566719));
#19843=CARTESIAN_POINT('Ctrl Pts',(-0.128319693277533,0.0540178939468163,
1.38926597378996));
#19844=CARTESIAN_POINT('Ctrl Pts',(-0.114939956470138,-0.0785664351508689,
1.39720814191275));
#19845=CARTESIAN_POINT('Ctrl Pts',(0.00373660876362508,-0.139175849115243,
1.40515031003553));
#19846=CARTESIAN_POINT('Ctrl Pts',(0.118990018389619,-0.0722858665142316,
1.41309247815831));
#19847=CARTESIAN_POINT('Ctrl Pts',(0.125236419206141,0.0608253567263532,
1.42103464628109));
#19848=CARTESIAN_POINT('Ctrl Pts',(0.0167532566496359,0.13821437898841,
1.42897681440387));
#19849=CARTESIAN_POINT('Ctrl Pts',(-0.107077349343502,0.0889846891406984,
1.43691898252665));
#19850=CARTESIAN_POINT('Ctrl Pts',(-0.132814597987359,-0.0417638487589672,
1.44486115064943));
#19851=CARTESIAN_POINT('Ctrl Pts',(-0.0368790902657646,-0.134252921254984,
1.45280331877221));
#19852=CARTESIAN_POINT('Ctrl Pts',(0.0928396680879532,-0.103751556080299,
1.46074548689499));
#19853=CARTESIAN_POINT('Ctrl Pts',(0.137511141307062,0.0217950526079239,
1.46868765501776));
#19854=CARTESIAN_POINT('Ctrl Pts',(0.0562018483347667,0.127378648737854,
1.47662982314055));
#19855=CARTESIAN_POINT('Ctrl Pts',(-0.0765818961642769,0.116263681173923,
1.48457199126332));
#19856=CARTESIAN_POINT('Ctrl Pts',(-0.13923195096087,-0.00134816270381636,
1.49251415938611));
#19857=CARTESIAN_POINT('Ctrl Pts',(-0.0742871760264013,-0.117748889605885,
1.50045632750888));
#19858=CARTESIAN_POINT('Ctrl Pts',(0.0586284551779338,-0.126233948370975,
1.50839849563167));
#19859=CARTESIAN_POINT('Ctrl Pts',(0.137995068118234,-0.019163470063063,
1.51634066375444));
#19860=CARTESIAN_POINT('Ctrl Pts',(0.0906261803825392,0.105639137646141,
1.52428283187723));
#19861=CARTESIAN_POINT('Ctrl Pts',(0.00417072711528833,0.124051375507138,
1.52957761062575));
#19862=CARTESIAN_POINT('Ctrl Pts',(-0.0334019664627544,0.1129391839063,
1.53222500000001));
#19863=CARTESIAN_POINT('Ctrl Pts',(-0.0551480035117261,0.114734422509858,
-0.0109985226280628));
#19864=CARTESIAN_POINT('Ctrl Pts',(-0.093317938433455,0.0963877427684319,
-0.00835113325380276));
#19865=CARTESIAN_POINT('Ctrl Pts',(-0.149247407742026,0.0189255452031589,
-0.00305635450528277));
#19866=CARTESIAN_POINT('Ctrl Pts',(-0.0966876253720675,-0.115446371588928,
0.00488581361749726));
#19867=CARTESIAN_POINT('Ctrl Pts',(0.0445747075563756,-0.143685636564375,
0.0128279817402772));
#19868=CARTESIAN_POINT('Ctrl Pts',(0.144936900801175,-0.0404809362687151,
0.0207701498630572));
#19869=CARTESIAN_POINT('Ctrl Pts',(0.112556116319125,0.0999057960529736,
0.0287123179858373));
#19870=CARTESIAN_POINT('Ctrl Pts',(-0.0229555792165621,0.148717415239805,
0.0366544861086172));
#19871=CARTESIAN_POINT('Ctrl Pts',(-0.137428156769908,0.0613155244327884,
0.0445966542313972));
#19872=CARTESIAN_POINT('Ctrl Pts',(-0.126007400730642,-0.0822718633254329,
0.0525388223541772));
#19873=CARTESIAN_POINT('Ctrl Pts',(0.000851700720621877,-0.150482305134309,
0.0604809904769572));
#19874=CARTESIAN_POINT('Ctrl Pts',(0.126929176276611,-0.0808394286734405,
0.0684231585997372));
#19875=CARTESIAN_POINT('Ctrl Pts',(0.136727213562698,0.0628627408439891,
0.0763653267225173));
#19876=CARTESIAN_POINT('Ctrl Pts',(0.0212686937255662,0.148975090584026,
0.0843074948452972));
#19877=CARTESIAN_POINT('Ctrl Pts',(-0.113673932864549,0.0986115272026031,
0.0922496629680772));
#19878=CARTESIAN_POINT('Ctrl Pts',(-0.144479665027646,-0.0420906285100245,
0.100191831090857));
#19879=CARTESIAN_POINT('Ctrl Pts',(-0.0429271251068198,-0.144233284958223,
0.108133999213637));
#19880=CARTESIAN_POINT('Ctrl Pts',(0.0979510420095061,-0.114243518700172,
0.116076167336417));
#19881=CARTESIAN_POINT('Ctrl Pts',(0.149096007275942,0.0204050915936607,
0.124018335459197));
#19882=CARTESIAN_POINT('Ctrl Pts',(0.0636537044864716,0.136360518400275,
0.131960503581977));
#19883=CARTESIAN_POINT('Ctrl Pts',(-0.0801019266996435,0.127395713772213,
0.139902671704757));
#19884=CARTESIAN_POINT('Ctrl Pts',(-0.15047596611352,0.00172334100814176,
0.147844839827537));
#19885=CARTESIAN_POINT('Ctrl Pts',(-0.0829985603893774,-0.125527785761544,
0.155787007950317));
#19886=CARTESIAN_POINT('Ctrl Pts',(0.0605140527882773,-0.137782566606816,
0.163729176073097));
#19887=CARTESIAN_POINT('Ctrl Pts',(0.148589577098441,-0.0238143605552183,
0.171671344195877));
#19888=CARTESIAN_POINT('Ctrl Pts',(0.100541783424623,0.111970245809892,
0.179613512318657));
#19889=CARTESIAN_POINT('Ctrl Pts',(-0.0396126128240685,0.145178604134651,
0.187555680441437));
#19890=CARTESIAN_POINT('Ctrl Pts',(-0.143477786216001,0.0453884461694337,
0.195497848564217));
#19891=CARTESIAN_POINT('Ctrl Pts',(-0.115902567375552,-0.095982191346566,
0.203440016686997));
#19892=CARTESIAN_POINT('Ctrl Pts',(0.0178513102906219,-0.149423281002214,
0.211382184809777));
#19893=CARTESIAN_POINT('Ctrl Pts',(0.135251553802876,-0.0659772944027704,
0.219324352932557));
#19894=CARTESIAN_POINT('Ctrl Pts',(0.128747479107914,0.07791067196398,0.227266521055337));
#19895=CARTESIAN_POINT('Ctrl Pts',(0.00429748682099232,0.150424458749874,
0.235208689178117));
#19896=CARTESIAN_POINT('Ctrl Pts',(-0.124089444892588,0.0851339876261335,
0.243150857300897));
#19897=CARTESIAN_POINT('Ctrl Pts',(-0.138797696890977,-0.0581479623084488,
0.251093025423677));
#19898=CARTESIAN_POINT('Ctrl Pts',(-0.0263529993083425,-0.148160405002171,
0.259035193546457));
#19899=CARTESIAN_POINT('Ctrl Pts',(0.110233752987369,-0.102442695616748,
0.266977361669237));
#19900=CARTESIAN_POINT('Ctrl Pts',(0.145835062802846,0.0371230472913779,
0.274919529792017));
#19901=CARTESIAN_POINT('Ctrl Pts',(0.0478364728857143,0.142680265085169,
0.282861697914797));
#19902=CARTESIAN_POINT('Ctrl Pts',(-0.0939852406223356,0.117527701960322,
0.290803866037577));
#19903=CARTESIAN_POINT('Ctrl Pts',(-0.14970681824969,-0.01529231023972,
0.298746034160357));
#19904=CARTESIAN_POINT('Ctrl Pts',(-0.0682815703945392,-0.134102995221473,
0.306688202283137));
#19905=CARTESIAN_POINT('Ctrl Pts',(0.0756966107742644,-0.1300615596562,
0.314630370405917));
#19906=CARTESIAN_POINT('Ctrl Pts',(0.150328919865546,-0.00687037371415525,
0.322572538528697));
#19907=CARTESIAN_POINT('Ctrl Pts',(0.0872444944832666,0.122614780370367,
0.330514706651477));
#19908=CARTESIAN_POINT('Ctrl Pts',(-0.0557648508131485,0.139772198940638,
0.338456874774257));
#19909=CARTESIAN_POINT('Ctrl Pts',(-0.147687863823926,0.0288839239377102,
0.346399042897038));
#19910=CARTESIAN_POINT('Ctrl Pts',(-0.104313621021262,-0.10846499275041,
0.354341211019817));
#19911=CARTESIAN_POINT('Ctrl Pts',(0.0346226151823369,-0.146448833047075,
0.362283379142597));
#19912=CARTESIAN_POINT('Ctrl Pts',(0.141840978962514,-0.0502704970123603,
0.370225547265377));
#19913=CARTESIAN_POINT('Ctrl Pts',(0.119118434135606,0.0919607787700563,
0.378167715388157));
#19914=CARTESIAN_POINT('Ctrl Pts',(-0.0127288338612142,0.149946533709345,
0.386109883510937));
#19915=CARTESIAN_POINT('Ctrl Pts',(-0.132915182358376,0.070565859178174,
0.394052051633717));
#19916=CARTESIAN_POINT('Ctrl Pts',(-0.131337568919768,-0.0734603918663599,
0.401994219756497));
#19917=CARTESIAN_POINT('Ctrl Pts',(-0.00944124952954395,-0.150189377088511,
0.409936387879277));
#19918=CARTESIAN_POINT('Ctrl Pts',(0.121104224366159,-0.0893294633566384,
0.417878556002057));
#19919=CARTESIAN_POINT('Ctrl Pts',(0.140705787232781,0.0533654159743681,
0.425820724124838));
#19920=CARTESIAN_POINT('Ctrl Pts',(0.0314063937394313,0.147172091835368,
0.433762892247617));
#19921=CARTESIAN_POINT('Ctrl Pts',(-0.106664482920656,0.106154012011714,
0.441705060370398));
#19922=CARTESIAN_POINT('Ctrl Pts',(-0.147019735166745,-0.032112048430678,
0.449647228493177));
#19923=CARTESIAN_POINT('Ctrl Pts',(-0.052689806088835,-0.14096017351449,
0.457589396615958));
#19924=CARTESIAN_POINT('Ctrl Pts',(0.0899093983958942,-0.120674298270189,
0.465531564738737));
#19925=CARTESIAN_POINT('Ctrl Pts',(0.15014235720654,0.0101616315312987,
0.473473732861518));
#19926=CARTESIAN_POINT('Ctrl Pts',(0.0728294921055832,0.131688462906045,
0.481415900984297));
#19927=CARTESIAN_POINT('Ctrl Pts',(-0.071202669822089,0.132575133389036,
0.489358069107078));
#19928=CARTESIAN_POINT('Ctrl Pts',(-0.150005871264529,0.012009361726732,
0.497300237229857));
#19929=CARTESIAN_POINT('Ctrl Pts',(-0.0913882839399832,-0.119558219045865,
0.505242405352637));
#19930=CARTESIAN_POINT('Ctrl Pts',(0.0509503601487159,-0.141598188489932,
0.513184573475417));
#19931=CARTESIAN_POINT('Ctrl Pts',(0.146613240011817,-0.0339196703426114,
0.521126741598197));
#19932=CARTESIAN_POINT('Ctrl Pts',(0.107963329873666,0.104832750538675,
0.529068909720978));
#19933=CARTESIAN_POINT('Ctrl Pts',(-0.0295920819230583,0.147547602048875,
0.537011077843756));
#19934=CARTESIAN_POINT('Ctrl Pts',(-0.140038106568177,0.055093691941219,
0.544953245966537));
#19935=CARTESIAN_POINT('Ctrl Pts',(-0.122194838935542,-0.0878316999746162,
0.552895414089317));
#19936=CARTESIAN_POINT('Ctrl Pts',(0.00759145471482065,-0.150294231420327,
0.560837582212097));
#19937=CARTESIAN_POINT('Ctrl Pts',(0.130423195946632,-0.0750718065719766,
0.568779750334878));
#19938=CARTESIAN_POINT('Ctrl Pts',(0.133773890807325,0.0689241055160235,
0.576721918457657));
#19939=CARTESIAN_POINT('Ctrl Pts',(0.0145739585745413,0.149778456108953,
0.584664086580438));
#19940=CARTESIAN_POINT('Ctrl Pts',(-0.117977216952174,0.0934203535806499,
0.592606254703216));
#19941=CARTESIAN_POINT('Ctrl Pts',(-0.142449141490696,-0.0485203902651028,
0.600548422825998));
#19942=CARTESIAN_POINT('Ctrl Pts',(-0.036423018067407,-0.146011471938939,
0.608490590948776));
#19943=CARTESIAN_POINT('Ctrl Pts',(0.102970331784443,-0.109741044988262,
0.616432759071558));
#19944=CARTESIAN_POINT('Ctrl Pts',(0.148032279177632,0.0270634532975707,
0.624374927194337));
#19945=CARTESIAN_POINT('Ctrl Pts',(0.0574814509102497,0.139075048028633,
0.632317095317117));
#19946=CARTESIAN_POINT('Ctrl Pts',(-0.0857282916847416,0.123679611042927,
0.640259263439898));
#19947=CARTESIAN_POINT('Ctrl Pts',(-0.150402111894479,-0.00501905574730406,
0.648201431562677));
#19948=CARTESIAN_POINT('Ctrl Pts',(-0.0772921462128499,-0.129119751845818,
0.656143599685457));
#19949=CARTESIAN_POINT('Ctrl Pts',(0.0666253659236285,-0.134933490277457,
0.664085767808237));
#19950=CARTESIAN_POINT('Ctrl Pts',(0.14950719819016,-0.0171342893707992,
0.672027935931017));
#19951=CARTESIAN_POINT('Ctrl Pts',(0.0954250774564579,0.11636168087194,
0.679970104053797));
#19952=CARTESIAN_POINT('Ctrl Pts',(-0.0460762176180427,0.143258397146306,
0.687912272176577));
#19953=CARTESIAN_POINT('Ctrl Pts',(-0.145366963764729,0.0389157041403328,
0.695854440299358));
#19954=CARTESIAN_POINT('Ctrl Pts',(-0.111486636987321,-0.101077771820372,
0.703796608422136));
#19955=CARTESIAN_POINT('Ctrl Pts',(0.02452690272786,-0.148473624679578,
0.711738776544918));
#19956=CARTESIAN_POINT('Ctrl Pts',(0.138071279799868,-0.0598523840572839,
0.719680944667696));
#19957=CARTESIAN_POINT('Ctrl Pts',(0.125128179973684,0.0835997892305201,
0.727623112790477));
#19958=CARTESIAN_POINT('Ctrl Pts',(-0.00244518761474098,0.150465967050502,
0.735565280913257));
#19959=CARTESIAN_POINT('Ctrl Pts',(-0.127778512144395,0.0794898610961098,
0.743507449036036));
#19960=CARTESIAN_POINT('Ctrl Pts',(-0.136053592364468,-0.0643071239260258,
0.751449617158818));
#19961=CARTESIAN_POINT('Ctrl Pts',(-0.019689604662082,-0.149192176910068,
0.759391785281597));
#19962=CARTESIAN_POINT('Ctrl Pts',(0.114712083700712,-0.0974018687498071,
0.767333953404378));
#19963=CARTESIAN_POINT('Ctrl Pts',(0.144025718573537,0.0436185576594447,
0.775276121527157));
#19964=CARTESIAN_POINT('Ctrl Pts',(0.0413969989087525,0.14467990414796,
0.783218289649938));
#19965=CARTESIAN_POINT('Ctrl Pts',(-0.0991556246317344,0.113199594905656,
0.791160457772717));
#19966=CARTESIAN_POINT('Ctrl Pts',(-0.148871509365196,-0.021983172706469,
0.799102625895497));
#19967=CARTESIAN_POINT('Ctrl Pts',(-0.062205797368885,-0.137027095702329,
0.807044794018277));
#19968=CARTESIAN_POINT('Ctrl Pts',(0.081446815661698,-0.126540121706451,
0.814986962141057));
#19969=CARTESIAN_POINT('Ctrl Pts',(0.150485778196879,-0.000129396266831759,
0.822929130263837));
#19970=CARTESIAN_POINT('Ctrl Pts',(0.0816643079123276,0.126399869446589,
0.830871298386618));
#19971=CARTESIAN_POINT('Ctrl Pts',(-0.0619700581130299,0.137133869194964,
0.838813466509397));
#19972=CARTESIAN_POINT('Ctrl Pts',(-0.148833484480893,0.0222391564630926,
0.846755634632177));
#19973=CARTESIAN_POINT('Ctrl Pts',(-0.0993501488194509,-0.113028908304323,
0.854697802754957));
#19974=CARTESIAN_POINT('Ctrl Pts',(0.041148129789194,-0.144750881164039,
0.862639970877736));
#19975=CARTESIAN_POINT('Ctrl Pts',(0.143950494202948,-0.0438661760544617,
0.870582139000517));
#19976=CARTESIAN_POINT('Ctrl Pts',(0.114879417330645,0.0972044528644933,
0.878524307123298));
#19977=CARTESIAN_POINT('Ctrl Pts',(-0.0194330078274841,0.149225816766708,
0.886466475246077));
#19978=CARTESIAN_POINT('Ctrl Pts',(-0.135942801386891,0.0645410019599824,
0.894408643368857));
#19979=CARTESIAN_POINT('Ctrl Pts',(-0.127915022941288,-0.0792700011911429,
0.902350811491637));
#19980=CARTESIAN_POINT('Ctrl Pts',(-0.00270394227186439,-0.150461539534541,
0.910292979614417));
#19981=CARTESIAN_POINT('Ctrl Pts',(0.124984227305131,-0.0838148501630433,
0.918235147737197));
#19982=CARTESIAN_POINT('Ctrl Pts',(0.138174004553101,0.0596148525845174,
0.926177315859977));
#19983=CARTESIAN_POINT('Ctrl Pts',(0.0247821984756025,0.148431225898158,
0.934119483982757));
#19984=CARTESIAN_POINT('Ctrl Pts',(-0.11131264737753,0.101269347369872,
0.942061652105537));
#19985=CARTESIAN_POINT('Ctrl Pts',(-0.145433672650089,-0.0386656571445607,
0.950003820228317));
#19986=CARTESIAN_POINT('Ctrl Pts',(-0.0463225128062989,-0.143178947440692,
0.957945988351097));
#19987=CARTESIAN_POINT('Ctrl Pts',(0.0952248276606132,-0.116525612549003,
0.965888156473877));
#19988=CARTESIAN_POINT('Ctrl Pts',(0.149536443172165,0.0168771545685866,
0.973830324596656));
#19989=CARTESIAN_POINT('Ctrl Pts',(0.0668573142755158,0.134818714245386,
0.981772492719438));
#19990=CARTESIAN_POINT('Ctrl Pts',(-0.0770699830103684,0.129252481220654,
0.989714660842216));
#19991=CARTESIAN_POINT('Ctrl Pts',(-0.15039325815857,0.00527769678589187,
0.997656828964997));
#19992=CARTESIAN_POINT('Ctrl Pts',(-0.0859408583470751,-0.123532000103139,
1.00559899708778));
#19993=CARTESIAN_POINT('Ctrl Pts',(0.0572421967501742,-0.139173693973137,
1.01354116521056));
#19994=CARTESIAN_POINT('Ctrl Pts',(0.147985518909957,-0.0273179863069172,
1.02148333333334));
#19995=CARTESIAN_POINT('Ctrl Pts',(0.103158902618224,0.109563803299803,
1.02942550145612));
#19996=CARTESIAN_POINT('Ctrl Pts',(-0.0361718663885326,0.146073893166727,
1.0373676695789));
#19997=CARTESIAN_POINT('Ctrl Pts',(-0.142365489706367,0.0487652901517079,
1.04530983770168));
#19998=CARTESIAN_POINT('Ctrl Pts',(-0.118137698690712,-0.0932173284908804,
1.05325200582446));
#19999=CARTESIAN_POINT('Ctrl Pts',(0.0143163610725534,-0.149803297655807,
1.06119417394724));
#20000=CARTESIAN_POINT('Ctrl Pts',(0.133655163317704,-0.0691540562905145,
1.06913634207002));
#20001=CARTESIAN_POINT('Ctrl Pts',(0.130552105047211,0.0748474051030229,
1.0770785101928));
#20002=CARTESIAN_POINT('Ctrl Pts',(0.0078499064261323,0.150280954056111,
1.08502067831558));
#20003=CARTESIAN_POINT('Ctrl Pts',(-0.122043612932812,0.0880417101447944,
1.09296284643836));
#20004=CARTESIAN_POINT('Ctrl Pts',(-0.140132644828567,-0.0548527851276936,
1.10090501456114));
#20005=CARTESIAN_POINT('Ctrl Pts',(-0.0298457776877653,-0.147496493982489,
1.10884718268392));
#20006=CARTESIAN_POINT('Ctrl Pts',(0.107782887988268,-0.10501826145877,
1.1167893508067));
#20007=CARTESIAN_POINT('Ctrl Pts',(0.146671355310253,0.033667487497105,
1.12473151892948));
#20008=CARTESIAN_POINT('Ctrl Pts',(0.0511937930472066,0.141510359113225,
1.13267368705226));
#20009=CARTESIAN_POINT('Ctrl Pts',(-0.0911825429852659,0.119715203870077,
1.14061585517504));
#20010=CARTESIAN_POINT('Ctrl Pts',(-0.150026302104679,-0.0117513769282424,
1.14855802329782));
#20011=CARTESIAN_POINT('Ctrl Pts',(-0.0714305557085884,-0.132452489195471,
1.1565001914206));
#20012=CARTESIAN_POINT('Ctrl Pts',(0.0726029180563751,-0.131813513998426,
1.16444235954338));
#20013=CARTESIAN_POINT('Ctrl Pts',(0.150124660100533,-0.010419818262018,
1.17238452766616));
#20014=CARTESIAN_POINT('Ctrl Pts',(0.0901167906002831,0.120519501471002,
1.18032669578894));
#20015=CARTESIAN_POINT('Ctrl Pts',(-0.0524473171394798,0.141050576417769,
1.18826886391172));
#20016=CARTESIAN_POINT('Ctrl Pts',(-0.146964294261872,0.0323648326895764,
1.1962110320345));
#20017=CARTESIAN_POINT('Ctrl Pts',(-0.106846879624786,-0.105970422747861,
1.20415320015727));
#20018=CARTESIAN_POINT('Ctrl Pts',(0.0311532535456026,-0.14722588419309,
1.21209536828006));
#20019=CARTESIAN_POINT('Ctrl Pts',(0.140613805972886,-0.0536073106276968,
1.22003753640283));
#20020=CARTESIAN_POINT('Ctrl Pts',(0.121257666323848,0.0891210667609394,
1.22797970452562));
#20021=CARTESIAN_POINT('Ctrl Pts',(-0.00918295295119051,0.150205391241489,
1.2359218726484));
#20022=CARTESIAN_POINT('Ctrl Pts',(-0.131211043922368,0.0736861461587066,
1.24386404077118));
#20023=CARTESIAN_POINT('Ctrl Pts',(-0.133036338837895,-0.0703371788708997,
1.25180620889396));
#20024=CARTESIAN_POINT('Ctrl Pts',(-0.0129866800356469,-0.149924422041766,
1.25974837701674));
#20025=CARTESIAN_POINT('Ctrl Pts',(0.118960111851797,-0.0921654923014072,
1.26769054513952));
#20026=CARTESIAN_POINT('Ctrl Pts',(0.141927220045961,0.050026496908035,
1.2756327132623));
#20027=CARTESIAN_POINT('Ctrl Pts',(0.0348744139414821,0.146389075532006,
1.28357488138508));
#20028=CARTESIAN_POINT('Ctrl Pts',(-0.104126938119509,0.108644221848311,
1.29151704950786));
#20029=CARTESIAN_POINT('Ctrl Pts',(-0.147737317493493,-0.0286299004949125,
1.29945921763064));
#20030=CARTESIAN_POINT('Ctrl Pts',(-0.0560051364173496,-0.139676092720537,
1.30740138575342));
#20031=CARTESIAN_POINT('Ctrl Pts',(0.0870335032532438,-0.122764634549313,
1.3153435538762));
#20032=CARTESIAN_POINT('Ctrl Pts',(0.150340512633584,0.00661184096937889,
1.32328572199898));
#20033=CARTESIAN_POINT('Ctrl Pts',(0.0759201674095095,0.129931190880528,
1.33122789012176));
#20034=CARTESIAN_POINT('Ctrl Pts',(-0.0680508508044829,0.134220221643466,
1.33917005824454));
#20035=CARTESIAN_POINT('Ctrl Pts',(-0.149680298423566,0.0155497403439283,
1.34711222636732));
#20036=CARTESIAN_POINT('Ctrl Pts',(-0.0941872156892785,-0.117365900463673,
1.3550543944901));
#20037=CARTESIAN_POINT('Ctrl Pts',(0.0475910332998192,-0.142762319241037,
1.36299656261288));
#20038=CARTESIAN_POINT('Ctrl Pts',(0.145771005694385,-0.0373737865856905,
1.37093873073566));
#20039=CARTESIAN_POINT('Ctrl Pts',(0.110409762917901,0.10225297323032,1.37888089885844));
#20040=CARTESIAN_POINT('Ctrl Pts',(-0.0260981686868614,0.148205506441964,
1.38682306698121));
#20041=CARTESIAN_POINT('Ctrl Pts',(-0.138697490589939,0.0583865667538053,
1.394765235104));
#20042=CARTESIAN_POINT('Ctrl Pts',(-0.124235673603468,-0.0849204601545819,
1.40270740322677));
#20043=CARTESIAN_POINT('Ctrl Pts',(0.0040388053119065,-0.150431633134115,
1.41064957134956));
#20044=CARTESIAN_POINT('Ctrl Pts',(0.12861328245382,-0.0781319533624403,
1.41859173947234));
#20045=CARTESIAN_POINT('Ctrl Pts',(0.1353648581188,0.0657445800149866,1.42653390759512));
#20046=CARTESIAN_POINT('Ctrl Pts',(0.0181081687242482,0.149392404544468,
1.43447607571789));
#20047=CARTESIAN_POINT('Ctrl Pts',(-0.115737181672069,0.0961812857364522,
1.44241824384068));
#20048=CARTESIAN_POINT('Ctrl Pts',(-0.143555918690644,-0.0451414811888502,
1.45036041196346));
#20049=CARTESIAN_POINT('Ctrl Pts',(-0.0398616700558823,-0.145110565703753,
1.45830258008624));
#20050=CARTESIAN_POINT('Ctrl Pts',(0.100348034367198,-0.112142416378873,
1.46624474820902));
#20051=CARTESIAN_POINT('Ctrl Pts',(0.14863229283285,0.0235577176564554,
1.4741869163318));
#20052=CARTESIAN_POINT('Ctrl Pts',(0.0607471474677608,0.137680339497592,
1.48212908445458));
#20053=CARTESIAN_POINT('Ctrl Pts',(-0.0827754224726193,0.125666453945577,
1.49007125257736));
#20054=CARTESIAN_POINT('Ctrl Pts',(-0.150492272191201,-0.00145719475437189,
1.49801342070014));
#20055=CARTESIAN_POINT('Ctrl Pts',(-0.0802951178786721,-0.12727177793954,
1.50595558882292));
#20056=CARTESIAN_POINT('Ctrl Pts',(0.0633700050447994,-0.136443062004882,
1.5138977569457));
#20057=CARTESIAN_POINT('Ctrl Pts',(0.149155357006591,-0.0207133070603065,
1.52183992506848));
#20058=CARTESIAN_POINT('Ctrl Pts',(0.0979555318420461,0.114182655252422,
1.52978209319126));
#20059=CARTESIAN_POINT('Ctrl Pts',(0.00450803278943675,0.134083974545181,
1.53507687193978));
#20060=CARTESIAN_POINT('Ctrl Pts',(-0.0361033354337414,0.122073089461022,
1.53772426131404));
#20061=CARTESIAN_POINT('Ctrl Pts',(-0.0592743564846203,0.123319225136773,
-0.00549926131403157));
#20062=CARTESIAN_POINT('Ctrl Pts',(-0.100300290071938,0.10359978715075,
-0.00285187193977157));
#20063=CARTESIAN_POINT('Ctrl Pts',(-0.160414584165772,0.0203416160441626,
0.00244290680874841));
#20064=CARTESIAN_POINT('Ctrl Pts',(-0.103922107946056,-0.124084444561314,
0.0103850749315284));
#20065=CARTESIAN_POINT('Ctrl Pts',(0.0479099321398382,-0.154436663180837,
0.0183272430543084));
#20066=CARTESIAN_POINT('Ctrl Pts',(0.155781551077148,-0.0435098515708298,
0.0262694111770884));
#20067=CARTESIAN_POINT('Ctrl Pts',(0.120977930992648,0.107381072623318,
0.0342115792998684));
#20068=CARTESIAN_POINT('Ctrl Pts',(-0.0246731903087699,0.159844935900913,
0.0421537474226484));
#20069=CARTESIAN_POINT('Ctrl Pts',(-0.147710978397823,0.0659033513787588,
0.0500959155454284));
#20070=CARTESIAN_POINT('Ctrl Pts',(-0.135435684249567,-0.0884277117007276,
0.0580380836682085));
#20071=CARTESIAN_POINT('Ctrl Pts',(0.000915427738408385,-0.16174188059703,
0.0659802517909884));
#20072=CARTESIAN_POINT('Ctrl Pts',(0.13642643003965,-0.0868880976295618,
0.0739224199137684));
#20073=CARTESIAN_POINT('Ctrl Pts',(0.146957588340267,0.0675663355536457,
0.0818645880365484));
#20074=CARTESIAN_POINT('Ctrl Pts',(0.0228600865593111,0.160121891352391,
0.0898067561593285));
#20075=CARTESIAN_POINT('Ctrl Pts',(-0.122179386207322,0.105989962368389,
0.0977489242821083));
#20076=CARTESIAN_POINT('Ctrl Pts',(-0.155290103436038,-0.0452399862206161,
0.105691092404888));
#20077=CARTESIAN_POINT('Ctrl Pts',(-0.0461390722131997,-0.155025288408554,
0.113633260527668));
#20078=CARTESIAN_POINT('Ctrl Pts',(0.105280057525145,-0.122791590307548,
0.121575428650448));
#20079=CARTESIAN_POINT('Ctrl Pts',(0.160251855424436,0.0219318669073289,
0.129517596773229));
#20080=CARTESIAN_POINT('Ctrl Pts',(0.0684164816681947,0.146563455853242,
0.137459764896008));
#20081=CARTESIAN_POINT('Ctrl Pts',(-0.086095413359615,0.136927875387926,
0.145401933018789));
#20082=CARTESIAN_POINT('Ctrl Pts',(-0.16173506727009,0.00185228698694943,
0.153344101141568));
#20083=CARTESIAN_POINT('Ctrl Pts',(-0.0892087826023274,-0.134920182928699,
0.161286269264348));
#20084=CARTESIAN_POINT('Ctrl Pts',(0.0650419110192955,-0.148091906331324,
0.169228437387128));
#20085=CARTESIAN_POINT('Ctrl Pts',(0.159707532494063,-0.025596228460074,
0.177170605509908));
#20086=CARTESIAN_POINT('Ctrl Pts',(0.108064646638443,0.120348223746572,
0.185112773632688));
#20087=CARTESIAN_POINT('Ctrl Pts',(-0.0425765573421325,0.156041339440091,
0.193054941755468));
#20088=CARTESIAN_POINT('Ctrl Pts',(-0.154213260793436,0.0487845573223287,
0.200997109878248));
#20089=CARTESIAN_POINT('Ctrl Pts',(-0.124574774400312,-0.103163891052585,
0.208939278001028));
#20090=CARTESIAN_POINT('Ctrl Pts',(0.0191870033818907,-0.160603616835255,
0.216881446123808));
#20091=CARTESIAN_POINT('Ctrl Pts',(0.145371514918136,-0.0709139301387177,
0.224823614246588));
#20092=CARTESIAN_POINT('Ctrl Pts',(0.138380784202201,0.0837402018183176,
0.232765782369368));
#20093=CARTESIAN_POINT('Ctrl Pts',(0.00461903876105218,0.161679705957985,
0.240707950492149));
#20094=CARTESIAN_POINT('Ctrl Pts',(-0.133374220718213,0.0915039894496894,
0.248650118614928));
#20095=CARTESIAN_POINT('Ctrl Pts',(-0.149182991964712,-0.0624987819548612,
0.256592286737709));
#20096=CARTESIAN_POINT('Ctrl Pts',(-0.0283248164207669,-0.159246248345813,
0.264534454860488));
#20097=CARTESIAN_POINT('Ctrl Pts',(0.118481800883715,-0.110107791262854,
0.272476622983269));
#20098=CARTESIAN_POINT('Ctrl Pts',(0.156746916480749,0.0399007144198201,
0.280418791106048));
#20099=CARTESIAN_POINT('Ctrl Pts',(0.0514157533588968,0.153356066537929,
0.288360959228829));
#20100=CARTESIAN_POINT('Ctrl Pts',(-0.101017521980764,0.126321506839912,
0.296303127351608));
#20101=CARTESIAN_POINT('Ctrl Pts',(-0.160908369261695,-0.0164365306249019,
0.304245295474388));
#20102=CARTESIAN_POINT('Ctrl Pts',(-0.0733906195540655,-0.144137017448375,
0.312187463597168));
#20103=CARTESIAN_POINT('Ctrl Pts',(0.0813604773699057,-0.13979318853071,
0.320129631719948));
#20104=CARTESIAN_POINT('Ctrl Pts',(0.161577018543625,-0.00738443741900211,
0.328071799842729));
#20105=CARTESIAN_POINT('Ctrl Pts',(0.0937724112935796,0.131789217000595,
0.336013967965508));
#20106=CARTESIAN_POINT('Ctrl Pts',(-0.0599373583072218,0.150230409426965,
0.343956136088289));
#20107=CARTESIAN_POINT('Ctrl Pts',(-0.158738350099833,0.0310451130618767,
0.351898304211068));
#20108=CARTESIAN_POINT('Ctrl Pts',(-0.112118705390683,-0.116580696253536,
0.359840472333849));
#20109=CARTESIAN_POINT('Ctrl Pts',(0.0372131918485748,-0.15740661101073,
0.367782640456628));
#20110=CARTESIAN_POINT('Ctrl Pts',(0.152453982298084,-0.0540318990865351,
0.375724808579408));
#20111=CARTESIAN_POINT('Ctrl Pts',(0.128031262769868,0.0988415833088236,
0.383666976702188));
#20112=CARTESIAN_POINT('Ctrl Pts',(-0.0136812466069205,0.161166021011634,
0.391609144824968));
#20113=CARTESIAN_POINT('Ctrl Pts',(-0.142860328563903,0.0758458262533652,
0.399551312947749));
#20114=CARTESIAN_POINT('Ctrl Pts',(-0.141164672957165,-0.0789569372907697,
0.407493481070528));
#20115=CARTESIAN_POINT('Ctrl Pts',(-0.0101476745237983,-0.161427034722196,
0.415435649193308));
#20116=CARTESIAN_POINT('Ctrl Pts',(0.130165636283581,-0.0960133843187101,
0.423377817316089));
#20117=CARTESIAN_POINT('Ctrl Pts',(0.151233851831306,0.0573583899504574,
0.431319985438868));
#20118=CARTESIAN_POINT('Ctrl Pts',(0.0337563222576384,0.158183986373718,
0.439262153561649));
#20119=CARTESIAN_POINT('Ctrl Pts',(-0.114645466422773,0.114096800420287,
0.447204321684428));
#20120=CARTESIAN_POINT('Ctrl Pts',(-0.158020229883659,-0.0345147763277912,
0.455146489807208));
#20121=CARTESIAN_POINT('Ctrl Pts',(-0.0566322287360923,-0.151507272121918,
0.463088657929988));
#20122=CARTESIAN_POINT('Ctrl Pts',(0.0966367119836487,-0.129703541718919,
0.471030826052768));
#20123=CARTESIAN_POINT('Ctrl Pts',(0.161376496659739,0.0109219578497271,
0.478972994175549));
#20124=CARTESIAN_POINT('Ctrl Pts',(0.0782788315581001,0.141541821972661,
0.486915162298328));
#20125=CARTESIAN_POINT('Ctrl Pts',(-0.0765302851406724,0.142494836024782,
0.494857330421108));
#20126=CARTESIAN_POINT('Ctrl Pts',(-0.161229798395673,0.0129079412274925,
0.502799498543889));
#20127=CARTESIAN_POINT('Ctrl Pts',(-0.0982262525537151,-0.128503953817366,
0.510741666666668));
#20128=CARTESIAN_POINT('Ctrl Pts',(0.0547626317937811,-0.152193025452748,
0.518683834789449));
#20129=CARTESIAN_POINT('Ctrl Pts',(0.157583319439253,-0.0364576503898468,
0.526626002912228));
#20130=CARTESIAN_POINT('Ctrl Pts',(0.116041497328862,0.112676677866884,
0.534568171035008));
#20131=CARTESIAN_POINT('Ctrl Pts',(-0.0318062577307366,0.158587593482618,
0.542510339157789));
#20132=CARTESIAN_POINT('Ctrl Pts',(-0.150516213127973,0.0592159811457737,
0.550452507280567));
#20133=CARTESIAN_POINT('Ctrl Pts',(-0.131337854181896,-0.0944035534094825,
0.558394675403349));
#20134=CARTESIAN_POINT('Ctrl Pts',(0.00815947204521347,-0.161539734596121,
0.566336843526128));
#20135=CARTESIAN_POINT('Ctrl Pts',(0.140181883624494,-0.080688923285235,
0.574279011648909));
#20136=CARTESIAN_POINT('Ctrl Pts',(0.143783288371658,0.0740812312429708,
0.582221179771688));
#20137=CARTESIAN_POINT('Ctrl Pts',(0.0156644295519346,0.160985367298567,
0.590163347894469));
#20138=CARTESIAN_POINT('Ctrl Pts',(-0.126804656005353,0.100410368253513,
0.598105516017247));
#20139=CARTESIAN_POINT('Ctrl Pts',(-0.153107649524464,-0.0521508436608248,
0.606047684140029));
#20140=CARTESIAN_POINT('Ctrl Pts',(-0.0391483067326994,-0.156936525122116,
0.613989852262808));
#20141=CARTESIAN_POINT('Ctrl Pts',(0.110674906884577,-0.117952226869747,
0.621932020385589));
#20142=CARTESIAN_POINT('Ctrl Pts',(0.159108535730396,0.0290884288879846,
0.629874188508368));
#20143=CARTESIAN_POINT('Ctrl Pts',(0.061782400006242,0.14948109541648,0.637816356631148));
#20144=CARTESIAN_POINT('Ctrl Pts',(-0.0921427612707386,0.132933721767072,
0.645758524753929));
#20145=CARTESIAN_POINT('Ctrl Pts',(-0.161655687038194,-0.0053945978210935,
0.653700692876707));
#20146=CARTESIAN_POINT('Ctrl Pts',(-0.0830753959589387,-0.138780911597048,
0.661642860999489));
#20147=CARTESIAN_POINT('Ctrl Pts',(0.0716104924784035,-0.145029652845349,
0.669585029122267));
#20148=CARTESIAN_POINT('Ctrl Pts',(0.160693812980115,-0.0184163326249747,
0.677527197245049));
#20149=CARTESIAN_POINT('Ctrl Pts',(0.102565092089392,0.125068240261613,
0.685469365367828));
#20150=CARTESIAN_POINT('Ctrl Pts',(-0.0495237900674707,0.153977456320057,
0.693411533490608));
#20151=CARTESIAN_POINT('Ctrl Pts',(-0.156243792750268,0.0418275036842162,
0.701353701613389));
#20152=CARTESIAN_POINT('Ctrl Pts',(-0.119828429739121,-0.108640739429086,
0.709295869736167));
#20153=CARTESIAN_POINT('Ctrl Pts',(0.0263620853553792,-0.159582904138124,
0.717238037858949));
#20154=CARTESIAN_POINT('Ctrl Pts',(0.148402221984423,-0.0643307340819919,
0.725180205981728));
#20155=CARTESIAN_POINT('Ctrl Pts',(0.134490677336207,0.0898549973406614,
0.733122374104509));
#20156=CARTESIAN_POINT('Ctrl Pts',(-0.00262814450422035,0.161724320044658,
0.741064542227287));
#20157=CARTESIAN_POINT('Ctrl Pts',(-0.137339315979238,0.0854375510170853,
0.749006710350069));
#20158=CARTESIAN_POINT('Ctrl Pts',(-0.146233564613262,-0.0691187920752458,
0.756948878472847));
#20159=CARTESIAN_POINT('Ctrl Pts',(-0.0211628449166461,-0.160355220783347,
0.764891046595629));
#20160=CARTESIAN_POINT('Ctrl Pts',(0.12329521486528,-0.104689793336152,
0.772833214718408));
#20161=CARTESIAN_POINT('Ctrl Pts',(0.154802191231926,0.0468822399980663,
0.780775382841188));
#20162=CARTESIAN_POINT('Ctrl Pts',(0.0444944569967772,0.155505325098544,
0.788717550963968));
#20163=CARTESIAN_POINT('Ctrl Pts',(-0.106574770936664,0.121669556739719,
0.796659719086747));
#20164=CARTESIAN_POINT('Ctrl Pts',(-0.160010559849905,-0.0236280251811701,
0.804601887209529));
#20165=CARTESIAN_POINT('Ctrl Pts',(-0.0668602374312443,-0.147279908636853,
0.812544055332307));
#20166=CARTESIAN_POINT('Ctrl Pts',(0.0875409312876049,-0.13600826514128,
0.820486223455089));
#20167=CARTESIAN_POINT('Ctrl Pts',(0.161745613525436,-0.000139078116330951,
0.828428391577867));
#20168=CARTESIAN_POINT('Ctrl Pts',(0.0877746970157421,0.135857518751215,
0.836370559700649));
#20169=CARTESIAN_POINT('Ctrl Pts',(-0.0666068593976089,0.147394671269449,
0.844312727823428));
#20170=CARTESIAN_POINT('Ctrl Pts',(-0.159969689820096,0.0239031624749592,
0.852254895946208));
#20171=CARTESIAN_POINT('Ctrl Pts',(-0.106783850056725,-0.121486098811777,
0.860197064068988));
#20172=CARTESIAN_POINT('Ctrl Pts',(0.0442269666803361,-0.155581612845794,
0.868139232191768));
#20173=CARTESIAN_POINT('Ctrl Pts',(0.154721338329289,-0.0471483860066884,
0.876081400314548));
#20174=CARTESIAN_POINT('Ctrl Pts',(0.123475068941597,0.104477606152275,
0.884023568437328));
#20175=CARTESIAN_POINT('Ctrl Pts',(-0.0208870486723946,0.160391377683462,
0.891965736560109));
#20176=CARTESIAN_POINT('Ctrl Pts',(-0.146114483894434,0.0693701696243073,
0.899907904682887));
#20177=CARTESIAN_POINT('Ctrl Pts',(-0.137486040957907,-0.0852012404790134,
0.907850072805669));
#20178=CARTESIAN_POINT('Ctrl Pts',(-0.00290626002629624,-0.161719561247554,
0.915792240928448));
#20179=CARTESIAN_POINT('Ctrl Pts',(0.134335953660838,-0.0900861498315643,
0.923734409051229));
#20180=CARTESIAN_POINT('Ctrl Pts',(0.148512632937768,0.0640754297319473,
0.931676577174007));
#20181=CARTESIAN_POINT('Ctrl Pts',(0.0266364831612253,0.159537332941991,
0.939618745296788));
#20182=CARTESIAN_POINT('Ctrl Pts',(-0.119641421660886,0.10884664928423,
0.947560913419568));
#20183=CARTESIAN_POINT('Ctrl Pts',(-0.156315493011378,-0.0415587473590326,
0.955503081542348));
#20184=CARTESIAN_POINT('Ctrl Pts',(-0.0497885138626987,-0.153892061929087,
0.963445249665127));
#20185=CARTESIAN_POINT('Ctrl Pts',(0.102349858952582,-0.125244437839883,
0.971387417787908));
#20186=CARTESIAN_POINT('Ctrl Pts',(0.160725246166783,0.018139958160622,
0.979329585910688));
#20187=CARTESIAN_POINT('Ctrl Pts',(0.0718597959603077,0.14490628889729,
0.987271754033468));
#20188=CARTESIAN_POINT('Ctrl Pts',(-0.0828366097831417,0.138923572215364,
0.995213922156248));
#20189=CARTESIAN_POINT('Ctrl Pts',(-0.161646170836971,0.00567259122332548,
1.00315609027903));
#20190=CARTESIAN_POINT('Ctrl Pts',(-0.0923712328620446,-0.132775066096718,
1.01109825840181));
#20191=CARTESIAN_POINT('Ctrl Pts',(0.0615252440718216,-0.149587122371362,
1.01904042652459));
#20192=CARTESIAN_POINT('Ctrl Pts',(0.159058276707423,-0.0293620068848675,
1.02698259464737));
#20193=CARTESIAN_POINT('Ctrl Pts',(0.1108775872014,0.117761723381742,1.03492476277015));
#20194=CARTESIAN_POINT('Ctrl Pts',(-0.0388783630684312,0.157003616909169,
1.04286693089293));
#20195=CARTESIAN_POINT('Ctrl Pts',(-0.153017738641585,0.0524140677533946,
1.05080909901571));
#20196=CARTESIAN_POINT('Ctrl Pts',(-0.126977145509477,-0.10019215216626,
1.05875126713849));
#20197=CARTESIAN_POINT('Ctrl Pts',(0.0153875577671049,-0.161012067570745,
1.06669343526127));
#20198=CARTESIAN_POINT('Ctrl Pts',(0.143655677305146,-0.0743283876822416,
1.07463560338405));
#20199=CARTESIAN_POINT('Ctrl Pts',(0.140320438123209,0.080447731368589,
1.08257777150683));
#20200=CARTESIAN_POINT('Ctrl Pts',(0.00843726195408678,0.161525463776335,
1.09051993962961));
#20201=CARTESIAN_POINT('Ctrl Pts',(-0.131175312957834,0.094629277223576,
1.09846210775239));
#20202=CARTESIAN_POINT('Ctrl Pts',(-0.150617825048456,-0.0589570489009974,
1.10640427587517));
#20203=CARTESIAN_POINT('Ctrl Pts',(-0.0320789358376135,-0.158532661344495,
1.11434644399795));
#20204=CARTESIAN_POINT('Ctrl Pts',(0.115847554194776,-0.112876069317329,
1.12228861212073));
#20205=CARTESIAN_POINT('Ctrl Pts',(0.157645783113317,0.0361865984037055,
1.13023078024351));
#20206=CARTESIAN_POINT('Ctrl Pts',(0.0550242791334153,0.152098624396442,
1.13817294836629));
#20207=CARTESIAN_POINT('Ctrl Pts',(-0.0980051173916675,0.128672684756662,
1.14611511648907));
#20208=CARTESIAN_POINT('Ctrl Pts',(-0.161251757937727,-0.0126306531673768,
1.15405728461185));
#20209=CARTESIAN_POINT('Ctrl Pts',(-0.0767752221903169,-0.142363015193798,
1.16199945273463));
#20210=CARTESIAN_POINT('Ctrl Pts',(0.0780353045016797,-0.141676229794458,
1.16994162085741));
#20211=CARTESIAN_POINT('Ctrl Pts',(0.161357475398708,-0.0111994629512984,
1.17788378898019));
#20212=CARTESIAN_POINT('Ctrl Pts',(0.0968596219472387,0.129537162519796,
1.18582595710297));
#20213=CARTESIAN_POINT('Ctrl Pts',(-0.0563715959749383,0.151604439264423,
1.19376812522575));
#20214=CARTESIAN_POINT('Ctrl Pts',(-0.157960640709981,0.0347864747270306,
1.20171029334853));
#20215=CARTESIAN_POINT('Ctrl Pts',(-0.114841510641486,-0.113899474410655,
1.20965246147131));
#20216=CARTESIAN_POINT('Ctrl Pts',(0.03348424129126,-0.158241803650584,
1.21759462959409));
#20217=CARTESIAN_POINT('Ctrl Pts',(0.151134988234409,-0.0576183839484237,
1.22553679771687));
#20218=CARTESIAN_POINT('Ctrl Pts',(0.130330559267559,0.0957893948119858,
1.23347896583965));
#20219=CARTESIAN_POINT('Ctrl Pts',(-0.0098700513554357,0.16144424710618,
1.24142113396243));
#20220=CARTESIAN_POINT('Ctrl Pts',(-0.141028680947982,0.0791995832534545,
1.24936330208521));
#20221=CARTESIAN_POINT('Ctrl Pts',(-0.142990550365238,-0.0756000353418,
1.25730547020799));
#20222=CARTESIAN_POINT('Ctrl Pts',(-0.013958385670676,-0.161142254877177,
1.26524763833077));
#20223=CARTESIAN_POINT('Ctrl Pts',(0.127861094297897,-0.0990616141723472,
1.27318980645355));
#20224=CARTESIAN_POINT('Ctrl Pts',(0.152546676219863,0.0537696421008814,
1.28113197457633));
#20225=CARTESIAN_POINT('Ctrl Pts',(0.0374838310097642,0.157342382244044,
1.28907414269911));
#20226=CARTESIAN_POINT('Ctrl Pts',(-0.111918054267102,0.116773335855419,
1.29701631082189));
#20227=CARTESIAN_POINT('Ctrl Pts',(-0.158791504053787,-0.0307720827589687,
1.30495847894467));
#20228=CARTESIAN_POINT('Ctrl Pts',(-0.060195622861772,-0.150127112226926,
1.31290064706745));
#20229=CARTESIAN_POINT('Ctrl Pts',(0.0935456330135535,-0.131950283756556,
1.32084281519023));
#20230=CARTESIAN_POINT('Ctrl Pts',(0.161589478720268,0.00710656041347678,
1.32878498331301));
#20231=CARTESIAN_POINT('Ctrl Pts',(0.0816007612396376,0.139653065139265,
1.33672715143579));
#20232=CARTESIAN_POINT('Ctrl Pts',(-0.0731426367739486,0.144263015132499,
1.34466931955857));
#20233=CARTESIAN_POINT('Ctrl Pts',(-0.160879865135934,0.0167132224867059,
1.35261148768135));
#20234=CARTESIAN_POINT('Ctrl Pts',(-0.101234609479067,-0.126147598829082,
1.36055365580413));
#20235=CARTESIAN_POINT('Ctrl Pts',(0.051151949184981,-0.153444260252591,
1.36849582392691));
#20236=CARTESIAN_POINT('Ctrl Pts',(0.15667806641111,-0.0401702148435725,
1.37643799204969));
#20237=CARTESIAN_POINT('Ctrl Pts',(0.118670980449659,0.10990387323047,1.38438016017247));
#20238=CARTESIAN_POINT('Ctrl Pts',(-0.0280509185434417,0.159294724422008,
1.39232232829525));
#20239=CARTESIAN_POINT('Ctrl Pts',(-0.149075287902345,0.0627552395607943,
1.40026449641803));
#20240=CARTESIAN_POINT('Ctrl Pts',(-0.133531390736797,-0.0912744851582948,
1.40820666454081));
#20241=CARTESIAN_POINT('Ctrl Pts',(0.00434100186018791,-0.161687417152987,
1.41614883266359));
#20242=CARTESIAN_POINT('Ctrl Pts',(0.138236546518021,-0.0839780402106489,
1.42409100078637));
#20243=CARTESIAN_POINT('Ctrl Pts',(0.145493297031458,0.07066380330362,1.43203316890915));
#20244=CARTESIAN_POINT('Ctrl Pts',(0.0194630807988606,0.160570430100525,
1.43997533703193));
#20245=CARTESIAN_POINT('Ctrl Pts',(-0.124397014000637,0.103377882332206,
1.44791750515471));
#20246=CARTESIAN_POINT('Ctrl Pts',(-0.15429723939393,-0.0485191136187331,
1.45585967327749));
#20247=CARTESIAN_POINT('Ctrl Pts',(-0.042844249846,-0.155968210152522,1.46380184140027));
#20248=CARTESIAN_POINT('Ctrl Pts',(0.107856400646442,-0.120533276677448,
1.47174400952305));
#20249=CARTESIAN_POINT('Ctrl Pts',(0.159753444358638,0.0253203827049868,
1.47968617764583));
#20250=CARTESIAN_POINT('Ctrl Pts',(0.0652924466007548,0.147982030257331,
1.48762834576861));
#20251=CARTESIAN_POINT('Ctrl Pts',(-0.0889689487809616,0.13506922671723,
1.49557051389139));
#20252=CARTESIAN_POINT('Ctrl Pts',(-0.161752593421533,-0.00156622680492735,
1.50351268201417));
#20253=CARTESIAN_POINT('Ctrl Pts',(-0.086303059730943,-0.136794666273195,
1.51145485013695));
#20254=CARTESIAN_POINT('Ctrl Pts',(0.0681115549116652,-0.14665217563879,
1.51939701825973));
#20255=CARTESIAN_POINT('Ctrl Pts',(0.160315645894948,-0.02226314405755,
1.52733918638251));
#20256=CARTESIAN_POINT('Ctrl Pts',(0.105284883301553,0.122726172858702,
1.53528135450529));
#20257=CARTESIAN_POINT('Ctrl Pts',(0.00484533846358528,0.144116573583224,
1.54057613325381));
#20258=CARTESIAN_POINT('Ctrl Pts',(-0.0388047044047284,0.131206995015745,
1.54322352262807));
#20259=CARTESIAN_POINT('Ctrl Pts',(-0.0634007094575145,0.131904027763688,
-3.88578058618805E-16));
#20260=CARTESIAN_POINT('Ctrl Pts',(-0.107282641710421,0.110811831533068,
0.00264738937425961));
#20261=CARTESIAN_POINT('Ctrl Pts',(-0.171581760589518,0.0217576868851663,
0.0079421681227796));
#20262=CARTESIAN_POINT('Ctrl Pts',(-0.111156590520044,-0.1327225175337,
0.0158843362455596));
#20263=CARTESIAN_POINT('Ctrl Pts',(0.0512451567233008,-0.165187689797298,
0.0238265043683396));
#20264=CARTESIAN_POINT('Ctrl Pts',(0.16662620135312,-0.0465387668729445,
0.0317686724911196));
#20265=CARTESIAN_POINT('Ctrl Pts',(0.129399745666171,0.114856349193662,
0.0397108406138996));
#20266=CARTESIAN_POINT('Ctrl Pts',(-0.026390801400978,0.170972456562021,
0.0476530087366796));
#20267=CARTESIAN_POINT('Ctrl Pts',(-0.157993800025737,0.070491178324729,
0.0555951768594596));
#20268=CARTESIAN_POINT('Ctrl Pts',(-0.144863967768493,-0.0945835600760224,
0.0635373449822396));
#20269=CARTESIAN_POINT('Ctrl Pts',(0.000979154756195248,-0.17300145605975,
0.0714795131050195));
#20270=CARTESIAN_POINT('Ctrl Pts',(0.145923683802689,-0.0929367665856833,
0.0794216812277997));
#20271=CARTESIAN_POINT('Ctrl Pts',(0.157187963117837,0.0722699302633024,
0.0873638493505794));
#20272=CARTESIAN_POINT('Ctrl Pts',(0.0244514793930555,0.171268692120756,
0.0953060174733598));
#20273=CARTESIAN_POINT('Ctrl Pts',(-0.130684839550095,0.113368397534175,
0.103248185596139));
#20274=CARTESIAN_POINT('Ctrl Pts',(-0.166100541844429,-0.0483893439312075,
0.11119035371892));
#20275=CARTESIAN_POINT('Ctrl Pts',(-0.0493510193195793,-0.165817291858885,
0.119132521841699));
#20276=CARTESIAN_POINT('Ctrl Pts',(0.112609073040783,-0.131339661914923,
0.12707468996448));
#20277=CARTESIAN_POINT('Ctrl Pts',(0.17140770357293,0.0234586422209967,
0.135016858087259));
#20278=CARTESIAN_POINT('Ctrl Pts',(0.0731792588499177,0.156766393306209,
0.14295902621004));
#20279=CARTESIAN_POINT('Ctrl Pts',(-0.0920889000195865,0.146460037003638,
0.150901194332819));
#20280=CARTESIAN_POINT('Ctrl Pts',(-0.172994168426659,0.00198123296575728,
0.1588433624556));
#20281=CARTESIAN_POINT('Ctrl Pts',(-0.0954190048152776,-0.144312580095855,
0.16678553057838));
#20282=CARTESIAN_POINT('Ctrl Pts',(0.0695697692503139,-0.158401246055831,
0.17472769870116));
#20283=CARTESIAN_POINT('Ctrl Pts',(0.170825487889685,-0.0273780963649298,
0.18266986682394));
#20284=CARTESIAN_POINT('Ctrl Pts',(0.115587509852263,0.128726201683253,
0.19061203494672));
#20285=CARTESIAN_POINT('Ctrl Pts',(-0.0455405018601966,0.16690407474553,
0.198554203069499));
#20286=CARTESIAN_POINT('Ctrl Pts',(-0.164948735370872,0.0521806684752238,
0.20649637119228));
#20287=CARTESIAN_POINT('Ctrl Pts',(-0.133246981425072,-0.110345590758605,
0.214438539315059));
#20288=CARTESIAN_POINT('Ctrl Pts',(0.0205226964731592,-0.171783952668295,
0.22238070743784));
#20289=CARTESIAN_POINT('Ctrl Pts',(0.155491476033395,-0.0758505658746651,
0.230322875560619));
#20290=CARTESIAN_POINT('Ctrl Pts',(0.148014089296488,0.0895697316726553,
0.2382650436834));
#20291=CARTESIAN_POINT('Ctrl Pts',(0.00494059070111224,0.172934953166096,
0.24620721180618));
#20292=CARTESIAN_POINT('Ctrl Pts',(-0.142658996543838,0.0978739912732451,
0.25414937992896));
#20293=CARTESIAN_POINT('Ctrl Pts',(-0.159568287038446,-0.0668496016012732,
0.262091548051739));
#20294=CARTESIAN_POINT('Ctrl Pts',(-0.0302966335331915,-0.170332091689456,
0.27003371617452));
#20295=CARTESIAN_POINT('Ctrl Pts',(0.126729848780061,-0.11777288690896,
0.2779758842973));
#20296=CARTESIAN_POINT('Ctrl Pts',(0.167658770158652,0.0426783815482623,
0.28591805242008));
#20297=CARTESIAN_POINT('Ctrl Pts',(0.0549950338320791,0.164031867990689,
0.293860220542859));
#20298=CARTESIAN_POINT('Ctrl Pts',(-0.108049803339193,0.135115311719503,
0.30180238866564));
#20299=CARTESIAN_POINT('Ctrl Pts',(-0.1721099202737,-0.0175807510100837,
0.309744556788419));
#20300=CARTESIAN_POINT('Ctrl Pts',(-0.0784996687135917,-0.154171039675278,
0.3176867249112));
#20301=CARTESIAN_POINT('Ctrl Pts',(0.087024343965547,-0.14952481740522,
0.325628893033979));
#20302=CARTESIAN_POINT('Ctrl Pts',(0.172825117221703,-0.00789850112384905,
0.33357106115676));
#20303=CARTESIAN_POINT('Ctrl Pts',(0.100300328103893,0.140963653630822,
0.341513229279539));
#20304=CARTESIAN_POINT('Ctrl Pts',(-0.0641098658012952,0.160688619913292,
0.349455397402319));
#20305=CARTESIAN_POINT('Ctrl Pts',(-0.16978883637574,0.033206302186043,
0.357397565525099));
#20306=CARTESIAN_POINT('Ctrl Pts',(-0.119923789760104,-0.124696399756661,
0.36533973364788));
#20307=CARTESIAN_POINT('Ctrl Pts',(0.0398037685148125,-0.168364388974385,
0.373281901770659));
#20308=CARTESIAN_POINT('Ctrl Pts',(0.163066985633654,-0.0577933011607096,
0.38122406989344));
#20309=CARTESIAN_POINT('Ctrl Pts',(0.136944091404129,0.10572238784759,0.38916623801622));
#20310=CARTESIAN_POINT('Ctrl Pts',(-0.0146336593526265,0.172385508313924,
0.397108406138999));
#20311=CARTESIAN_POINT('Ctrl Pts',(-0.152805474769431,0.0811257933285562,
0.40505057426178));
#20312=CARTESIAN_POINT('Ctrl Pts',(-0.150991776994562,-0.0844534827151793,
0.412992742384559));
#20313=CARTESIAN_POINT('Ctrl Pts',(-0.0108540995180527,-0.172664692355881,
0.42093491050734));
#20314=CARTESIAN_POINT('Ctrl Pts',(0.139227048201004,-0.102697305280782,
0.428877078630119));
#20315=CARTESIAN_POINT('Ctrl Pts',(0.16176191642983,0.0613513639265466,
0.4368192467529));
#20316=CARTESIAN_POINT('Ctrl Pts',(0.0361062507758455,0.169195880912067,
0.444761414875679));
#20317=CARTESIAN_POINT('Ctrl Pts',(-0.12262644992489,0.12203958882886,0.45270358299846));
#20318=CARTESIAN_POINT('Ctrl Pts',(-0.169020724600573,-0.0369175042249048,
0.460645751121239));
#20319=CARTESIAN_POINT('Ctrl Pts',(-0.0605746513833496,-0.162054370729346,
0.468587919244019));
#20320=CARTESIAN_POINT('Ctrl Pts',(0.103364025571403,-0.138732785167649,
0.4765300873668));
#20321=CARTESIAN_POINT('Ctrl Pts',(0.172610636112938,0.0116822841681558,
0.484472255489579));
#20322=CARTESIAN_POINT('Ctrl Pts',(0.083728171010617,0.151395181039277,
0.49241442361236));
#20323=CARTESIAN_POINT('Ctrl Pts',(-0.081857900459256,0.152414538660527,
0.500356591735139));
#20324=CARTESIAN_POINT('Ctrl Pts',(-0.172453725526818,0.0138065207282529,
0.50829875985792));
#20325=CARTESIAN_POINT('Ctrl Pts',(-0.105064221167447,-0.137449688588867,
0.516240927980699));
#20326=CARTESIAN_POINT('Ctrl Pts',(0.0585749034388466,-0.162787862415564,
0.52418309610348));
#20327=CARTESIAN_POINT('Ctrl Pts',(0.168553398866689,-0.0389956304370821,
0.532125264226259));
#20328=CARTESIAN_POINT('Ctrl Pts',(0.124119664784058,0.120520605195094,
0.54006743234904));
#20329=CARTESIAN_POINT('Ctrl Pts',(-0.0340204335384149,0.16962758491636,
0.548009600471819));
#20330=CARTESIAN_POINT('Ctrl Pts',(-0.160994319687769,0.0633382703503284,
0.5559517685946));
#20331=CARTESIAN_POINT('Ctrl Pts',(-0.14048086942825,-0.100975406844349,
0.563893936717379));
#20332=CARTESIAN_POINT('Ctrl Pts',(0.00872748937560605,-0.172785237771916,
0.57183610484016));
#20333=CARTESIAN_POINT('Ctrl Pts',(0.149940571302356,-0.0863060399984934,
0.579778272962939));
#20334=CARTESIAN_POINT('Ctrl Pts',(0.153792685935992,0.0792383569699183,
0.58772044108572));
#20335=CARTESIAN_POINT('Ctrl Pts',(0.0167549005293281,0.17219227848818,
0.595662609208499));
#20336=CARTESIAN_POINT('Ctrl Pts',(-0.135632095058532,0.107400382926376,
0.60360477733128));
#20337=CARTESIAN_POINT('Ctrl Pts',(-0.163766157558233,-0.0557812970565469,
0.611546945454059));
#20338=CARTESIAN_POINT('Ctrl Pts',(-0.0418735953979919,-0.167861578305293,
0.61948911357684));
#20339=CARTESIAN_POINT('Ctrl Pts',(0.118379481984711,-0.126163408751231,
0.627431281699619));
#20340=CARTESIAN_POINT('Ctrl Pts',(0.17018479228316,0.0311134044783985,
0.6353734498224));
#20341=CARTESIAN_POINT('Ctrl Pts',(0.0660833491022344,0.159887142804326,
0.643315617945179));
#20342=CARTESIAN_POINT('Ctrl Pts',(-0.0985572308567358,0.142187832491218,
0.651257786067961));
#20343=CARTESIAN_POINT('Ctrl Pts',(-0.172909262181909,-0.00577013989488307,
0.659199954190738));
#20344=CARTESIAN_POINT('Ctrl Pts',(-0.0888586457050277,-0.148442071348278,
0.667142122313521));
#20345=CARTESIAN_POINT('Ctrl Pts',(0.0765956190331784,-0.155125815413241,
0.675084290436298));
#20346=CARTESIAN_POINT('Ctrl Pts',(0.171880427770071,-0.0196983758791502,
0.683026458559081));
#20347=CARTESIAN_POINT('Ctrl Pts',(0.109705106722326,0.133774799651286,
0.690968626681858));
#20348=CARTESIAN_POINT('Ctrl Pts',(-0.0529713625168984,0.164696515493808,
0.698910794804641));
#20349=CARTESIAN_POINT('Ctrl Pts',(-0.167120621735807,0.0447393032280997,
0.706852962927418));
#20350=CARTESIAN_POINT('Ctrl Pts',(-0.12817022249092,-0.116203707037801,
0.7147951310502));
#20351=CARTESIAN_POINT('Ctrl Pts',(0.0281972679828983,-0.17069218359667,
0.722737299172979));
#20352=CARTESIAN_POINT('Ctrl Pts',(0.158733164168978,-0.0688090841067,0.73067946729576));
#20353=CARTESIAN_POINT('Ctrl Pts',(0.14385317469873,0.0961102054508026,
0.738621635418538));
#20354=CARTESIAN_POINT('Ctrl Pts',(-0.00281110139369983,0.172982673038814,
0.746563803541321));
#20355=CARTESIAN_POINT('Ctrl Pts',(-0.146900119814081,0.0913852409380608,
0.754505971664098));
#20356=CARTESIAN_POINT('Ctrl Pts',(-0.156413536862055,-0.0739304602244656,
0.762448139786881));
#20357=CARTESIAN_POINT('Ctrl Pts',(-0.0226360851712103,-0.171518264656626,
0.770390307909658));
#20358=CARTESIAN_POINT('Ctrl Pts',(0.131878346029848,-0.111977717922496,
0.778332476032441));
#20359=CARTESIAN_POINT('Ctrl Pts',(0.165578663890314,0.0501459223366878,
0.786274644155218));
#20360=CARTESIAN_POINT('Ctrl Pts',(0.047591915084802,0.166330746049129,
0.794216812278001));
#20361=CARTESIAN_POINT('Ctrl Pts',(-0.113993917241593,0.130139518573781,
0.802158980400778));
#20362=CARTESIAN_POINT('Ctrl Pts',(-0.171149610334614,-0.0252728776558711,
0.81010114852356));
#20363=CARTESIAN_POINT('Ctrl Pts',(-0.0715146774936035,-0.157532721571376,
0.818043316646339));
#20364=CARTESIAN_POINT('Ctrl Pts',(0.0936350469135118,-0.14547640857611,
0.825985484769119));
#20365=CARTESIAN_POINT('Ctrl Pts',(0.173005448853992,-0.000148759965830227,
0.8339276528919));
#20366=CARTESIAN_POINT('Ctrl Pts',(0.0938850861191564,0.145315168055841,
0.841869821014678));
#20367=CARTESIAN_POINT('Ctrl Pts',(-0.0712436606821878,0.157655473343934,
0.849811989137461));
#20368=CARTESIAN_POINT('Ctrl Pts',(-0.171105895159299,0.0255671684868261,
0.857754157260238));
#20369=CARTESIAN_POINT('Ctrl Pts',(-0.114217551294,-0.129943289319231,0.86569632538302));
#20370=CARTESIAN_POINT('Ctrl Pts',(0.0473058035714782,-0.166412344527548,
0.873638493505798));
#20371=CARTESIAN_POINT('Ctrl Pts',(0.16549218245563,-0.0504305959589149,
0.88158066162858));
#20372=CARTESIAN_POINT('Ctrl Pts',(0.132070720552549,0.111750759440056,
0.889522829751358));
#20373=CARTESIAN_POINT('Ctrl Pts',(-0.022341089517305,0.171556938600217,
0.89746499787414));
#20374=CARTESIAN_POINT('Ctrl Pts',(-0.156286166401977,0.074199337288632,
0.905407165996919));
#20375=CARTESIAN_POINT('Ctrl Pts',(-0.147057058974526,-0.0911324797668838,
0.913349334119699));
#20376=CARTESIAN_POINT('Ctrl Pts',(-0.00310857778072832,-0.172977582960567,
0.92129150224248));
#20377=CARTESIAN_POINT('Ctrl Pts',(0.143687680016546,-0.0963574495000853,
0.929233670365259));
#20378=CARTESIAN_POINT('Ctrl Pts',(0.158851261322436,0.0685360068793772,
0.93717583848804));
#20379=CARTESIAN_POINT('Ctrl Pts',(0.0284907678468484,0.170643439985825,
0.945118006610819));
#20380=CARTESIAN_POINT('Ctrl Pts',(-0.127970195944242,0.116423951198588,
0.9530601747336));
#20381=CARTESIAN_POINT('Ctrl Pts',(-0.167197313372666,-0.0444518375735043,
0.961002342856378));
#20382=CARTESIAN_POINT('Ctrl Pts',(-0.0532545149190986,-0.164605176417482,
0.96894451097916));
#20383=CARTESIAN_POINT('Ctrl Pts',(0.10947489024455,-0.133963263130763,
0.976886679101939));
#20384=CARTESIAN_POINT('Ctrl Pts',(0.1719140491614,0.0194027617526574,0.984828847224719));
#20385=CARTESIAN_POINT('Ctrl Pts',(0.0768622776450996,0.154993863549195,
0.992771015347499));
#20386=CARTESIAN_POINT('Ctrl Pts',(-0.088603236555915,0.148594663210074,
1.00071318347028));
#20387=CARTESIAN_POINT('Ctrl Pts',(-0.172899083515371,0.00606748566075909,
1.00865535159306));
#20388=CARTESIAN_POINT('Ctrl Pts',(-0.0988016073770141,-0.142018132090297,
1.01659751971584));
#20389=CARTESIAN_POINT('Ctrl Pts',(0.0658082913934689,-0.160000550769587,
1.02453968783862));
#20390=CARTESIAN_POINT('Ctrl Pts',(0.170131034504888,-0.0314060274628177,
1.0324818559614));
#20391=CARTESIAN_POINT('Ctrl Pts',(0.118596271784576,0.125959643463681,
1.04042402408418));
#20392=CARTESIAN_POINT('Ctrl Pts',(-0.0415848597483297,0.167933340651612,
1.04836619220696));
#20393=CARTESIAN_POINT('Ctrl Pts',(-0.163669987576804,0.0560628453550813,
1.05630836032974));
#20394=CARTESIAN_POINT('Ctrl Pts',(-0.135816592328243,-0.107166975841641,
1.06425052845252));
#20395=CARTESIAN_POINT('Ctrl Pts',(0.0164587544616562,-0.172220837485682,
1.0721926965753));
#20396=CARTESIAN_POINT('Ctrl Pts',(0.153656191292587,-0.0795027190739688,
1.08013486469808));
#20397=CARTESIAN_POINT('Ctrl Pts',(0.150088771199207,0.0860480576341552,
1.08807703282086));
#20398=CARTESIAN_POINT('Ctrl Pts',(0.00902461748204118,0.172769973496559,
1.09601920094364));
#20399=CARTESIAN_POINT('Ctrl Pts',(-0.140307012982855,0.101216844302358,
1.10396136906642));
#20400=CARTESIAN_POINT('Ctrl Pts',(-0.161103005268346,-0.0630613126743013,
1.1119035371892));
#20401=CARTESIAN_POINT('Ctrl Pts',(-0.0343120939874615,-0.1695688287065,
1.11984570531198));
#20402=CARTESIAN_POINT('Ctrl Pts',(0.123912220401285,-0.120733877175888,
1.12778787343476));
#20403=CARTESIAN_POINT('Ctrl Pts',(0.168620210916381,0.0387057093103061,
1.13573004155754));
#20404=CARTESIAN_POINT('Ctrl Pts',(0.0588547652196237,0.162686889679659,
1.14367220968032));
#20405=CARTESIAN_POINT('Ctrl Pts',(-0.104827691798069,0.137630165643247,
1.1516143778031));
#20406=CARTESIAN_POINT('Ctrl Pts',(-0.172477213770776,-0.0135099294065116,
1.15955654592588));
#20407=CARTESIAN_POINT('Ctrl Pts',(-0.0821198886720452,-0.152273541192125,
1.16749871404866));
#20408=CARTESIAN_POINT('Ctrl Pts',(0.083467690946984,-0.15153894559049,
1.17544088217144));
#20409=CARTESIAN_POINT('Ctrl Pts',(0.172590290696882,-0.0119791076405788,
1.18338305029422));
#20410=CARTESIAN_POINT('Ctrl Pts',(0.103602453294194,0.13855482356859,1.191325218417));
#20411=CARTESIAN_POINT('Ctrl Pts',(-0.0602958748103966,0.162158302111078,
1.19926738653978));
#20412=CARTESIAN_POINT('Ctrl Pts',(-0.168956987158091,0.0372081167644847,
1.20720955466256));
#20413=CARTESIAN_POINT('Ctrl Pts',(-0.122836141658186,-0.121828526073448,
1.21515172278534));
#20414=CARTESIAN_POINT('Ctrl Pts',(0.0358152290369173,-0.169257723108079,
1.22309389090812));
#20415=CARTESIAN_POINT('Ctrl Pts',(0.161656170495932,-0.0616294572691503,
1.2310360590309));
#20416=CARTESIAN_POINT('Ctrl Pts',(0.13940345221127,0.102457722863032,1.23897822715368));
#20417=CARTESIAN_POINT('Ctrl Pts',(-0.0105571497596809,0.172683102970871,
1.24692039527646));
#20418=CARTESIAN_POINT('Ctrl Pts',(-0.150846317973597,0.0847130203482025,
1.25486256339924));
#20419=CARTESIAN_POINT('Ctrl Pts',(-0.152944761892581,-0.0808628918127005,
1.26280473152202));
#20420=CARTESIAN_POINT('Ctrl Pts',(-0.0149300913057054,-0.172360087712588,
1.2707468996448));
#20421=CARTESIAN_POINT('Ctrl Pts',(0.136762076743997,-0.105957736043287,
1.27868906776758));
#20422=CARTESIAN_POINT('Ctrl Pts',(0.163166132393764,0.0575127872937276,
1.28663123589036));
#20423=CARTESIAN_POINT('Ctrl Pts',(0.0400932480780463,0.168295688956082,
1.29457340401314));
#20424=CARTESIAN_POINT('Ctrl Pts',(-0.119709170414695,0.124902449862528,
1.30251557213592));
#20425=CARTESIAN_POINT('Ctrl Pts',(-0.169845690614082,-0.0329142650230248,
1.3104577402587));
#20426=CARTESIAN_POINT('Ctrl Pts',(-0.0643861093061943,-0.160578131733314,
1.31839990838148));
#20427=CARTESIAN_POINT('Ctrl Pts',(0.100057762773863,-0.141135932963798,
1.32634207650426));
#20428=CARTESIAN_POINT('Ctrl Pts',(0.172838444806952,0.00760127985757451,
1.33428424462704));
#20429=CARTESIAN_POINT('Ctrl Pts',(0.0872813550697656,0.149374939398002,
1.34222641274982));
#20430=CARTESIAN_POINT('Ctrl Pts',(-0.0782344227434143,0.154305808621531,
1.3501685808726));
#20431=CARTESIAN_POINT('Ctrl Pts',(-0.172079431848303,0.0178767046294837,
1.35811074899538));
#20432=CARTESIAN_POINT('Ctrl Pts',(-0.108282003268856,-0.134929297194493,
1.36605291711816));
#20433=CARTESIAN_POINT('Ctrl Pts',(0.0547128650701426,-0.164126201264144,
1.37399508524094));
#20434=CARTESIAN_POINT('Ctrl Pts',(0.167585127127835,-0.0429666431014547,
1.38193725336372));
#20435=CARTESIAN_POINT('Ctrl Pts',(0.126932197981417,0.117554773230619,
1.3898794214865));
#20436=CARTESIAN_POINT('Ctrl Pts',(-0.0300036684000219,0.170383942402052,
1.39782158960928));
#20437=CARTESIAN_POINT('Ctrl Pts',(-0.159453085214751,0.0671239123677834,
1.40576375773206));
#20438=CARTESIAN_POINT('Ctrl Pts',(-0.142827107870127,-0.0976285101620078,
1.41370592585484));
#20439=CARTESIAN_POINT('Ctrl Pts',(0.00464319840846943,-0.172943201171859,
1.42164809397762));
#20440=CARTESIAN_POINT('Ctrl Pts',(0.147859810582222,-0.0898241270588577,
1.4295902621004));
#20441=CARTESIAN_POINT('Ctrl Pts',(0.155621735944117,0.0755830265922534,
1.43753243022318));
#20442=CARTESIAN_POINT('Ctrl Pts',(0.0208179928734729,0.171748455656582,
1.44547459834596));
#20443=CARTESIAN_POINT('Ctrl Pts',(-0.133056846329205,0.11057447892796,
1.45341676646874));
#20444=CARTESIAN_POINT('Ctrl Pts',(-0.165038560097216,-0.0518967460486161,
1.46135893459152));
#20445=CARTESIAN_POINT('Ctrl Pts',(-0.0458268296361176,-0.166825854601292,
1.4693011027143));
#20446=CARTESIAN_POINT('Ctrl Pts',(0.115364766925686,-0.128924136976022,
1.47724327083708));
#20447=CARTESIAN_POINT('Ctrl Pts',(0.170874595884426,0.0270830477535184,
1.48518543895986));
#20448=CARTESIAN_POINT('Ctrl Pts',(0.0698377457337486,0.158283721017069,
1.49312760708264));
#20449=CARTESIAN_POINT('Ctrl Pts',(-0.0951624750893037,0.144471999488883,
1.50106977520542));
#20450=CARTESIAN_POINT('Ctrl Pts',(-0.173012914651864,-0.00167525885548286,
1.5090119433282));
#20451=CARTESIAN_POINT('Ctrl Pts',(-0.092311001583214,-0.14631755460685,
1.51695411145098));
#20452=CARTESIAN_POINT('Ctrl Pts',(0.072853104778531,-0.156861289272697,
1.52489627957376));
#20453=CARTESIAN_POINT('Ctrl Pts',(0.171475934783304,-0.0238129810547936,
1.53283844769654));
#20454=CARTESIAN_POINT('Ctrl Pts',(0.11261423476106,0.131269690464983,1.54078061581932));
#20455=CARTESIAN_POINT('Ctrl Pts',(0.00518264413773371,0.154149172621267,
1.54607539456784));
#20456=CARTESIAN_POINT('Ctrl Pts',(-0.0415060733757155,0.140340900570467,
1.5487227839421));
#20457=CARTESIAN_POINT('Ctrl Pts',(-0.146248097568756,-0.000123763188177425,
1.45893449541571));
#20458=CARTESIAN_POINT('Ctrl Pts',(-0.146367493381718,-0.0150081347743067,
1.45974264180765));
#20459=CARTESIAN_POINT('Ctrl Pts',(-0.144277648885518,-0.0298597803798721,
1.46055078819958));
#20460=CARTESIAN_POINT('Ctrl Pts',(-0.139839652725699,-0.043973059977961,
1.46135893459152));
#20461=CARTESIAN_POINT('Ctrl Pts',(-0.125301316610186,-0.0902064488995044,
1.46400632396578));
#20462=CARTESIAN_POINT('Ctrl Pts',(-0.08556407312315,-0.1285161517504,1.46665371334004));
#20463=CARTESIAN_POINT('Ctrl Pts',(-0.0388301852859989,-0.141354050238301,
1.4693011027143));
#20464=CARTESIAN_POINT('Ctrl Pts',(0.00790370255115092,-0.154191948726202,
1.47194849208856));
#20465=CARTESIAN_POINT('Ctrl Pts',(0.0616342347384179,-0.141558042851112,
1.47459588146282));
#20466=CARTESIAN_POINT('Ctrl Pts',(0.0977511389918415,-0.109239892458645,
1.47724327083708));
#20467=CARTESIAN_POINT('Ctrl Pts',(0.133868043245265,-0.0769217420661769,
1.47989066021134));
#20468=CARTESIAN_POINT('Ctrl Pts',(0.152371319564846,-0.024919347156331,
1.4825380495856));
#20469=CARTESIAN_POINT('Ctrl Pts',(0.144783482699524,0.0229486291758506,
1.48518543895986));
#20470=CARTESIAN_POINT('Ctrl Pts',(0.137195645834202,0.0708166055080336,
1.48783282833412));
#20471=CARTESIAN_POINT('Ctrl Pts',(0.103516695783975,0.114550163262552,
1.49048021770838));
#20472=CARTESIAN_POINT('Ctrl Pts',(0.0591771839550196,0.13411498855178,
1.49312760708264));
#20473=CARTESIAN_POINT('Ctrl Pts',(0.014837672126065,0.153679813841007,
1.4957749964569));
#20474=CARTESIAN_POINT('Ctrl Pts',(-0.0401624014816186,0.149075906664945,
1.49842238583116));
#20475=CARTESIAN_POINT('Ctrl Pts',(-0.0806375115458872,0.122416076686187,
1.50106977520542));
#20476=CARTESIAN_POINT('Ctrl Pts',(-0.0937869288003098,0.113754921033589,
1.50192985013695));
#20477=CARTESIAN_POINT('Ctrl Pts',(-0.105403311347291,0.102765876910903,
1.50278992506847));
#20478=CARTESIAN_POINT('Ctrl Pts',(-0.115078604842433,0.0902138214954038,
1.50365));
#20479=CARTESIAN_POINT('Ctrl Pts',(-0.0686146973663081,-0.0959584553529135,
1.07336015076065E-17));
#20480=CARTESIAN_POINT('Ctrl Pts',(-0.0712979561985307,-0.0944995001033786,
9.02613639135873E-18));
#20481=CARTESIAN_POINT('Ctrl Pts',(-0.0739152333025289,-0.0929325179580126,
1.64107321374712E-17));
#20482=CARTESIAN_POINT('Ctrl Pts',(-0.0764591723283171,-0.0912589988675934,
1.6154612370034E-17));
#20483=CARTESIAN_POINT('Ctrl Pts',(-0.0824897891353913,-0.0872917841461184,
1.52077426268717E-17));
#20484=CARTESIAN_POINT('Ctrl Pts',(-0.0881090519769445,-0.0827275518978924,
1.30971627060498E-17));
#20485=CARTESIAN_POINT('Ctrl Pts',(-0.0932912133381108,-0.0776621329443405,
1.43114686768087E-17));
#20486=CARTESIAN_POINT('Ctrl Pts',(-0.0960634919631888,-0.074952307504085,
1.49610807310118E-17));
#20487=CARTESIAN_POINT('Ctrl Pts',(-0.0987043519497191,-0.0721043812799658,
1.74993329480528E-17));
#20488=CARTESIAN_POINT('Ctrl Pts',(-0.101206237074718,-0.0691378820326018,
9.97465998686664E-18));
#20489=CARTESIAN_POINT('Ctrl Pts',(-0.105823426721714,-0.0636632543305198,
-3.91200561030858E-18));
#20490=CARTESIAN_POINT('Ctrl Pts',(-0.109972666997065,-0.0577811896139199,
2.24798207762934E-18));
#20491=CARTESIAN_POINT('Ctrl Pts',(-0.113625452403263,-0.0515741981665521,
9.54097911787244E-18));
#20492=CARTESIAN_POINT('Ctrl Pts',(-0.115386295340069,-0.0485820878086944,
1.30566037435822E-17));
#20493=CARTESIAN_POINT('Ctrl Pts',(-0.117027309103105,-0.0455212415157476,
-2.79521757168051E-18));
#20494=CARTESIAN_POINT('Ctrl Pts',(-0.118543833519887,-0.0424058589801268,
-3.46944695195361E-18));
#20495=CARTESIAN_POINT('Ctrl Pts',(-0.122700941917732,-0.0338659484069709,
-5.31764971597768E-18));
#20496=CARTESIAN_POINT('Ctrl Pts',(-0.125931492798984,-0.0249085743588085,
-1.15219401683824E-18));
#20497=CARTESIAN_POINT('Ctrl Pts',(-0.128167520083254,-0.0157105262534848,
9.54097911787244E-18));
#20498=CARTESIAN_POINT('Ctrl Pts',(-0.128992166906242,-0.0123182862745252,
1.3484621181291E-17));
#20499=CARTESIAN_POINT('Ctrl Pts',(-0.129681150280034,-0.00889298553317688,
1.10989611676181E-17));
#20500=CARTESIAN_POINT('Ctrl Pts',(-0.130229483957028,-0.00544263935519351,
9.54097911787244E-18));
#20501=CARTESIAN_POINT('Ctrl Pts',(-0.130761899349706,-0.00209245771889707,
8.02822573502553E-18));
#20502=CARTESIAN_POINT('Ctrl Pts',(-0.131160261982709,0.00127366115726457,
1.11791151702242E-17));
#20503=CARTESIAN_POINT('Ctrl Pts',(-0.131420990891747,0.00464012593483382,
8.67361737988404E-18));
#20504=CARTESIAN_POINT('Ctrl Pts',(-0.131728666658755,0.00861275649723166,
5.71697955546795E-18));
#20505=CARTESIAN_POINT('Ctrl Pts',(-0.131845259942619,0.0125891451047215,
-9.26473565962443E-18));
#20506=CARTESIAN_POINT('Ctrl Pts',(-0.131765781147177,0.0165567997877194,
-1.04083408558608E-17));
#20507=CARTESIAN_POINT('Ctrl Pts',(-0.131635692412819,0.0230509492424239,
-1.21888544026837E-17));
#20508=CARTESIAN_POINT('Ctrl Pts',(-0.13098103789945,0.0295216962360144,
-2.67049856555875E-17));
#20509=CARTESIAN_POINT('Ctrl Pts',(-0.129839098367345,0.0359278479980343,
-3.46944695195361E-17));
#20510=CARTESIAN_POINT('Ctrl Pts',(-0.129254890951344,0.0392051855997028,
-3.87818275556788E-17));
#20511=CARTESIAN_POINT('Ctrl Pts',(-0.128542951403208,0.0424656461998481,
-3.10678831811161E-17));
#20512=CARTESIAN_POINT('Ctrl Pts',(-0.1277070993652,0.0457037274559979,
-3.29597460435593E-17));
#20513=CARTESIAN_POINT('Ctrl Pts',(-0.126886363095037,0.0488832504000222,
-3.48173959609792E-17));
#20514=CARTESIAN_POINT('Ctrl Pts',(-0.125948031872817,0.0520333657183593,
-3.53366201082739E-17));
#20515=CARTESIAN_POINT('Ctrl Pts',(-0.124899042599898,0.0551436241923499,
-3.46944695195361E-17));
#20516=CARTESIAN_POINT('Ctrl Pts',(-0.122234979928128,0.0630425834229368,
-3.30636335736642E-17));
#20517=CARTESIAN_POINT('Ctrl Pts',(-0.118856305871375,0.070695441500891,
-2.1366080483524E-17));
#20518=CARTESIAN_POINT('Ctrl Pts',(-0.114834854776346,0.078019637496205,
-1.73472347597681E-17));
#20519=CARTESIAN_POINT('Ctrl Pts',(-0.11215901866562,0.0828930893082948,
-1.46731322388254E-17));
#20520=CARTESIAN_POINT('Ctrl Pts',(-0.109198005187061,0.0876211033078822,
8.28606628989234E-18));
#20521=CARTESIAN_POINT('Ctrl Pts',(-0.105966883726074,0.0921780034666525,
8.67361737988404E-18));
#20522=CARTESIAN_POINT('Ctrl Pts',(-0.104137243112614,0.094758373688769,
8.89307035390601E-18));
#20523=CARTESIAN_POINT('Ctrl Pts',(-0.102221042121924,0.0972831505018574,
-2.31209379389524E-17));
#20524=CARTESIAN_POINT('Ctrl Pts',(-0.100229777791505,0.0997373632832089,
-2.08166817117217E-17));
#20525=CARTESIAN_POINT('Ctrl Pts',(-0.0937202782075859,0.107760254486057,
-1.32840027382311E-17));
#20526=CARTESIAN_POINT('Ctrl Pts',(-0.0863914655699752,0.115060936709644,
5.4842312373535E-18));
#20527=CARTESIAN_POINT('Ctrl Pts',(-0.0783508402622743,0.121487309774744,
1.38777878078145E-17));
#20528=CARTESIAN_POINT('Ctrl Pts',(-0.073610711791116,0.125275800441382,
1.8825977152717E-17));
#20529=CARTESIAN_POINT('Ctrl Pts',(-0.068622257850438,0.128760167547443,
-9.09579695168528E-18));
#20530=CARTESIAN_POINT('Ctrl Pts',(-0.0634007094575209,0.131904027763685,
-6.93889390390723E-18));
#20531=CARTESIAN_POINT('Origin',(0.,0.,0.));
#20532=CARTESIAN_POINT('Origin',(-0.0721687836487033,-0.125,-0.3));
#20533=CARTESIAN_POINT('',(-0.0721687836487033,-0.125,-0.3));
#20534=CARTESIAN_POINT('',(0.0721687836487032,-0.125,-0.3));
#20535=CARTESIAN_POINT('',(-0.0360843918243517,-0.125,-0.3));
#20536=CARTESIAN_POINT('',(-0.0721687836487033,-0.125,-0.15));
#20537=CARTESIAN_POINT('',(-0.0721687836487033,-0.125,-0.3));
#20538=CARTESIAN_POINT('',(0.0721687836487032,-0.125,-0.15));
#20539=CARTESIAN_POINT('',(-0.0721687836487033,-0.125,-0.15));
#20540=CARTESIAN_POINT('',(0.0721687836487032,-0.125,-0.3));
#20541=CARTESIAN_POINT('Origin',(-0.144337567297406,1.76762539787485E-17,
-0.3));
#20542=CARTESIAN_POINT('',(-0.144337567297406,1.76762539787485E-17,-0.3));
#20543=CARTESIAN_POINT('',(-0.126295371385231,-0.03125,-0.3));
#20544=CARTESIAN_POINT('',(-0.144337567297406,2.77555756156289E-17,-0.15));
#20545=CARTESIAN_POINT('',(-0.144337567297406,1.76762539787485E-17,-0.3));
#20546=CARTESIAN_POINT('',(-0.144337567297406,1.76762539787485E-17,-0.15));
#20547=CARTESIAN_POINT('Origin',(-0.0721687836487032,0.125,-0.3));
#20548=CARTESIAN_POINT('',(-0.0721687836487032,0.125,-0.3));
#20549=CARTESIAN_POINT('',(-0.090210979560879,0.09375,-0.3));
#20550=CARTESIAN_POINT('',(-0.0721687836487032,0.125,-0.15));
#20551=CARTESIAN_POINT('',(-0.0721687836487032,0.125,-0.3));
#20552=CARTESIAN_POINT('',(-0.0721687836487032,0.125,-0.15));
#20553=CARTESIAN_POINT('Origin',(0.0721687836487032,0.125,-0.3));
#20554=CARTESIAN_POINT('',(0.0721687836487032,0.125,-0.3));
#20555=CARTESIAN_POINT('',(0.0360843918243516,0.125,-0.3));
#20556=CARTESIAN_POINT('',(0.0721687836487032,0.125,-0.15));
#20557=CARTESIAN_POINT('',(0.0721687836487032,0.125,-0.3));
#20558=CARTESIAN_POINT('',(0.0721687836487032,0.125,-0.15));
#20559=CARTESIAN_POINT('Origin',(0.144337567297406,0.,-0.3));
#20560=CARTESIAN_POINT('',(0.144337567297406,0.,-0.3));
#20561=CARTESIAN_POINT('',(0.126295371385231,0.03125,-0.3));
#20562=CARTESIAN_POINT('',(0.144337567297406,0.,-0.15));
#20563=CARTESIAN_POINT('',(0.144337567297406,0.,-0.3));
#20564=CARTESIAN_POINT('',(0.144337567297406,0.,-0.15));
#20565=CARTESIAN_POINT('Origin',(0.0721687836487032,-0.125,-0.3));
#20566=CARTESIAN_POINT('',(0.0902109795608791,-0.09375,-0.3));
#20567=CARTESIAN_POINT('',(0.0721687836487032,-0.125,-0.15));
#20568=CARTESIAN_POINT('Origin',(0.,0.,-0.15));
#20569=CARTESIAN_POINT('Origin',(0.,0.,0.));
#20570=CARTESIAN_POINT('',(-0.275,-3.36777869765522E-17,0.));
#20571=CARTESIAN_POINT('Origin',(0.,0.,0.));
#20572=CARTESIAN_POINT('Origin',(0.,0.,-0.3));
#20573=CARTESIAN_POINT('',(-0.275,-3.36777869765522E-17,-0.3));
#20574=CARTESIAN_POINT('',(-0.275,-3.36777869765522E-17,-0.3));
#20575=CARTESIAN_POINT('Origin',(0.,0.,-0.3));
#20576=CARTESIAN_POINT('Origin',(0.,0.,-0.3));
#20577=CARTESIAN_POINT('Origin',(0.,0.,1.6));
#22113=UNCERTAINTY_MEASURE_WITH_UNIT(LENGTH_MEASURE(0.001),#22130,
'DISTANCE_ACCURACY_VALUE',
'Maximum model space distance between geometric entities at asserted c
onnectivities');
#22117=UNCERTAINTY_MEASURE_WITH_UNIT(LENGTH_MEASURE(0.001),#22130,
'DISTANCE_ACCURACY_VALUE',
'Maximum model space distance between geometric entities at asserted c
onnectivities');
#22125=(
GEOMETRIC_REPRESENTATION_CONTEXT(3)
GLOBAL_UNCERTAINTY_ASSIGNED_CONTEXT((#22113))
GLOBAL_UNIT_ASSIGNED_CONTEXT((#22130,#22132,#22133))
REPRESENTATION_CONTEXT('','3D')
);
#22129=(
GEOMETRIC_REPRESENTATION_CONTEXT(3)
GLOBAL_UNCERTAINTY_ASSIGNED_CONTEXT((#22117))
GLOBAL_UNIT_ASSIGNED_CONTEXT((#22130,#22132,#22133))
REPRESENTATION_CONTEXT('','3D')
);
#22130=(
LENGTH_UNIT()
NAMED_UNIT(*)
SI_UNIT(.CENTI.,.METRE.)
);
#22132=(
NAMED_UNIT(*)
PLANE_ANGLE_UNIT()
SI_UNIT($,.RADIAN.)
);
#22133=(
NAMED_UNIT(*)
SI_UNIT($,.STERADIAN.)
SOLID_ANGLE_UNIT()
);
#22141=SHAPE_DEFINITION_REPRESENTATION(#22152,#22179);
#22152=PRODUCT_DEFINITION_SHAPE('',$,#22191);
#22179=SHAPE_REPRESENTATION('',(#9314),#22125);
#22183=PRODUCT_DEFINITION_CONTEXT('part definition',#22218,'design');
#22191=PRODUCT_DEFINITION('2026-11-10-05-10-49-240',
'Socket head cap screw M3x16',#22202,#22183);
#22202=PRODUCT_DEFINITION_FORMATION('',$,#22227);
#22218=APPLICATION_CONTEXT(
'Core Data for Automotive Mechanical Design Process');
#22219=PRODUCT_CONTEXT('part definition',#22218,'mechanical');
#22227=PRODUCT('2026-11-10-05-10-49-240','Socket head cap screw M3x16',
$,(#22219));
#22234=PRESENTATION_STYLE_ASSIGNMENT((#22242));
#22242=SURFACE_STYLE_USAGE(.BOTH.,#22250);
#22250=SURFACE_SIDE_STYLE('',(#22258));
#22258=SURFACE_STYLE_FILL_AREA(#22266);
#22266=FILL_AREA_STYLE('Dark gray',(#22274));
#22274=FILL_AREA_STYLE_COLOUR('Dark gray',#22282);
#22282=COLOUR_RGB('Dark gray',0.250980392156863,0.282352941176471,0.32156862745098);
ENDSEC;
END-ISO-10303-21;
